ISO-10303-21;
HEADER;
FILE_DESCRIPTION (('STEP AP214'),
    '1' );
FILE_NAME ('short pitch roller chain wheel_s_iso_Chain wheel ISO - 20Z 05B-1 --20SA8.0N.step',
    '2026-10-08T05:56:58',
    ( '' ),
    ( '' ),
    'SwSTEP 2.0',
    'SolidWorks 2026',
    '' );
FILE_SCHEMA (( 'AUTOMOTIVE_DESIGN' ));
ENDSEC;

DATA;
#2=CARTESIAN_POINT ( 'NONE',  ( 0.07186808533286707934, 10.24630254990548650, -23.19485392143201707 ) ) ;
#5=VECTOR ( 'NONE', #6897, 1000.000000000000000 ) ;
#9=CARTESIAN_POINT ( 'NONE',  ( 2.257825462012207574, 23.74442027961379864, -12.96514671151741638 ) ) ;
#17=B_SPLINE_CURVE_WITH_KNOTS ( 'NONE', 3,
 ( #2444, #6941, #2258, #8559, #14668, #14761 ),
 .UNSPECIFIED., .F., .F.,
 ( 4, 2, 4 ),
 ( 4.462636731831954487E-07, 0.001879885066974966781, 0.003759323870276750149 ),
 .UNSPECIFIED. ) ;
#19=CARTESIAN_POINT ( 'NONE',  ( 2.789999999999999147, -23.17675759782046541, 7.772527002114348882 ) ) ;
#26=ADVANCED_FACE ( 'NONE', ( #15747 ), #18840, .T. ) ;
#31=CARTESIAN_POINT ( 'NONE',  ( 2.789999999999999147, -24.34211360614294506, -7.909232158575071558 ) ) ;
#39=DIRECTION ( 'NONE',  ( -1.000000000000000000, -0.000000000000000000, -0.000000000000000000 ) ) ;
#53=EDGE_LOOP ( 'NONE', ( #13652, #15680, #15664, #19409 ) ) ;
#54=ORIENTED_EDGE ( 'NONE', *, *, #11125, .T. ) ;
#55=CARTESIAN_POINT ( 'NONE',  ( 0.1882238782932349475, -17.47009390565476750, -19.18368891937510412 ) ) ;
#58=B_SPLINE_CURVE_WITH_KNOTS ( 'NONE', 3,
 ( #4738, #3235, #18159, #5934, #19743, #13850 ),
 .UNSPECIFIED., .F., .F.,
 ( 4, 2, 4 ),
 ( 4.462636882236601199E-07, 0.001879885203074806947, 0.003759324142461389993 ),
 .UNSPECIFIED. ) ;
#59=VERTEX_POINT ( 'NONE', #14445 ) ;
#64=VECTOR ( 'NONE', #5510, 1000.000000000000000 ) ;
#67=DIRECTION ( 'NONE',  ( -1.000000000000000000, 0.000000000000000000, 0.000000000000000000 ) ) ;
#71=B_SPLINE_CURVE_WITH_KNOTS ( 'NONE', 3,
 ( #7909, #17128, #18622, #4920 ),
 .UNSPECIFIED., .F., .F.,
 ( 4, 4 ),
 ( 0.005258110598983589158, 0.005948376585272731332 ),
 .UNSPECIFIED. ) ;
#72=CARTESIAN_POINT ( 'NONE',  ( 0.02436607992776411782, 22.71065055754465689, -9.836394144775473691 ) ) ;
#75=ORIENTED_EDGE ( 'NONE', *, *, #12842, .F. ) ;
#76=CARTESIAN_POINT ( 'NONE',  ( 2.789999999999999147, 19.64056340710875048, -14.55412442567624609 ) ) ;
#77=AXIS2_PLACEMENT_3D ( 'NONE', #8605, #16216, #8311 ) ;
#80=CARTESIAN_POINT ( 'NONE',  ( 2.789999999999999147, -15.04425356660744839, -18.18163861606288378 ) ) ;
#82=CARTESIAN_POINT ( 'NONE',  ( 2.765633920072239516, 21.30679549418631780, 12.59161484032919986 ) ) ;
#87=VECTOR ( 'NONE', #9663, 1000.000000000000000 ) ;
#89=ORIENTED_EDGE ( 'NONE', *, *, #3339, .T. ) ;
#95=DIRECTION ( 'NONE',  ( -1.000000000000000000, -0.000000000000000000, 0.000000000000000000 ) ) ;
#101=CARTESIAN_POINT ( 'NONE',  ( 1.749999999999998002, -12.52377138324241734, 25.12109765559649688 ) ) ;
#113=FACE_OUTER_BOUND ( 'NONE', #17596, .T. ) ;
#114=DIRECTION ( 'NONE',  ( -1.000000000000000000, -0.000000000000000000, -0.000000000000000000 ) ) ;
#116=AXIS2_PLACEMENT_3D ( 'NONE', #3393, #4893, #17196 ) ;
#117=CARTESIAN_POINT ( 'NONE',  ( 1.749999999999998002, -4.633866840648726004, -27.68468304288263582 ) ) ;
#119=ORIENTED_EDGE ( 'NONE', *, *, #8237, .F. ) ;
#120=( GEOMETRIC_REPRESENTATION_CONTEXT ( 3 ) GLOBAL_UNCERTAINTY_ASSIGNED_CONTEXT ( ( #987 ) ) GLOBAL_UNIT_ASSIGNED_CONTEXT ( ( #1597, #16819, #7588 ) ) REPRESENTATION_CONTEXT ( 'NONE', 'WORKASPACE' ) );
#121=LINE ( 'NONE', #4819, #1475 ) ;
#125=DIRECTION ( 'NONE',  ( -1.000000000000000000, -0.000000000000000000, -0.000000000000000000 ) ) ;
#132=CARTESIAN_POINT ( 'NONE',  ( 2.631259771887293653, -22.38003579136350396, 12.81821841996065636 ) ) ;
#135=CARTESIAN_POINT ( 'NONE',  ( 0.1855656748306462045, -2.851997810081830842, 25.77772010606605235 ) ) ;
#136=ORIENTED_EDGE ( 'NONE', *, *, #8190, .F. ) ;
#137=DIRECTION ( 'NONE',  ( 0.000000000000000000, 0.000000000000000000, 1.000000000000000000 ) ) ;
#141=EDGE_LOOP ( 'NONE', ( #3157, #7243, #2430, #12729, #17262, #10969 ) ) ;
#142=VECTOR ( 'NONE', #16132, 1000.000000000000000 ) ;
#144=CARTESIAN_POINT ( 'NONE',  ( 2.790000000000076419, -22.38018801136469094, -9.515416771311432598 ) ) ;
#162=EDGE_CURVE ( 'NONE', #18627, #6765, #11284, .T. ) ;
#164=CYLINDRICAL_SURFACE ( 'NONE', #11252, 13.19999999999999929 ) ;
#167=EDGE_CURVE ( 'NONE', #11813, #19442, #2963, .T. ) ;
#172=ORIENTED_EDGE ( 'NONE', *, *, #5127, .T. ) ;
#173=CARTESIAN_POINT ( 'NONE',  ( -7.634507448887241432E-14, 22.38018801136490055, -9.515416771310970745 ) ) ;
#181=CARTESIAN_POINT ( 'NONE',  ( 8.000000000000000000, 0.000000000000000000, 0.000000000000000000 ) ) ;
#185=ORIENTED_EDGE ( 'NONE', *, *, #222, .T. ) ;
#191=CARTESIAN_POINT ( 'NONE',  ( 1.039999999999997593, 0.000000000000000000, 0.000000000000000000 ) ) ;
#194=DIRECTION ( 'NONE',  ( -1.000000000000000000, -0.000000000000000000, 0.000000000000000000 ) ) ;
#196=VERTEX_POINT ( 'NONE', #4350 ) ;
#200=DIRECTION ( 'NONE',  ( 0.000000000000000000, 0.000000000000000000, 1.000000000000000000 ) ) ;
#202=DIRECTION ( 'NONE',  ( -1.000000000000000000, -0.000000000000000000, -0.000000000000000000 ) ) ;
#204=LINE ( 'NONE', #3197, #2253 ) ;
#212=ORIENTED_EDGE ( 'NONE', *, *, #10668, .T. ) ;
#215=ORIENTED_EDGE ( 'NONE', *, *, #17541, .F. ) ;
#222=EDGE_CURVE ( 'NONE', #241, #19442, #19105, .T. ) ;
#224=EDGE_LOOP ( 'NONE', ( #18143, #6308, #7180, #10221, #12160, #16054 ) ) ;
#227=CARTESIAN_POINT ( 'NONE',  ( 0.02436607992776325046, -24.15498966839958683, -5.391175441198872598 ) ) ;
#233=ORIENTED_EDGE ( 'NONE', *, *, #5523, .T. ) ;
#238=ORIENTED_EDGE ( 'NONE', *, *, #5736, .T. ) ;
#239=CARTESIAN_POINT ( 'NONE',  ( 2.790000000000000036, 20.85230829256853013, 12.51294990530023732 ) ) ;
#241=VERTEX_POINT ( 'NONE', #6034 ) ;
#242=CARTESIAN_POINT ( 'NONE',  ( 2.030753602223784871, 27.14986936243581184, -4.828194074574073902 ) ) ;
#244=ADVANCED_FACE ( 'NONE', ( #13550 ), #6454, .T. ) ;
#248=ORIENTED_EDGE ( 'NONE', *, *, #1052, .F. ) ;
#250=CARTESIAN_POINT ( 'NONE',  ( 0.02436607992776151574, 24.15498966839970052, -5.391175441198366336 ) ) ;
#253=VERTEX_POINT ( 'NONE', #1447 ) ;
#254=ORIENTED_EDGE ( 'NONE', *, *, #5488, .T. ) ;
#255=CARTESIAN_POINT ( 'NONE',  ( 0.02436607992776411782, -16.37294372382844543, -18.55949924794910544 ) ) ;
#262=CARTESIAN_POINT ( 'NONE',  ( 2.789999999999999147, 24.15498966839970052, -5.391175441198366336 ) ) ;
#263=EDGE_CURVE ( 'NONE', #17130, #17826, #3141, .T. ) ;
#272=CARTESIAN_POINT ( 'NONE',  ( 2.030753603471112889, -12.98165646470063983, -24.32906614999630790 ) ) ;
#280=ORIENTED_EDGE ( 'NONE', *, *, #9401, .T. ) ;
#281=CARTESIAN_POINT ( 'NONE',  ( 1.394999999999999574, -19.67366047555515607, -20.02152543075367319 ) ) ;
#283=VERTEX_POINT ( 'NONE', #13651 ) ;
#287=DIRECTION ( 'NONE',  ( 0.000000000000000000, 0.000000000000000000, 1.000000000000000000 ) ) ;
#290=CYLINDRICAL_SURFACE ( 'NONE', #1072, 13.19999999999999929 ) ;
#291=CARTESIAN_POINT ( 'NONE',  ( -6.403158385254602634E-17, -23.69843731927173991, 5.456805104201007950 ) ) ;
#298=VERTEX_POINT ( 'NONE', #551 ) ;
#302=CARTESIAN_POINT ( 'NONE',  ( 0.02436607992776325046, -18.55949924794904504, 16.37294372382852004 ) ) ;
#303=VERTEX_POINT ( 'NONE', #15551 ) ;
#309=B_SPLINE_CURVE_WITH_KNOTS ( 'NONE', 3,
 ( #72, #13681, #173, #13881 ),
 .UNSPECIFIED., .F., .F.,
 ( 4, 4 ),
 ( 3.059063720795852959E-07, 0.0006888942284914018055 ),
 .UNSPECIFIED. ) ;
#311=CIRCLE ( 'NONE', #4137, 28.06981291497571007 ) ;
#312=VERTEX_POINT ( 'NONE', #643 ) ;
#313=CARTESIAN_POINT ( 'NONE',  ( 8.000000000000000000, 0.000000000000000000, 0.000000000000000000 ) ) ;
#317=CYLINDRICAL_SURFACE ( 'NONE', #4942, 28.06981291497571362 ) ;
#318=ORIENTED_EDGE ( 'NONE', *, *, #3578, .F. ) ;
#323=B_SPLINE_CURVE_WITH_KNOTS ( 'NONE', 3,
 ( #16486, #1173, #972, #14689 ),
 .UNSPECIFIED., .F., .F.,
 ( 4, 4 ),
 ( 0.005258120783916789796, 0.005948386350302923772 ),
 .UNSPECIFIED. ) ;
#324=CIRCLE ( 'NONE', #2869, 2.524999999999995914 ) ;
#326=B_SPLINE_CURVE_WITH_KNOTS ( 'NONE', 3,
 ( #1232, #13430, #19527, #11936, #18048, #15038 ),
 .UNSPECIFIED., .F., .F.,
 ( 4, 2, 4 ),
 ( 4.462636793144857890E-07, 0.001879885123570645663, 0.003759323983461976531 ),
 .UNSPECIFIED. ) ;
#327=LINE ( 'NONE', #14033, #13965 ) ;
#331=CARTESIAN_POINT ( 'NONE',  ( 0.8291131470075423504, 24.44424927289185945, 12.96989951879416125 ) ) ;
#332=DIRECTION ( 'NONE',  ( 0.000000000000000000, 0.000000000000000000, 1.000000000000000000 ) ) ;
#338=DIRECTION ( 'NONE',  ( 0.000000000000000000, 0.000000000000000000, 1.000000000000000000 ) ) ;
#339=ORIENTED_EDGE ( 'NONE', *, *, #167, .F. ) ;
#349=CARTESIAN_POINT ( 'NONE',  ( 0.000000000000000000, 9.324097380959777581, -22.25075486061729535 ) ) ;
#351=FACE_OUTER_BOUND ( 'NONE', #6860, .T. ) ;
#361=EDGE_LOOP ( 'NONE', ( #9949, #14872, #12238, #18808 ) ) ;
#363=( NAMED_UNIT ( * ) PLANE_ANGLE_UNIT ( ) SI_UNIT ( $, .RADIAN. ) );
#367=CARTESIAN_POINT ( 'NONE',  ( -7.372183127218402931E-16, -20.85230829256862961, 12.51294990530008988 ) ) ;
#374=AXIS2_PLACEMENT_3D ( 'NONE', #709, #6787, #13013 ) ;
#375=ORIENTED_EDGE ( 'NONE', *, *, #4815, .F. ) ;
#376=CARTESIAN_POINT ( 'NONE',  ( 1.039999999999996483, -19.67366047555544384, 20.02152543075338897 ) ) ;
#378=EDGE_CURVE ( 'NONE', #12550, #10168, #4252, .T. ) ;
#384=CARTESIAN_POINT ( 'NONE',  ( 0.000000000000000000, -7.909232158574647009, -24.34211360614308006 ) ) ;
#387=ORIENTED_EDGE ( 'NONE', *, *, #12742, .F. ) ;
#395=EDGE_LOOP ( 'NONE', ( #14835, #13456, #12249, #10403 ) ) ;
#398=CARTESIAN_POINT ( 'NONE',  ( 2.765633920072235963, -5.391175441198450713, -24.15498966839968276 ) ) ;
#401=CARTESIAN_POINT ( 'NONE',  ( 1.749999999999998002, 25.12109765559671004, -12.52377138324198391 ) ) ;
#403=ORIENTED_EDGE ( 'NONE', *, *, #6295, .F. ) ;
#405=DIRECTION ( 'NONE',  ( 1.000000000000000000, 0.000000000000000000, 0.000000000000000000 ) ) ;
#408=EDGE_CURVE ( 'NONE', #12256, #1337, #17055, .T. ) ;
#419=CARTESIAN_POINT ( 'NONE',  ( 0.000000000000000000, -25.59481291497571220, -1.787276233276378314E-13 ) ) ;
#420=ORIENTED_EDGE ( 'NONE', *, *, #3095, .T. ) ;
#423=EDGE_CURVE ( 'NONE', #17227, #18545, #14802, .T. ) ;
#428=B_SPLINE_CURVE_WITH_KNOTS ( 'NONE', 3,
 ( #14907, #7276, #7374, #13499, #10410, #7684 ),
 .UNSPECIFIED., .F., .F.,
 ( 4, 2, 4 ),
 ( 2.132675795043207789E-07, 0.001878604073277004988, 0.003756994878974505639 ),
 .UNSPECIFIED. ) ;
#429=EDGE_CURVE ( 'NONE', #1337, #18773, #8416, .T. ) ;
#432=DIRECTION ( 'NONE',  ( 0.000000000000000000, 0.000000000000000000, 1.000000000000000000 ) ) ;
#433=CIRCLE ( 'NONE', #15125, 24.12539914357697413 ) ;
#436=B_SPLINE_CURVE_WITH_KNOTS ( 'NONE', 3,
 ( #7801, #2, #10814, #16923, #1712, #13914 ),
 .UNSPECIFIED., .F., .F.,
 ( 4, 2, 4 ),
 ( 2.586195665735896780E-07, 0.001878649493629692057, 0.003757040367692810780 ),
 .UNSPECIFIED. ) ;
#439=DIRECTION ( 'NONE',  ( -1.000000000000000000, -0.000000000000000000, -0.000000000000000000 ) ) ;
#447=CARTESIAN_POINT ( 'NONE',  ( 0.02436607992776628623, 24.63872515616082737, -2.336989772644355590 ) ) ;
#451=SHAPE_REPRESENTATION ( 'short pitch roller chain wheel_s_iso_Chain wheel ISO - 20Z 05B-1 --20SA8.0N', ( #16724 ), #120 ) ;
#453=EDGE_CURVE ( 'NONE', #4439, #253, #13521, .T. ) ;
#456=EDGE_CURVE ( 'NONE', #15001, #196, #433, .T. ) ;
#460=CARTESIAN_POINT ( 'NONE',  ( 2.789999999999999147, 24.34211360614300190, 7.909232158574900140 ) ) ;
#465=EDGE_CURVE ( 'NONE', #9137, #16676, #4084, .T. ) ;
#471=B_SPLINE_CURVE_WITH_KNOTS ( 'NONE', 3,
 ( #16379, #8875, #2659, #8775 ),
 .UNSPECIFIED., .F., .F.,
 ( 4, 4 ),
 ( 0.005258214619651984008, 0.005948481662034168192 ),
 .UNSPECIFIED. ) ;
#472=CARTESIAN_POINT ( 'NONE',  ( 0.000000000000000000, 20.62201879784911540, 12.52067188844362100 ) ) ;
#479=VERTEX_POINT ( 'NONE', #7106 ) ;
#484=ORIENTED_EDGE ( 'NONE', *, *, #3994, .T. ) ;
#486=B_SPLINE_CURVE_WITH_KNOTS ( 'NONE', 3,
 ( #997, #905, #15546, #3338 ),
 .UNSPECIFIED., .F., .F.,
 ( 4, 4 ),
 ( 2.324263106257895883E-07, 0.0006888201370294903293 ),
 .UNSPECIFIED. ) ;
#493=DIRECTION ( 'NONE',  ( -1.000000000000000000, -0.000000000000000000, -0.000000000000000000 ) ) ;
#495=CARTESIAN_POINT ( 'NONE',  ( 0.7592463941534238758, 3.797885586973211325, 27.31305418910211458 ) ) ;
#503=EDGE_CURVE ( 'NONE', #12346, #5672, #2341, .T. ) ;
#507=CARTESIAN_POINT ( 'NONE',  ( 2.783025325906567371, -24.42374957165203853, -2.249040938978752013 ) ) ;
#508=CARTESIAN_POINT ( 'NONE',  ( 2.789999999999999147, -5.535312321042557215, -23.48180575137735815 ) ) ;
#515=DIRECTION ( 'NONE',  ( 1.000000000000000000, 0.000000000000000000, -0.000000000000000000 ) ) ;
#519=AXIS2_PLACEMENT_3D ( 'NONE', #1734, #18343, #15443 ) ;
#520=ORIENTED_EDGE ( 'NONE', *, *, #17895, .F. ) ;
#522=DIRECTION ( 'NONE',  ( -1.000000000000000000, -0.000000000000000000, -0.000000000000000000 ) ) ;
#523=ORIENTED_EDGE ( 'NONE', *, *, #4370, .F. ) ;
#525=DIRECTION ( 'NONE',  ( -1.000000000000000000, 0.000000000000000000, 0.000000000000000000 ) ) ;
#528=EDGE_LOOP ( 'NONE', ( #18613, #17354, #7427, #17792, #19667, #11057 ) ) ;
#539=CARTESIAN_POINT ( 'NONE',  ( 0.5279272933715194460, 19.66369668717032937, 18.56460150496945971 ) ) ;
#540=VERTEX_POINT ( 'NONE', #1616 ) ;
#543=CARTESIAN_POINT ( 'NONE',  ( 1.749999999999998002, 0.000000000000000000, 0.000000000000000000 ) ) ;
#549=B_SPLINE_CURVE_WITH_KNOTS ( 'NONE', 3,
 ( #17300, #8294, #9715, #15905 ),
 .UNSPECIFIED., .F., .F.,
 ( 4, 4 ),
 ( 3.059063720746924101E-07, 0.0006888942284913933487 ),
 .UNSPECIFIED. ) ;
#551=CARTESIAN_POINT ( 'NONE',  ( 0.02436607992776281678, 2.336989772644269436, 24.63872515616083447 ) ) ;
#552=ORIENTED_EDGE ( 'NONE', *, *, #14437, .T. ) ;
#553=CARTESIAN_POINT ( 'NONE',  ( 2.789999999999999147, -16.37294372382871188, 18.55949924794887096 ) ) ;
#568=ORIENTED_EDGE ( 'NONE', *, *, #14160, .F. ) ;
#569=VERTEX_POINT ( 'NONE', #18234 ) ;
#570=CIRCLE ( 'NONE', #12063, 2.524999999999995914 ) ;
#572=AXIS2_PLACEMENT_3D ( 'NONE', #18958, #5144, #9567 ) ;
#577=CYLINDRICAL_SURFACE ( 'NONE', #2328, 13.19999999999999929 ) ;
#581=B_SPLINE_CURVE_WITH_KNOTS ( 'NONE', 3,
 ( #3144, #12451, #4841, #13951, #18645, #4946 ),
 .UNSPECIFIED., .F., .F.,
 ( 4, 2, 4 ),
 ( 4.462636882221166670E-07, 0.001879885203074807814, 0.003759324142461393462 ),
 .UNSPECIFIED. ) ;
#583=AXIS2_PLACEMENT_3D ( 'NONE', #18408, #5087, #17013 ) ;
#592=CYLINDRICAL_SURFACE ( 'NONE', #9309, 28.06981291497571362 ) ;
#605=CARTESIAN_POINT ( 'NONE',  ( 0.000000000000000000, 22.25075486061737351, 9.324097380959511128 ) ) ;
#607=EDGE_CURVE ( 'NONE', #9627, #16718, #13871, .T. ) ;
#608=VERTEX_POINT ( 'NONE', #10727 ) ;
#609=DIRECTION ( 'NONE',  ( -1.000000000000000000, -0.000000000000000000, -0.000000000000000000 ) ) ;
#619=VERTEX_POINT ( 'NONE', #10824 ) ;
#621=CARTESIAN_POINT ( 'NONE',  ( 2.789999999999999147, 24.04302995059966364, 1.991882183130384121 ) ) ;
#623=ORIENTED_EDGE ( 'NONE', *, *, #8596, .T. ) ;
#626=VECTOR ( 'NONE', #14370, 1000.000000000000000 ) ;
#627=DIRECTION ( 'NONE',  ( -1.000000000000000000, 0.000000000000000000, 0.000000000000000000 ) ) ;
#630=CARTESIAN_POINT ( 'NONE',  ( 0.5321745379877897975, 12.96514671151801323, -23.74442027961346113 ) ) ;
#632=CARTESIAN_POINT ( 'NONE',  ( 0.000000000000000000, -22.25075486061745167, 9.324097380959385006 ) ) ;
#633=AXIS2_PLACEMENT_3D ( 'NONE', #11254, #17358, #4851 ) ;
#637=DIRECTION ( 'NONE',  ( 0.000000000000000000, 0.000000000000000000, 1.000000000000000000 ) ) ;
#638=ADVANCED_FACE ( 'NONE', ( #7400 ), #13014, .T. ) ;
#643=CARTESIAN_POINT ( 'NONE',  ( 0.02436607992776585255, -5.391175441198789109, 24.15498966839961170 ) ) ;
#650=EDGE_CURVE ( 'NONE', #1292, #12256, #16241, .T. ) ;
#658=DIRECTION ( 'NONE',  ( -1.000000000000000000, 0.000000000000000000, 0.000000000000000000 ) ) ;
#661=ORIENTED_EDGE ( 'NONE', *, *, #17194, .F. ) ;
#665=CARTESIAN_POINT ( 'NONE',  ( 1.749999999999998002, 25.12109765559653596, 12.52377138324232675 ) ) ;
#671=CARTESIAN_POINT ( 'NONE',  ( 0.7592463977762113903, 27.14986936243574078, 4.828194074574446049 ) ) ;
#680=CYLINDRICAL_SURFACE ( 'NONE', #3555, 2.524999999999995914 ) ;
#683=CARTESIAN_POINT ( 'NONE',  ( 0.000000000000000000, -23.48180575137736170, 5.535312321042622052 ) ) ;
#688=CARTESIAN_POINT ( 'NONE',  ( 2.765633920072239516, 16.37294372382858398, 18.55949924794898465 ) ) ;
#691=CARTESIAN_POINT ( 'NONE',  ( 0.1855655959470677019, -19.17825124759764677, -17.45907811351477079 ) ) ;
#694=CARTESIAN_POINT ( 'NONE',  ( 1.394999999999999574, -27.68468304288262161, 4.633866840648820151 ) ) ;
#709=CARTESIAN_POINT ( 'NONE',  ( 2.789999999999999147, -23.31896751603337137, 7.334849878007427826 ) ) ;
#714=CARTESIAN_POINT ( 'NONE',  ( 2.030753602223783538, 4.828194074574346573, 27.14986936243576565 ) ) ;
#719=DIRECTION ( 'NONE',  ( -1.000000000000000000, 0.000000000000000000, 0.000000000000000000 ) ) ;
#721=DIRECTION ( 'NONE',  ( -1.000000000000000000, 0.000000000000000000, 0.000000000000000000 ) ) ;
#725=VERTEX_POINT ( 'NONE', #9325 ) ;
#728=CARTESIAN_POINT ( 'NONE',  ( 2.765633920072239516, -2.336989772644097574, -24.63872515616085224 ) ) ;
#729=ORIENTED_EDGE ( 'NONE', *, *, #5218, .T. ) ;
#734=TOROIDAL_SURFACE ( 'NONE', #17664, 24.12539914357697413, 8.000000000000000000 ) ;
#737=AXIS2_PLACEMENT_3D ( 'NONE', #19098, #609, #6683 ) ;
#739=CARTESIAN_POINT ( 'NONE',  ( 2.789999999999999147, -22.71065055754459650, 9.836394144775621129 ) ) ;
#740=ORIENTED_EDGE ( 'NONE', *, *, #3539, .T. ) ;
#741=AXIS2_PLACEMENT_3D ( 'NONE', #12660, #7645, #17254 ) ;
#746=ADVANCED_FACE ( 'NONE', ( #7179 ), #9075, .T. ) ;
#747=ORIENTED_EDGE ( 'NONE', *, *, #8475, .F. ) ;
#751=CARTESIAN_POINT ( 'NONE',  ( 1.039999999999996039, 19.67366047555559305, -20.02152543075323976 ) ) ;
#756=VECTOR ( 'NONE', #1088, 1000.000000000000000 ) ;
#758=VERTEX_POINT ( 'NONE', #14421 ) ;
#761=DIRECTION ( 'NONE',  ( -1.000000000000000000, -0.000000000000000000, -0.000000000000000000 ) ) ;
#769=VECTOR ( 'NONE', #719, 1000.000000000000000 ) ;
#785=DIRECTION ( 'NONE',  ( -1.000000000000000000, -0.000000000000000000, -0.000000000000000000 ) ) ;
#786=AXIS2_PLACEMENT_3D ( 'NONE', #14254, #7938, #12454 ) ;
#789=CARTESIAN_POINT ( 'NONE',  ( 1.749999999999998002, 0.000000000000000000, 0.000000000000000000 ) ) ;
#791=AXIS2_PLACEMENT_3D ( 'NONE', #5408, #8423, #8809 ) ;
#806=DIRECTION ( 'NONE',  ( 0.000000000000000000, 0.000000000000000000, 1.000000000000000000 ) ) ;
#810=DIRECTION ( 'NONE',  ( -1.000000000000000000, 0.000000000000000000, 0.000000000000000000 ) ) ;
#811=ADVANCED_FACE ( 'NONE', ( #819 ), #5404, .T. ) ;
#812=CARTESIAN_POINT ( 'NONE',  ( 2.789999999999999147, 12.52067188844351442, 20.62201879784917935 ) ) ;
#819=FACE_OUTER_BOUND ( 'NONE', #16646, .T. ) ;
#831=CYLINDRICAL_SURFACE ( 'NONE', #13469, 13.19999999999999929 ) ;
#836=B_SPLINE_CURVE_WITH_KNOTS ( 'NONE', 3,
 ( #844, #7013, #11538, #2423 ),
 .UNSPECIFIED., .F., .F.,
 ( 4, 4 ),
 ( 0.005258105385878707357, 0.005948373736081385803 ),
 .UNSPECIFIED. ) ;
#840=EDGE_CURVE ( 'NONE', #6761, #4306, #6819, .T. ) ;
#844=CARTESIAN_POINT ( 'NONE',  ( 0.000000000000000000, 9.324097380959777581, -22.25075486061729535 ) ) ;
#848=ORIENTED_EDGE ( 'NONE', *, *, #11223, .F. ) ;
#849=CARTESIAN_POINT ( 'NONE',  ( 0.7592463977762105021, -27.14986936243570526, -4.828194074574642336 ) ) ;
#850=ORIENTED_EDGE ( 'NONE', *, *, #16620, .T. ) ;
#852=CYLINDRICAL_SURFACE ( 'NONE', #12511, 2.524999999999995914 ) ;
#853=ORIENTED_EDGE ( 'NONE', *, *, #15946, .F. ) ;
#858=EDGE_CURVE ( 'NONE', #1292, #4347, #3906, .T. ) ;
#861=EDGE_CURVE ( 'NONE', #6715, #196, #5862, .T. ) ;
#866=VECTOR ( 'NONE', #8883, 1000.000000000000000 ) ;
#872=CARTESIAN_POINT ( 'NONE',  ( 2.789999999999999147, -9.514945144208585504, -22.37986894186682107 ) ) ;
#873=EDGE_CURVE ( 'NONE', #3731, #5937, #2990, .T. ) ;
#874=CARTESIAN_POINT ( 'NONE',  ( 2.718131885465892239, -16.91241718341984779, -18.89333555428573774 ) ) ;
#879=EDGE_CURVE ( 'NONE', #7960, #312, #16126, .T. ) ;
#881=VERTEX_POINT ( 'NONE', #3710 ) ;
#882=FACE_OUTER_BOUND ( 'NONE', #16027, .T. ) ;
#890=CARTESIAN_POINT ( 'NONE',  ( 2.765633920072235075, -12.59161484032896361, -21.30679549418645280 ) ) ;
#891=ORIENTED_EDGE ( 'NONE', *, *, #3139, .T. ) ;
#892=EDGE_CURVE ( 'NONE', #18407, #15571, #10660, .T. ) ;
#899=FACE_OUTER_BOUND ( 'NONE', #11788, .T. ) ;
#905=CARTESIAN_POINT ( 'NONE',  ( 2.783025306068356741, 18.43727551351032190, 16.17543236987995314 ) ) ;
#910=DIRECTION ( 'NONE',  ( 0.000000000000000000, 0.000000000000000000, 1.000000000000000000 ) ) ;
#919=ORIENTED_EDGE ( 'NONE', *, *, #12816, .T. ) ;
#921=CARTESIAN_POINT ( 'NONE',  ( 0.02436607992776455150, 5.391175441198956086, -24.15498966839956907 ) ) ;
#938=ADVANCED_FACE ( 'NONE', ( #5984 ), #16710, .F. ) ;
#941=VERTEX_POINT ( 'NONE', #7583 ) ;
#946=ORIENTED_EDGE ( 'NONE', *, *, #18987, .F. ) ;
#948=LINE ( 'NONE', #5142, #3038 ) ;
#950=ADVANCED_FACE ( 'NONE', ( #16412 ), #6083, .T. ) ;
#955=DIRECTION ( 'NONE',  ( 0.000000000000000000, 0.000000000000000000, 1.000000000000000000 ) ) ;
#966=ADVANCED_FACE ( 'NONE', ( #2687 ), #16816, .F. ) ;
#969=DIRECTION ( 'NONE',  ( -1.000000000000000000, -0.000000000000000000, -0.000000000000000000 ) ) ;
#972=CARTESIAN_POINT ( 'NONE',  ( 0.006931054464085153848, 2.248820353273311756, -24.42321038836780644 ) ) ;
#974=AXIS2_PLACEMENT_3D ( 'NONE', #1599, #16821, #7888 ) ;
#975=CARTESIAN_POINT ( 'NONE',  ( 2.262072769566604080, -11.57956866523201178, -24.43806413951687873 ) ) ;
#977=EDGE_CURVE ( 'NONE', #5363, #18719, #18306, .T. ) ;
#978=DIRECTION ( 'NONE',  ( 0.000000000000000000, 0.000000000000000000, 1.000000000000000000 ) ) ;
#985=EDGE_CURVE ( 'NONE', #15288, #59, #8806, .T. ) ;
#987=UNCERTAINTY_MEASURE_WITH_UNIT (LENGTH_MEASURE( 1.000000000000000082E-05 ), #1597, 'distance_accuracy_value', 'NONE');
#991=CIRCLE ( 'NONE', #15371, 24.12539914357697768 ) ;
#993=VERTEX_POINT ( 'NONE', #17908 ) ;
#994=CARTESIAN_POINT ( 'NONE',  ( 2.789999999999999147, -18.28042085475266276, -15.74360496233401996 ) ) ;
#997=CARTESIAN_POINT ( 'NONE',  ( 2.765633920072235519, 18.55949924794892780, 16.37294372382865504 ) ) ;
#998=DIRECTION ( 'NONE',  ( -1.000000000000000000, 0.000000000000000000, 0.000000000000000000 ) ) ;
#999=CARTESIAN_POINT ( 'NONE',  ( 2.789999999999999147, -15.74360496233394002, 18.28042085475272671 ) ) ;
#1000=ORIENTED_EDGE ( 'NONE', *, *, #10017, .T. ) ;
#1001=AXIS2_PLACEMENT_3D ( 'NONE', #3476, #9794, #9585 ) ;
#1003=CARTESIAN_POINT ( 'NONE',  ( 2.601776121706764311, -19.18368891937477727, -17.47009390565512632 ) ) ;
#1007=CARTESIAN_POINT ( 'NONE',  ( 1.039999999999997371, -4.147968289691092991, -27.76164181293055933 ) ) ;
#1008=EDGE_CURVE ( 'NONE', #9627, #14187, #12006, .T. ) ;
#1013=VERTEX_POINT ( 'NONE', #5784 ) ;
#1015=CARTESIAN_POINT ( 'NONE',  ( 2.789999999999999147, -2.336989772644440855, 24.63872515616082026 ) ) ;
#1023=EDGE_CURVE ( 'NONE', #1471, #15059, #3313, .T. ) ;
#1029=B_SPLINE_CURVE_WITH_KNOTS ( 'NONE', 3,
 ( #17819, #16318, #7089, #16224 ),
 .UNSPECIFIED., .F., .F.,
 ( 4, 4 ),
 ( 1.981826382900813409E-07, 0.0006887856082032216450 ),
 .UNSPECIFIED. ) ;
#1032=ORIENTED_EDGE ( 'NONE', *, *, #7222, .T. ) ;
#1033=DIRECTION ( 'NONE',  ( -1.000000000000000000, 0.000000000000000000, -0.000000000000000000 ) ) ;
#1034=AXIS2_PLACEMENT_3D ( 'NONE', #3290, #9404, #10094 ) ;
#1038=CARTESIAN_POINT ( 'NONE',  ( 2.257825491203655943, -24.44564404695836402, -11.58891744060133355 ) ) ;
#1039=TOROIDAL_SURFACE ( 'NONE', #8382, 24.12539914357697768, 8.000000000000000000 ) ;
#1046=AXIS2_PLACEMENT_3D ( 'NONE', #7959, #6258, #16985 ) ;
#1047=DIRECTION ( 'NONE',  ( -1.000000000000000000, 0.000000000000000000, 0.000000000000000000 ) ) ;
#1048=EDGE_CURVE ( 'NONE', #10126, #13404, #8108, .T. ) ;
#1049=TOROIDAL_SURFACE ( 'NONE', #4235, 24.12539914357697768, 8.000000000000000000 ) ;
#1052=EDGE_CURVE ( 'NONE', #11676, #59, #3252, .T. ) ;
#1054=CARTESIAN_POINT ( 'NONE',  ( 0.006931069955679000985, 16.17493693894905959, -18.43696893154741190 ) ) ;
#1055=EDGE_CURVE ( 'NONE', #11999, #7717, #12788, .T. ) ;
#1056=AXIS2_PLACEMENT_3D ( 'NONE', #2528, #10810, #9310 ) ;
#1057=CARTESIAN_POINT ( 'NONE',  ( 2.765633920072238627, -21.30679549418621832, -12.59161484032935618 ) ) ;
#1062=ORIENTED_EDGE ( 'NONE', *, *, #10676, .F. ) ;
#1068=ORIENTED_EDGE ( 'NONE', *, *, #3459, .T. ) ;
#1069=CARTESIAN_POINT ( 'NONE',  ( 0.1855657389739088781, -25.39738473785004302, 5.253342437939627629 ) ) ;
#1070=ORIENTED_EDGE ( 'NONE', *, *, #3622, .F. ) ;
#1072=AXIS2_PLACEMENT_3D ( 'NONE', #18591, #15796, #15599 ) ;
#1078=ADVANCED_FACE ( 'NONE', ( #7789 ), #290, .T. ) ;
#1086=EDGE_LOOP ( 'NONE', ( #14105, #10699, #4262, #2894, #2428, #15632, #5816, #10568 ) ) ;
#1088=DIRECTION ( 'NONE',  ( -1.000000000000000000, 0.000000000000000000, 0.000000000000000000 ) ) ;
#1090=DIRECTION ( 'NONE',  ( 0.000000000000000000, 0.000000000000000000, 1.000000000000000000 ) ) ;
#1092=VECTOR ( 'NONE', #14739, 1000.000000000000000 ) ;
#1094=ADVANCED_FACE ( 'NONE', ( #3490 ), #10996, .F. ) ;
#1096=CARTESIAN_POINT ( 'NONE',  ( 0.07186808533286581646, -23.19485392143207036, -10.24630254990540834 ) ) ;
#1102=CARTESIAN_POINT ( 'NONE',  ( 2.789999999999999147, -24.44424927289185590, -0.2301004812060095106 ) ) ;
#1104=EDGE_CURVE ( 'NONE', #17455, #298, #6560, .T. ) ;
#1105=CARTESIAN_POINT ( 'NONE',  ( 0.000000000000000000, 5.535312321043032391, -23.48180575137725867 ) ) ;
#1120=VERTEX_POINT ( 'NONE', #1984 ) ;
#1127=CARTESIAN_POINT ( 'NONE',  ( 0.07181524296601557444, 18.89296398180216130, -16.91181672897712929 ) ) ;
#1128=EDGE_CURVE ( 'NONE', #12550, #10762, #14243, .T. ) ;
#1133=ORIENTED_EDGE ( 'NONE', *, *, #15532, .F. ) ;
#1134=DIRECTION ( 'NONE',  ( 0.000000000000000000, 0.000000000000000000, 1.000000000000000000 ) ) ;
#1138=ORIENTED_EDGE ( 'NONE', *, *, #8534, .T. ) ;
#1140=CARTESIAN_POINT ( 'NONE',  ( 1.749999999999998002, -27.68468304288262516, 4.633866840648810381 ) ) ;
#1141=CIRCLE ( 'NONE', #6870, 24.12539914357697413 ) ;
#1155=FACE_OUTER_BOUND ( 'NONE', #17530, .T. ) ;
#1157=ORIENTED_EDGE ( 'NONE', *, *, #5900, .F. ) ;
#1162=VERTEX_POINT ( 'NONE', #3983 ) ;
#1168=CARTESIAN_POINT ( 'NONE',  ( 1.039999999999997149, -27.68468304288261805, 4.633866840648821039 ) ) ;
#1173=CARTESIAN_POINT ( 'NONE',  ( 1.774186184918758212E-16, 2.133490293297354956, -24.22479935914658000 ) ) ;
#1178=DIRECTION ( 'NONE',  ( -1.000000000000000000, -0.000000000000000000, -0.000000000000000000 ) ) ;
#1179=DIRECTION ( 'NONE',  ( -1.000000000000000000, 0.000000000000000000, -0.000000000000000000 ) ) ;
#1187=CARTESIAN_POINT ( 'NONE',  ( 2.765633920072235519, -9.836394144775869819, 22.71065055754449347 ) ) ;
#1188=B_SPLINE_CURVE_WITH_KNOTS ( 'NONE', 3,
 ( #16068, #17851, #14568, #4147, #2833, #10651 ),
 .UNSPECIFIED., .F., .F.,
 ( 4, 2, 4 ),
 ( 1.979325885386966398E-07, 0.001878588715165604951, 0.003756979497742671432 ),
 .UNSPECIFIED. ) ;
#1191=ADVANCED_FACE ( 'NONE', ( #6964 ), #14504, .T. ) ;
#1193=ORIENTED_EDGE ( 'NONE', *, *, #3422, .T. ) ;
#1199=CARTESIAN_POINT ( 'NONE',  ( 0.1855656748306449277, 2.851997810082009366, -25.77772010606602748 ) ) ;
#1200=CARTESIAN_POINT ( 'NONE',  ( 2.789999999999999147, -19.64056340710884996, 14.55412442567610931 ) ) ;
#1204=TOROIDAL_SURFACE ( 'NONE', #572, 24.12539914357697768, 8.000000000000000000 ) ;
#1208=CARTESIAN_POINT ( 'NONE',  ( 2.789999999999999147, -15.04425356660744839, -18.18163861606288378 ) ) ;
#1209=ORIENTED_EDGE ( 'NONE', *, *, #3804, .F. ) ;
#1212=CARTESIAN_POINT ( 'NONE',  ( 0.02436607992776194942, -5.391175441198450713, -24.15498966839968276 ) ) ;
#1218=CIRCLE ( 'NONE', #9208, 24.12539914357697413 ) ;
#1219=VERTEX_POINT ( 'NONE', #14599 ) ;
#1221=CYLINDRICAL_SURFACE ( 'NONE', #6122, 13.19999999999999929 ) ;
#1226=CARTESIAN_POINT ( 'NONE',  ( 0.001869172971454433714, -20.90869469097853894, -12.51925356660784594 ) ) ;
#1227=ORIENTED_EDGE ( 'NONE', *, *, #12892, .T. ) ;
#1228=EDGE_CURVE ( 'NONE', #3208, #2962, #13744, .T. ) ;
#1232=CARTESIAN_POINT ( 'NONE',  ( 1.749999999999998002, 20.02152543075346003, 19.67366047555537634 ) ) ;
#1233=ORIENTED_EDGE ( 'NONE', *, *, #17608, .T. ) ;
#1234=CARTESIAN_POINT ( 'NONE',  ( 2.765633920072235963, -16.37294372382871188, 18.55949924794887096 ) ) ;
#1240=CARTESIAN_POINT ( 'NONE',  ( 1.749999999999998002, 12.96210679857786552, 24.89775460606837143 ) ) ;
#1248=CYLINDRICAL_SURFACE ( 'NONE', #7349, 13.19999999999999929 ) ;
#1251=LINE ( 'NONE', #2941, #13207 ) ;
#1252=ORIENTED_EDGE ( 'NONE', *, *, #2254, .T. ) ;
#1257=CARTESIAN_POINT ( 'NONE',  ( 2.765633920072235519, -9.836394144775869819, 22.71065055754449347 ) ) ;
#1259=ORIENTED_EDGE ( 'NONE', *, *, #6877, .F. ) ;
#1267=ORIENTED_EDGE ( 'NONE', *, *, #7190, .F. ) ;
#1271=EDGE_CURVE ( 'NONE', #9660, #13659, #16197, .T. ) ;
#1272=EDGE_CURVE ( 'NONE', #16734, #11638, #15911, .T. ) ;
#1274=DIRECTION ( 'NONE',  ( -1.000000000000000000, 0.000000000000000000, -0.000000000000000000 ) ) ;
#1279=DIRECTION ( 'NONE',  ( -1.000000000000000000, -0.000000000000000000, -0.000000000000000000 ) ) ;
#1281=DIRECTION ( 'NONE',  ( 0.000000000000000000, 0.000000000000000000, -1.000000000000000000 ) ) ;
#1282=B_SPLINE_CURVE_WITH_KNOTS ( 'NONE', 3,
 ( #13247, #11275, #6547, #17273 ),
 .UNSPECIFIED., .F., .F.,
 ( 4, 4 ),
 ( 0.005258120783916793266, 0.005948386350302923772 ),
 .UNSPECIFIED. ) ;
#1284=DIRECTION ( 'NONE',  ( 0.000000000000000000, 0.000000000000000000, 1.000000000000000000 ) ) ;
#1287=CARTESIAN_POINT ( 'NONE',  ( 2.789999999999999147, -9.324097380959603498, 22.25075486061734864 ) ) ;
#1292=VERTEX_POINT ( 'NONE', #3782 ) ;
#1296=CARTESIAN_POINT ( 'NONE',  ( 2.789999999999999147, 0.000000000000000000, 0.000000000000000000 ) ) ;
#1299=ORIENTED_EDGE ( 'NONE', *, *, #2125, .F. ) ;
#1301=PRESENTATION_STYLE_ASSIGNMENT (( #3093 ) ) ;
#1302=DIRECTION ( 'NONE',  ( -1.000000000000000000, 0.000000000000000000, -0.000000000000000000 ) ) ;
#1304=ORIENTED_EDGE ( 'NONE', *, *, #4647, .T. ) ;
#1316=EDGE_LOOP ( 'NONE', ( #3437, #8697, #2402, #4230 ) ) ;
#1318=AXIS2_PLACEMENT_3D ( 'NONE', #3845, #11458, #5724 ) ;
#1321=ORIENTED_EDGE ( 'NONE', *, *, #8475, .T. ) ;
#1327=FACE_OUTER_BOUND ( 'NONE', #9120, .T. ) ;
#1328=VERTEX_POINT ( 'NONE', #18186 ) ;
#1336=CARTESIAN_POINT ( 'NONE',  ( 2.604434404052930141, 19.17825124759803401, -17.45907811351434802 ) ) ;
#1337=VERTEX_POINT ( 'NONE', #7457 ) ;
#1340=CARTESIAN_POINT ( 'NONE',  ( 2.790000000000000924, 4.898587196589412829E-16, -4.000000000000000000 ) ) ;
#1341=EDGE_CURVE ( 'NONE', #9831, #1519, #12084, .T. ) ;
#1354=VERTEX_POINT ( 'NONE', #11782 ) ;
#1360=CIRCLE ( 'NONE', #3910, 2.524999999999995914 ) ;
#1361=ORIENTED_EDGE ( 'NONE', *, *, #4390, .T. ) ;
#1365=EDGE_LOOP ( 'NONE', ( #19565, #9472, #1138, #3199, #3300, #7236, #9317, #15325 ) ) ;
#1366=AXIS2_PLACEMENT_3D ( 'NONE', #9478, #15575, #1768 ) ;
#1368=ORIENTED_EDGE ( 'NONE', *, *, #5730, .T. ) ;
#1369=CARTESIAN_POINT ( 'NONE',  ( 0.000000000000000000, 24.34211360614310848, -7.909232158574561744 ) ) ;
#1376=ADVANCED_FACE ( 'NONE', ( #4178 ), #8880, .F. ) ;
#1377=DIRECTION ( 'NONE',  ( 0.000000000000000000, 0.000000000000000000, 1.000000000000000000 ) ) ;
#1379=DIRECTION ( 'NONE',  ( 0.000000000000000000, 0.000000000000000000, 1.000000000000000000 ) ) ;
#1382=DIRECTION ( 'NONE',  ( 0.000000000000000000, 0.000000000000000000, 1.000000000000000000 ) ) ;
#1385=CYLINDRICAL_SURFACE ( 'NONE', #1537, 2.524999999999995914 ) ;
#1412=CARTESIAN_POINT ( 'NONE',  ( 2.789679245949062913, -20.70663861606260525, -12.51925356660783528 ) ) ;
#1413=DIRECTION ( 'NONE',  ( 0.000000000000000000, 0.000000000000000000, 1.000000000000000000 ) ) ;
#1415=CARTESIAN_POINT ( 'NONE',  ( 0.000000000000000000, 0.000000000000000000, 0.000000000000000000 ) ) ;
#1416=DIRECTION ( 'NONE',  ( 1.000000000000000000, 0.000000000000000000, 0.000000000000000000 ) ) ;
#1428=DIRECTION ( 'NONE',  ( -1.000000000000000000, -0.000000000000000000, -0.000000000000000000 ) ) ;
#1431=CARTESIAN_POINT ( 'NONE',  ( 2.789999999999999147, 16.37294372382885044, -18.55949924794875017 ) ) ;
#1432=ORIENTED_EDGE ( 'NONE', *, *, #7613, .F. ) ;
#1437=CARTESIAN_POINT ( 'NONE',  ( 0.000000000000000000, 0.000000000000000000, 0.000000000000000000 ) ) ;
#1439=CARTESIAN_POINT ( 'NONE',  ( 2.765633920072241292, 18.55949924794916228, -16.37294372382838148 ) ) ;
#1447=CARTESIAN_POINT ( 'NONE',  ( 2.789999999999999147, 5.535312321042718864, 23.48180575137732262 ) ) ;
#1449=VECTOR ( 'NONE', #14188, 1000.000000000000000 ) ;
#1450=FACE_OUTER_BOUND ( 'NONE', #4388, .T. ) ;
#1452=FACE_OUTER_BOUND ( 'NONE', #1797, .T. ) ;
#1455=CARTESIAN_POINT ( 'NONE',  ( 2.765633920072238183, 2.336989772644269436, 24.63872515616083447 ) ) ;
#1456=B_SPLINE_CURVE_WITH_KNOTS ( 'NONE', 3,
 ( #9561, #11157, #4748, #250 ),
 .UNSPECIFIED., .F., .F.,
 ( 4, 4 ),
 ( 0.005258214619651972732, 0.005948481662034169060 ),
 .UNSPECIFIED. ) ;
#1461=ADVANCED_FACE ( 'NONE', ( #3163 ), #11637, .T. ) ;
#1463=CARTESIAN_POINT ( 'NONE',  ( 0.5321745227542320489, -18.57583492944406700, -19.66801664102725056 ) ) ;
#1471=VERTEX_POINT ( 'NONE', #14349 ) ;
#1472=CARTESIAN_POINT ( 'NONE',  ( 2.765633920072237295, 12.59161484032912171, 21.30679549418635688 ) ) ;
#1475=VECTOR ( 'NONE', #7713, 1000.000000000000000 ) ;
#1476=ORIENTED_EDGE ( 'NONE', *, *, #5448, .F. ) ;
#1477=CARTESIAN_POINT ( 'NONE',  ( 0.02436607992776151574, -16.37294372382871188, 18.55949924794887096 ) ) ;
#1483=DIRECTION ( 'NONE',  ( 0.000000000000000000, 0.000000000000000000, 1.000000000000000000 ) ) ;
#1492=AXIS2_PLACEMENT_3D ( 'NONE', #4280, #1279, #14789 ) ;
#1496=DIRECTION ( 'NONE',  ( 0.000000000000000000, 0.000000000000000000, 1.000000000000000000 ) ) ;
#1512=AXIS2_PLACEMENT_3D ( 'NONE', #10517, #15118, #1413 ) ;
#1519=VERTEX_POINT ( 'NONE', #3838 ) ;
#1520=EDGE_CURVE ( 'NONE', #8830, #16588, #11823, .T. ) ;
#1521=B_SPLINE_CURVE_WITH_KNOTS ( 'NONE', 3,
 ( #10115, #714, #14524, #14809, #17808, #4101 ),
 .UNSPECIFIED., .F., .F.,
 ( 4, 2, 4 ),
 ( 4.462636682232942879E-07, 0.001879885020955589887, 0.003759323778242956802 ),
 .UNSPECIFIED. ) ;
#1529=ORIENTED_EDGE ( 'NONE', *, *, #16686, .T. ) ;
#1535=DIRECTION ( 'NONE',  ( -1.000000000000000000, -0.000000000000000000, -0.000000000000000000 ) ) ;
#1537=AXIS2_PLACEMENT_3D ( 'NONE', #7162, #19482, #1284 ) ;
#1546=DIRECTION ( 'NONE',  ( 0.000000000000000000, 0.000000000000000000, 1.000000000000000000 ) ) ;
#1548=EDGE_LOOP ( 'NONE', ( #9036, #16446, #9572, #7477, #9877, #1944, #3479, #18925 ) ) ;
#1551=ORIENTED_EDGE ( 'NONE', *, *, #5162, .T. ) ;
#1559=FACE_OUTER_BOUND ( 'NONE', #1830, .T. ) ;
#1560=CARTESIAN_POINT ( 'NONE',  ( 2.262072661820536013, -3.461047254864073164, -26.82026385750182129 ) ) ;
#1562=CIRCLE ( 'NONE', #1886, 24.12539914357697768 ) ;
#1563=EDGE_CURVE ( 'NONE', #2313, #18773, #2744, .T. ) ;
#1565=FACE_OUTER_BOUND ( 'NONE', #16871, .T. ) ;
#1566=ORIENTED_EDGE ( 'NONE', *, *, #9806, .F. ) ;
#1570=CARTESIAN_POINT ( 'NONE',  ( 0.000000000000000000, 0.000000000000000000, 0.000000000000000000 ) ) ;
#1575=CARTESIAN_POINT ( 'NONE',  ( 0.000000000000000000, -15.04425356660774682, 20.70663861606266209 ) ) ;
#1578=DIRECTION ( 'NONE',  ( -1.000000000000000000, -0.000000000000000000, -0.000000000000000000 ) ) ;
#1584=VERTEX_POINT ( 'NONE', #4329 ) ;
#1586=CARTESIAN_POINT ( 'NONE',  ( -10.00000000000000000, 0.000000000000000000, 0.000000000000000000 ) ) ;
#1587=ORIENTED_EDGE ( 'NONE', *, *, #3578, .T. ) ;
#1590=CARTESIAN_POINT ( 'NONE',  ( 1.039999999999996705, -20.02152543075359503, 19.67366047555523423 ) ) ;
#1591=AXIS2_PLACEMENT_3D ( 'NONE', #12213, #17921, #2798 ) ;
#1592=CARTESIAN_POINT ( 'NONE',  ( 0.7589665283900990378, 3.797536611356696845, -27.31260702007171304 ) ) ;
#1597=( LENGTH_UNIT ( ) NAMED_UNIT ( * ) SI_UNIT ( .MILLI., .METRE. ) );
#1599=CARTESIAN_POINT ( 'NONE',  ( -10.00000000000000000, 0.000000000000000000, 0.000000000000000000 ) ) ;
#1601=CARTESIAN_POINT ( 'NONE',  ( 2.765633920072235963, -24.63872515616080960, -2.336989772644527008 ) ) ;
#1605=ORIENTED_EDGE ( 'NONE', *, *, #17370, .F. ) ;
#1606=DIRECTION ( 'NONE',  ( -1.000000000000000000, 0.000000000000000000, -0.000000000000000000 ) ) ;
#1608=CARTESIAN_POINT ( 'NONE',  ( 2.789999999999999147, 5.456805104201435164, -23.69843731927162978 ) ) ;
#1612=DIRECTION ( 'NONE',  ( -1.000000000000000000, -0.000000000000000000, -0.000000000000000000 ) ) ;
#1616=CARTESIAN_POINT ( 'NONE',  ( 1.749999999999998002, -4.147968289691086774, -27.76164181293056288 ) ) ;
#1618=CIRCLE ( 'NONE', #5123, 28.06981291497571007 ) ;
#1619=CARTESIAN_POINT ( 'NONE',  ( 2.789999999999999147, -20.70663861606282197, 15.04425356660753188 ) ) ;
#1625=ADVANCED_FACE ( 'NONE', ( #19631 ), #6208, .T. ) ;
#1626=CARTESIAN_POINT ( 'NONE',  ( 0.000000000000000000, 24.04302995059966364, -1.991882183130399664 ) ) ;
#1627=EDGE_LOOP ( 'NONE', ( #9838, #19624, #19392, #9842, #6600, #1252 ) ) ;
#1628=DIRECTION ( 'NONE',  ( 0.000000000000000000, 0.000000000000000000, 1.000000000000000000 ) ) ;
#1635=AXIS2_PLACEMENT_3D ( 'NONE', #789, #10263, #5642 ) ;
#1637=ADVANCED_FACE ( 'NONE', ( #16633 ), #13567, .T. ) ;
#1639=ORIENTED_EDGE ( 'NONE', *, *, #6877, .T. ) ;
#1646=LINE ( 'NONE', #14324, #4574 ) ;
#1661=CARTESIAN_POINT ( 'NONE',  ( 2.789999999999999147, 19.64056340710875048, 14.55412442567624609 ) ) ;
#1663=VECTOR ( 'NONE', #13188, 1000.000000000000000 ) ;
#1667=COLOUR_RGB ( '', 0.66274510, 0.83137255, 0.94901961) ;
#1671=CARTESIAN_POINT ( 'NONE',  ( -7.922038997698610785E-14, 18.34439787333529992, -15.96555658743743145 ) ) ;
#1672=ORIENTED_EDGE ( 'NONE', *, *, #1563, .T. ) ;
#1674=EDGE_CURVE ( 'NONE', #11007, #11676, #8466, .T. ) ;
#1677=ORIENTED_EDGE ( 'NONE', *, *, #5606, .T. ) ;
#1680=AXIS2_PLACEMENT_3D ( 'NONE', #11781, #7250, #1377 ) ;
#1682=CIRCLE ( 'NONE', #12866, 28.06981291497571007 ) ;
#1687=ORIENTED_EDGE ( 'NONE', *, *, #14904, .F. ) ;
#1688=CARTESIAN_POINT ( 'NONE',  ( 2.765633920072239516, -24.15498966839958683, -5.391175441198872598 ) ) ;
#1698=ORIENTED_EDGE ( 'NONE', *, *, #8157, .F. ) ;
#1699=B_SPLINE_CURVE_WITH_KNOTS ( 'NONE', 3,
 ( #4812, #17021, #3311, #14707 ),
 .UNSPECIFIED., .F., .F.,
 ( 4, 4 ),
 ( 2.135345996334758909E-07, 0.0006888010880211141137 ),
 .UNSPECIFIED. ) ;
#1702=CARTESIAN_POINT ( 'NONE',  ( 1.749999999999998002, 27.76164181293051669, 4.147968289691386090 ) ) ;
#1705=VERTEX_POINT ( 'NONE', #6698 ) ;
#1706=DIRECTION ( 'NONE',  ( 0.000000000000000000, 0.000000000000000000, 1.000000000000000000 ) ) ;
#1707=DIRECTION ( 'NONE',  ( 0.000000000000000000, 0.000000000000000000, 1.000000000000000000 ) ) ;
#1709=DIRECTION ( 'NONE',  ( -1.000000000000000000, -0.000000000000000000, -0.000000000000000000 ) ) ;
#1711=ORIENTED_EDGE ( 'NONE', *, *, #1341, .T. ) ;
#1712=CARTESIAN_POINT ( 'NONE',  ( 0.7589665089996505687, 12.05173163741758380, -24.80232951178364686 ) ) ;
#1717=CARTESIAN_POINT ( 'NONE',  ( 2.789999999999999147, 2.680914349914567470E-13, -25.59481291497571220 ) ) ;
#1726=VERTEX_POINT ( 'NONE', #1818 ) ;
#1729=DIRECTION ( 'NONE',  ( 0.000000000000000000, 1.374038396813314756E-15, -1.000000000000000000 ) ) ;
#1734=CARTESIAN_POINT ( 'NONE',  ( -5.209999999999999964, 0.000000000000000000, 0.000000000000000000 ) ) ;
#1738=FACE_OUTER_BOUND ( 'NONE', #12469, .T. ) ;
#1739=ADVANCED_FACE ( 'NONE', ( #12823 ), #317, .T. ) ;
#1740=EDGE_CURVE ( 'NONE', #17455, #569, #11970, .T. ) ;
#1741=VERTEX_POINT ( 'NONE', #12628 ) ;
#1742=AXIS2_PLACEMENT_3D ( 'NONE', #4699, #16913, #13607 ) ;
#1746=DIRECTION ( 'NONE',  ( 0.000000000000000000, 0.000000000000000000, 1.000000000000000000 ) ) ;
#1748=EDGE_LOOP ( 'NONE', ( #16255, #14164, #9476, #19113 ) ) ;
#1756=VERTEX_POINT ( 'NONE', #18718 ) ;
#1758=CARTESIAN_POINT ( 'NONE',  ( -5.209999999999999964, 0.000000000000000000, 0.000000000000000000 ) ) ;
#1768=DIRECTION ( 'NONE',  ( 0.000000000000000000, -1.374038396813314756E-15, -1.000000000000000000 ) ) ;
#1771=CARTESIAN_POINT ( 'NONE',  ( 2.789999999999999147, 23.48180575137737947, -5.535312321042476391 ) ) ;
#1773=VERTEX_POINT ( 'NONE', #13219 ) ;
#1775=AXIS2_PLACEMENT_3D ( 'NONE', #15348, #13939, #432 ) ;
#1792=ORIENTED_EDGE ( 'NONE', *, *, #3339, .F. ) ;
#1793=DIRECTION ( 'NONE',  ( -1.000000000000000000, -0.000000000000000000, -0.000000000000000000 ) ) ;
#1797=EDGE_LOOP ( 'NONE', ( #9983, #2137, #1209, #7611, #6830, #5049, #16780 ) ) ;
#1801=ADVANCED_FACE ( 'NONE', ( #5502 ), #2308, .T. ) ;
#1802=CARTESIAN_POINT ( 'NONE',  ( 0.000000000000000000, 20.62201879784932856, -12.52067188844328705 ) ) ;
#1807=AXIS2_PLACEMENT_3D ( 'NONE', #8972, #16484, #19568 ) ;
#1811=ORIENTED_EDGE ( 'NONE', *, *, #15845, .F. ) ;
#1817=CARTESIAN_POINT ( 'NONE',  ( 2.789999999999999147, 15.74360496233408213, -18.28042085475260592 ) ) ;
#1818=CARTESIAN_POINT ( 'NONE',  ( 1.749999999999998002, -12.96210679857767367, -24.89775460606847091 ) ) ;
#1822=DIRECTION ( 'NONE',  ( -1.000000000000000000, 0.000000000000000000, 0.000000000000000000 ) ) ;
#1826=DIRECTION ( 'NONE',  ( 0.000000000000000000, 0.000000000000000000, 1.000000000000000000 ) ) ;
#1828=DIRECTION ( 'NONE',  ( 1.000000000000000000, -0.000000000000000000, -0.000000000000000000 ) ) ;
#1829=CYLINDRICAL_SURFACE ( 'NONE', #3376, 2.524999999999995914 ) ;
#1830=EDGE_LOOP ( 'NONE', ( #6602, #3647, #13917, #10088, #9890, #14417 ) ) ;
#1834=CIRCLE ( 'NONE', #5665, 2.524999999999997691 ) ;
#1835=B_SPLINE_CURVE_WITH_KNOTS ( 'NONE', 3,
 ( #890, #11589, #7060, #8585 ),
 .UNSPECIFIED., .F., .F.,
 ( 4, 4 ),
 ( 2.034713381942717623E-07, 0.0006887909409525284563 ),
 .UNSPECIFIED. ) ;
#1841=ORIENTED_EDGE ( 'NONE', *, *, #11626, .F. ) ;
#1842=CARTESIAN_POINT ( 'NONE',  ( 2.765633920072235519, 24.15498966839970052, -5.391175441198366336 ) ) ;
#1846=EDGE_CURVE ( 'NONE', #2546, #9696, #3288, .T. ) ;
#1850=CARTESIAN_POINT ( 'NONE',  ( 2.765633920072238627, 12.59161484032942901, -21.30679549418617924 ) ) ;
#1854=ORIENTED_EDGE ( 'NONE', *, *, #14270, .T. ) ;
#1859=EDGE_CURVE ( 'NONE', #12256, #8014, #3341, .T. ) ;
#1863=EDGE_CURVE ( 'NONE', #18773, #8014, #7084, .T. ) ;
#1872=CARTESIAN_POINT ( 'NONE',  ( 0.006931038682727013421, -21.08061549536624568, 12.53626894672821201 ) ) ;
#1875=CARTESIAN_POINT ( 'NONE',  ( 0.000000000000000000, 0.000000000000000000, 4.000000000000000000 ) ) ;
#1879=EDGE_CURVE ( 'NONE', #11367, #12759, #13883, .T. ) ;
#1880=CARTESIAN_POINT ( 'NONE',  ( 2.718131847775120402, -24.78765742476134548, -5.344160105508965586 ) ) ;
#1881=CARTESIAN_POINT ( 'NONE',  ( 1.039999999999997593, 0.000000000000000000, 0.000000000000000000 ) ) ;
#1886=AXIS2_PLACEMENT_3D ( 'NONE', #3455, #12761, #1946 ) ;
#1893=ORIENTED_EDGE ( 'NONE', *, *, #2125, .T. ) ;
#1901=DIRECTION ( 'NONE',  ( 0.000000000000000000, 0.000000000000000000, 1.000000000000000000 ) ) ;
#1912=CARTESIAN_POINT ( 'NONE',  ( 0.02436607992776238310, -2.336989772644097574, -24.63872515616085224 ) ) ;
#1916=ORIENTED_EDGE ( 'NONE', *, *, #12572, .T. ) ;
#1923=CARTESIAN_POINT ( 'NONE',  ( 1.749999999999998002, 0.000000000000000000, 0.000000000000000000 ) ) ;
#1926=ORIENTED_EDGE ( 'NONE', *, *, #3409, .T. ) ;
#1927=CYLINDRICAL_SURFACE ( 'NONE', #15105, 13.20000000000000284 ) ;
#1940=VERTEX_POINT ( 'NONE', #4494 ) ;
#1944=ORIENTED_EDGE ( 'NONE', *, *, #15674, .T. ) ;
#1946=DIRECTION ( 'NONE',  ( 0.000000000000000000, 0.000000000000000000, 1.000000000000000000 ) ) ;
#1951=EDGE_CURVE ( 'NONE', #12561, #2276, #10709, .T. ) ;
#1957=VECTOR ( 'NONE', #15647, 1000.000000000000000 ) ;
#1960=AXIS2_PLACEMENT_3D ( 'NONE', #13369, #5755, #14978 ) ;
#1964=CARTESIAN_POINT ( 'NONE',  ( 0.000000000000000000, -24.04302995059965653, -1.991882183130557094 ) ) ;
#1965=DIRECTION ( 'NONE',  ( 0.000000000000000000, 0.000000000000000000, 1.000000000000000000 ) ) ;
#1972=AXIS2_PLACEMENT_3D ( 'NONE', #4783, #10596, #15496 ) ;
#1975=CIRCLE ( 'NONE', #12857, 28.06981291497571007 ) ;
#1981=EDGE_CURVE ( 'NONE', #8201, #5965, #13802, .T. ) ;
#1984=CARTESIAN_POINT ( 'NONE',  ( 1.749999999999998002, 12.52377138324224148, 25.12109765559658570 ) ) ;
#1986=ORIENTED_EDGE ( 'NONE', *, *, #16386, .T. ) ;
#1992=ORIENTED_EDGE ( 'NONE', *, *, #8446, .T. ) ;
#1993=ADVANCED_FACE ( 'NONE', ( #18405 ), #10378, .T. ) ;
#1994=CARTESIAN_POINT ( 'NONE',  ( 2.790000000000077751, -24.22524813288760370, -2.133839912091053836 ) ) ;
#2003=DIRECTION ( 'NONE',  ( 0.000000000000000000, 0.9510565162951567508, -0.3090169943749379589 ) ) ;
#2011=CARTESIAN_POINT ( 'NONE',  ( 2.765633920072242180, 22.71065055754465689, -9.836394144775473691 ) ) ;
#2014=CARTESIAN_POINT ( 'NONE',  ( 2.765633920072239516, -24.15498966839958683, -5.391175441198872598 ) ) ;
#2018=ORIENTED_EDGE ( 'NONE', *, *, #6435, .F. ) ;
#2019=CARTESIAN_POINT ( 'NONE',  ( 0.000000000000000000, -24.34211360614294506, -7.909232158575071558 ) ) ;
#2026=CARTESIAN_POINT ( 'NONE',  ( 2.789999999999999147, 0.000000000000000000, 0.000000000000000000 ) ) ;
#2029=AXIS2_PLACEMENT_3D ( 'NONE', #10316, #18109, #19603 ) ;
#2030=CARTESIAN_POINT ( 'NONE',  ( 2.789999999999999147, -7.772527002114597572, 23.17675759782038369 ) ) ;
#2032=ORIENTED_EDGE ( 'NONE', *, *, #11621, .F. ) ;
#2035=DIRECTION ( 'NONE',  ( -1.000000000000000000, -0.000000000000000000, -0.000000000000000000 ) ) ;
#2042=CYLINDRICAL_SURFACE ( 'NONE', #786, 2.524999999999995914 ) ;
#2043=ORIENTED_EDGE ( 'NONE', *, *, #11534, .F. ) ;
#2049=CARTESIAN_POINT ( 'NONE',  ( 0.4386599019957485579, -23.41653927703718097, 12.93238701107298283 ) ) ;
#2050=LINE ( 'NONE', #12570, #8235 ) ;
#2052=VERTEX_POINT ( 'NONE', #9007 ) ;
#2055=ORIENTED_EDGE ( 'NONE', *, *, #1674, .T. ) ;
#2058=CARTESIAN_POINT ( 'NONE',  ( 0.02436607992776455150, -22.71065055754459650, 9.836394144775621129 ) ) ;
#2062=CARTESIAN_POINT ( 'NONE',  ( 1.039999999999995373, 12.96210679857822434, -24.89775460606817958 ) ) ;
#2063=DIRECTION ( 'NONE',  ( 0.000000000000000000, 0.000000000000000000, 1.000000000000000000 ) ) ;
#2067=CARTESIAN_POINT ( 'NONE',  ( 2.765633920072241736, -9.836394144775550075, -22.71065055754462492 ) ) ;
#2068=ADVANCED_BREP_SHAPE_REPRESENTATION ( '', ( #2500, #16724 ), #120 ) ;
#2069=ADVANCED_FACE ( 'NONE', ( #15799 ), #7987, .T. ) ;
#2070=CARTESIAN_POINT ( 'NONE',  ( 2.789999999999999147, -15.74360496233368245, -18.28042085475295409 ) ) ;
#2078=DIRECTION ( 'NONE',  ( -1.000000000000000000, -0.000000000000000000, 0.000000000000000000 ) ) ;
#2080=CARTESIAN_POINT ( 'NONE',  ( 2.765633920072235075, -12.59161484032896361, -21.30679549418645280 ) ) ;
#2081=DIRECTION ( 'NONE',  ( -1.000000000000000000, -0.000000000000000000, -0.000000000000000000 ) ) ;
#2090=CYLINDRICAL_SURFACE ( 'NONE', #6315, 13.20000000000000107 ) ;
#2099=CARTESIAN_POINT ( 'NONE',  ( 0.000000000000000000, 0.000000000000000000, 0.000000000000000000 ) ) ;
#2105=CARTESIAN_POINT ( 'NONE',  ( 0.000000000000000000, -15.74360496233395956, 18.28042085475273026 ) ) ;
#2108=CARTESIAN_POINT ( 'NONE',  ( 0.000000000000000000, -15.74360496233370021, -18.28042085475294698 ) ) ;
#2121=CARTESIAN_POINT ( 'NONE',  ( 0.02436607992776238310, -2.336989772644097574, -24.63872515616085224 ) ) ;
#2124=CARTESIAN_POINT ( 'NONE',  ( 2.789999999999999147, 14.18181402625769749, -19.91106274590499225 ) ) ;
#2125=EDGE_CURVE ( 'NONE', #2052, #15555, #19510, .T. ) ;
#2126=EDGE_LOOP ( 'NONE', ( #12924, #8084, #4483, #12872, #14040, #9043, #13960, #2828 ) ) ;
#2128=DIRECTION ( 'NONE',  ( -1.000000000000000000, -0.000000000000000000, -0.000000000000000000 ) ) ;
#2134=CARTESIAN_POINT ( 'NONE',  ( 2.718184749312773540, 2.576941577947758688, -25.22524549359947343 ) ) ;
#2137=ORIENTED_EDGE ( 'NONE', *, *, #1228, .F. ) ;
#2141=ORIENTED_EDGE ( 'NONE', *, *, #4784, .T. ) ;
#2146=ORIENTED_EDGE ( 'NONE', *, *, #5730, .F. ) ;
#2147=B_SPLINE_CURVE_WITH_KNOTS ( 'NONE', 3,
 ( #17756, #5835, #16457, #11948, #2352, #4054 ),
 .UNSPECIFIED., .F., .F.,
 ( 4, 2, 4 ),
 ( 4.462636732217463004E-07, 0.001879885066975006029, 0.003759323870276790047 ),
 .UNSPECIFIED. ) ;
#2150=AXIS2_PLACEMENT_3D ( 'NONE', #4869, #3070, #18381 ) ;
#2161=CARTESIAN_POINT ( 'NONE',  ( 0.5321745407694753460, 26.58873630738052185, 4.993157874727903511 ) ) ;
#2162=VERTEX_POINT ( 'NONE', #1702 ) ;
#2168=EDGE_CURVE ( 'NONE', #2600, #18594, #2699, .T. ) ;
#2172=AXIS2_PLACEMENT_3D ( 'NONE', #17140, #18931, #14133 ) ;
#2186=CARTESIAN_POINT ( 'NONE',  ( 2.789999999999999147, 7.909232158575156824, -21.81711360614291806 ) ) ;
#2191=EDGE_LOOP ( 'NONE', ( #10278, #7435, #9899, #9170, #318, #13941 ) ) ;
#2204=DIRECTION ( 'NONE',  ( 1.000000000000000000, 0.000000000000000000, 0.000000000000000000 ) ) ;
#2205=CARTESIAN_POINT ( 'NONE',  ( 2.790000000000079527, -15.96555658743774941, 18.34439787333500860 ) ) ;
#2214=CARTESIAN_POINT ( 'NONE',  ( 2.789999999999999147, -1.991882183130126549, -24.04302995059967429 ) ) ;
#2217=DIRECTION ( 'NONE',  ( -1.000000000000000000, -0.000000000000000000, -0.000000000000000000 ) ) ;
#2220=B_SPLINE_CURVE_WITH_KNOTS ( 'NONE', 3,
 ( #19778, #9190, #6071, #12186, #18292, #15295 ),
 .UNSPECIFIED., .F., .F.,
 ( 4, 2, 4 ),
 ( 4.462636732861906317E-07, 0.001879885066975067612, 0.003759323870276849028 ),
 .UNSPECIFIED. ) ;
#2225=CARTESIAN_POINT ( 'NONE',  ( 0.000000000000000000, -20.62201879784923264, 12.52067188844344336 ) ) ;
#2228=EDGE_CURVE ( 'NONE', #7268, #758, #2782, .T. ) ;
#2229=CARTESIAN_POINT ( 'NONE',  ( 1.749999999999998002, 0.000000000000000000, 0.000000000000000000 ) ) ;
#2230=CARTESIAN_POINT ( 'NONE',  ( 2.789999999999999147, 0.000000000000000000, 0.000000000000000000 ) ) ;
#2236=CIRCLE ( 'NONE', #5113, 2.524999999999995914 ) ;
#2238=B_SPLINE_CURVE_WITH_KNOTS ( 'NONE', 3,
 ( #2214, #2408, #13119, #728 ),
 .UNSPECIFIED., .F., .F.,
 ( 4, 4 ),
 ( 0.005258120783916825358, 0.005948386350302978416 ),
 .UNSPECIFIED. ) ;
#2240=CARTESIAN_POINT ( 'NONE',  ( -2.179313406705571952E-17, -18.34424029220099683, -15.96500990068145853 ) ) ;
#2245=EDGE_CURVE ( 'NONE', #8648, #7952, #10616, .T. ) ;
#2249=CYLINDRICAL_SURFACE ( 'NONE', #12119, 28.06981291497571362 ) ;
#2251=DIRECTION ( 'NONE',  ( 0.000000000000000000, 0.000000000000000000, 1.000000000000000000 ) ) ;
#2253=VECTOR ( 'NONE', #9311, 1000.000000000000000 ) ;
#2254=EDGE_CURVE ( 'NONE', #18935, #12759, #1835, .T. ) ;
#2256=CARTESIAN_POINT ( 'NONE',  ( 2.601776144743011443, 23.64332819722380918, 10.68696068830415946 ) ) ;
#2258=CARTESIAN_POINT ( 'NONE',  ( 2.257825467309738432, 26.83036154824994313, 3.467596033028380376 ) ) ;
#2268=VERTEX_POINT ( 'NONE', #2186 ) ;
#2276=VERTEX_POINT ( 'NONE', #4087 ) ;
#2277=DIRECTION ( 'NONE',  ( -1.000000000000000000, -0.000000000000000000, -0.000000000000000000 ) ) ;
#2281=CARTESIAN_POINT ( 'NONE',  ( 2.765633920072234631, 5.391175441198615914, 24.15498966839965078 ) ) ;
#2285=DIRECTION ( 'NONE',  ( 1.000000000000000000, 0.000000000000000000, 0.000000000000000000 ) ) ;
#2294=CARTESIAN_POINT ( 'NONE',  ( 2.789999999999999147, -0.2301004812059262439, 24.44424927289185590 ) ) ;
#2298=CARTESIAN_POINT ( 'NONE',  ( 2.783025336474041822, 12.53640742967753141, 21.08118142846907972 ) ) ;
#2299=ORIENTED_EDGE ( 'NONE', *, *, #7127, .F. ) ;
#2308=CYLINDRICAL_SURFACE ( 'NONE', #791, 13.19999999999999929 ) ;
#2310=ORIENTED_EDGE ( 'NONE', *, *, #977, .T. ) ;
#2311=EDGE_CURVE ( 'NONE', #241, #2766, #17890, .T. ) ;
#2312=DIRECTION ( 'NONE',  ( 0.000000000000000000, 0.000000000000000000, -1.000000000000000000 ) ) ;
#2313=VERTEX_POINT ( 'NONE', #8682 ) ;
#2316=CARTESIAN_POINT ( 'NONE',  ( 0.006974663525957706944, 21.08118142846903353, 12.53640742967760602 ) ) ;
#2323=EDGE_LOOP ( 'NONE', ( #8523, #233, #1361, #4923 ) ) ;
#2324=CARTESIAN_POINT ( 'NONE',  ( 2.765633920072235519, 9.836394144776026138, -22.71065055754441531 ) ) ;
#2328=AXIS2_PLACEMENT_3D ( 'NONE', #14174, #11177, #4970 ) ;
#2336=EDGE_LOOP ( 'NONE', ( #18850, #5277, #7151, #9720, #1068, #13183, #13467, #16106 ) ) ;
#2341=CIRCLE ( 'NONE', #14165, 2.524999999999996803 ) ;
#2344=VECTOR ( 'NONE', #10398, 1000.000000000000000 ) ;
#2346=ORIENTED_EDGE ( 'NONE', *, *, #14684, .T. ) ;
#2351=ADVANCED_FACE ( 'NONE', ( #5382 ), #11684, .T. ) ;
#2352=CARTESIAN_POINT ( 'NONE',  ( 2.718184749312773540, -2.576941577947583273, 25.22524549359949120 ) ) ;
#2355=EDGE_CURVE ( 'NONE', #298, #881, #8539, .T. ) ;
#2358=VERTEX_POINT ( 'NONE', #16200 ) ;
#2368=CARTESIAN_POINT ( 'NONE',  ( 2.765633920072239071, -16.37294372382844543, -18.55949924794910544 ) ) ;
#2381=CARTESIAN_POINT ( 'NONE',  ( 0.006974674093432167536, 2.249040938978497994, 24.42374957165206695 ) ) ;
#2390=CARTESIAN_POINT ( 'NONE',  ( 0.1882239080259289210, -5.251266773802552024, 25.40949241676352344 ) ) ;
#2401=CARTESIAN_POINT ( 'NONE',  ( 2.765633920072235963, -16.37294372382871188, 18.55949924794887096 ) ) ;
#2402=ORIENTED_EDGE ( 'NONE', *, *, #10017, .F. ) ;
#2403=DIRECTION ( 'NONE',  ( -1.000000000000000000, 0.000000000000000000, 0.000000000000000000 ) ) ;
#2405=EDGE_CURVE ( 'NONE', #13251, #9816, #3032, .T. ) ;
#2408=CARTESIAN_POINT ( 'NONE',  ( 2.789999999999999147, -2.133490293296841589, -24.22479935914661198 ) ) ;
#2416=ORIENTED_EDGE ( 'NONE', *, *, #7238, .F. ) ;
#2418=LINE ( 'NONE', #1015, #10750 ) ;
#2423=CARTESIAN_POINT ( 'NONE',  ( 0.02436607992775674525, 9.836394144776026138, -22.71065055754441531 ) ) ;
#2426=EDGE_CURVE ( 'NONE', #1337, #4347, #6604, .T. ) ;
#2428=ORIENTED_EDGE ( 'NONE', *, *, #11867, .T. ) ;
#2429=CARTESIAN_POINT ( 'NONE',  ( 2.783025342027734883, 23.92335783895644852, -5.408388659523843067 ) ) ;
#2430=ORIENTED_EDGE ( 'NONE', *, *, #18387, .F. ) ;
#2432=CARTESIAN_POINT ( 'NONE',  ( 2.030753616560876829, -24.80264696524875490, -12.05220173035465336 ) ) ;
#2433=DIRECTION ( 'NONE',  ( -1.000000000000000000, 0.000000000000000000, 0.000000000000000000 ) ) ;
#2436=CARTESIAN_POINT ( 'NONE',  ( 2.789999999999999147, 19.91106274590514147, 14.18181402625749676 ) ) ;
#2443=ADVANCED_FACE ( 'NONE', ( #9185 ), #10293, .T. ) ;
#2444=CARTESIAN_POINT ( 'NONE',  ( 1.749999999999998002, 27.76164181293051669, 4.147968289691386090 ) ) ;
#2446=VERTEX_POINT ( 'NONE', #10685 ) ;
#2452=VECTOR ( 'NONE', #4478, 1000.000000000000000 ) ;
#2462=CIRCLE ( 'NONE', #13658, 2.524999999999996358 ) ;
#2465=EDGE_CURVE ( 'NONE', #16863, #2982, #1360, .T. ) ;
#2470=CYLINDRICAL_SURFACE ( 'NONE', #16114, 13.19999999999999929 ) ;
#2472=LINE ( 'NONE', #11984, #18118 ) ;
#2474=ORIENTED_EDGE ( 'NONE', *, *, #10806, .T. ) ;
#2481=DIRECTION ( 'NONE',  ( 0.000000000000000000, 0.000000000000000000, 1.000000000000000000 ) ) ;
#2483=ORIENTED_EDGE ( 'NONE', *, *, #10663, .T. ) ;
#2484=CARTESIAN_POINT ( 'NONE',  ( 2.789999999999999147, -12.52067188844365830, 20.62201879784908698 ) ) ;
#2486=EDGE_CURVE ( 'NONE', #17826, #18420, #5275, .T. ) ;
#2492=FACE_OUTER_BOUND ( 'NONE', #17685, .T. ) ;
#2493=CARTESIAN_POINT ( 'NONE',  ( 2.783025228907522575, 22.53337530003403799, 9.686319561461028016 ) ) ;
#2495=B_SPLINE_CURVE_WITH_KNOTS ( 'NONE', 3,
 ( #1007, #17722, #6808, #12829, #6902, #2121 ),
 .UNSPECIFIED., .F., .F.,
 ( 4, 2, 4 ),
 ( 4.462636732861906317E-07, 0.001879885066975067178, 0.003759323870276848160 ),
 .UNSPECIFIED. ) ;
#2500=MANIFOLD_SOLID_BREP ( 'Bore', #8722 ) ;
#2503=CARTESIAN_POINT ( 'NONE',  ( 0.07186808533286645484, -10.24630254990532663, 23.19485392143210944 ) ) ;
#2504=CARTESIAN_POINT ( 'NONE',  ( 2.718131914667133220, 23.19485392143227642, -10.24630254990492340 ) ) ;
#2513=ADVANCED_FACE ( 'NONE', ( #15678 ), #18477, .T. ) ;
#2514=ORIENTED_EDGE ( 'NONE', *, *, #19377, .T. ) ;
#2520=DIRECTION ( 'NONE',  ( 0.000000000000000000, -0.8090169943749444537, -0.5877852522924771339 ) ) ;
#2521=EDGE_CURVE ( 'NONE', #5672, #9010, #16367, .T. ) ;
#2528=CARTESIAN_POINT ( 'NONE',  ( 0.000000000000000000, -24.34211360614305875, 7.909232158574721616 ) ) ;
#2545=ADVANCED_FACE ( 'NONE', ( #7863 ), #577, .T. ) ;
#2546=VERTEX_POINT ( 'NONE', #9384 ) ;
#2549=DIRECTION ( 'NONE',  ( 0.000000000000000000, 0.000000000000000000, 1.000000000000000000 ) ) ;
#2551=DIRECTION ( 'NONE',  ( 0.000000000000000000, 0.5877852522924805756, -0.8090169943749421222 ) ) ;
#2553=ORIENTED_EDGE ( 'NONE', *, *, #15596, .T. ) ;
#2556=ADVANCED_FACE ( 'NONE', ( #14072 ), #15112, .T. ) ;
#2560=ORIENTED_EDGE ( 'NONE', *, *, #11689, .F. ) ;
#2561=CARTESIAN_POINT ( 'NONE',  ( 2.790000000000000036, 23.69843731927168662, 5.456805104201184697 ) ) ;
#2566=FACE_OUTER_BOUND ( 'NONE', #18468, .T. ) ;
#2567=CARTESIAN_POINT ( 'NONE',  ( 2.789999999999999147, 20.62201879784931435, -12.52067188844328882 ) ) ;
#2579=EDGE_CURVE ( 'NONE', #9276, #2546, #4554, .T. ) ;
#2580=CYLINDRICAL_SURFACE ( 'NONE', #14443, 13.19999999999999929 ) ;
#2581=EDGE_CURVE ( 'NONE', #18102, #10126, #4676, .T. ) ;
#2583=ORIENTED_EDGE ( 'NONE', *, *, #11378, .T. ) ;
#2585=CARTESIAN_POINT ( 'NONE',  ( 0.7592463977762118343, 4.828194074574732930, -27.14986936243569460 ) ) ;
#2586=CARTESIAN_POINT ( 'NONE',  ( 2.765633920072238183, -18.55949924794904504, 16.37294372382852004 ) ) ;
#2590=ORIENTED_EDGE ( 'NONE', *, *, #16110, .T. ) ;
#2596=CARTESIAN_POINT ( 'NONE',  ( 0.000000000000000000, -18.28042085475288303, 15.74360496233377305 ) ) ;
#2598=EDGE_CURVE ( 'NONE', #19366, #19037, #7085, .T. ) ;
#2599=CARTESIAN_POINT ( 'NONE',  ( 0.1855657168891856057, 12.84444904262024956, 22.53097606932990260 ) ) ;
#2600=VERTEX_POINT ( 'NONE', #6947 ) ;
#2601=ADVANCED_FACE ( 'NONE', ( #8659 ), #19260, .T. ) ;
#2604=CARTESIAN_POINT ( 'NONE',  ( 2.765633920072236851, 24.15498966839963302, 5.391175441198700291 ) ) ;
#2606=ORIENTED_EDGE ( 'NONE', *, *, #12764, .T. ) ;
#2608=CARTESIAN_POINT ( 'NONE',  ( 1.749999999999998002, 0.000000000000000000, 0.000000000000000000 ) ) ;
#2611=VECTOR ( 'NONE', #17682, 1000.000000000000000 ) ;
#2614=CARTESIAN_POINT ( 'NONE',  ( 2.789999999999999147, 0.000000000000000000, 0.000000000000000000 ) ) ;
#2615=ORIENTED_EDGE ( 'NONE', *, *, #18615, .T. ) ;
#2618=CARTESIAN_POINT ( 'NONE',  ( 0.0003207540509381473352, -20.70663861606275447, -12.51925356660783528 ) ) ;
#2620=DIRECTION ( 'NONE',  ( 0.000000000000000000, 0.000000000000000000, 1.000000000000000000 ) ) ;
#2623=CIRCLE ( 'NONE', #8377, 2.524999999999995914 ) ;
#2639=B_SPLINE_CURVE_WITH_KNOTS ( 'NONE', 3,
 ( #18612, #18707, #10917, #18810, #5199, #11317 ),
 .UNSPECIFIED., .F., .F.,
 ( 4, 2, 4 ),
 ( 4.462636882206429356E-07, 0.001879885203074806513, 0.003759324142461392161 ),
 .UNSPECIFIED. ) ;
#2640=CARTESIAN_POINT ( 'NONE',  ( 2.789999999999999147, 0.000000000000000000, 0.000000000000000000 ) ) ;
#2641=VECTOR ( 'NONE', #12255, 1000.000000000000000 ) ;
#2644=LINE ( 'NONE', #18357, #18320 ) ;
#2647=LINE ( 'NONE', #12066, #11270 ) ;
#2648=EDGE_CURVE ( 'NONE', #6118, #12561, #17683, .T. ) ;
#2654=ORIENTED_EDGE ( 'NONE', *, *, #1104, .F. ) ;
#2659=CARTESIAN_POINT ( 'NONE',  ( 0.006930995026450116094, -5.408431875071277872, -23.92277630352801054 ) ) ;
#2673=DIRECTION ( 'NONE',  ( -1.000000000000000000, -0.000000000000000000, -0.000000000000000000 ) ) ;
#2675=CARTESIAN_POINT ( 'NONE',  ( 2.789999999999999147, 20.70663861606293210, -15.04425356660737556 ) ) ;
#2687=FACE_OUTER_BOUND ( 'NONE', #2789, .T. ) ;
#2691=CARTESIAN_POINT ( 'NONE',  ( 0.000000000000000000, -9.324097380959594616, 22.25075486061734509 ) ) ;
#2694=ORIENTED_EDGE ( 'NONE', *, *, #12053, .T. ) ;
#2696=CARTESIAN_POINT ( 'NONE',  ( 0.5279273620711159021, 12.96450951081217084, 23.73240184472501113 ) ) ;
#2697=ORIENTED_EDGE ( 'NONE', *, *, #7222, .F. ) ;
#2699=CIRCLE ( 'NONE', #16683, 28.06981291497571007 ) ;
#2704=CARTESIAN_POINT ( 'NONE',  ( 1.749999999999998002, 19.67366047555530528, 20.02152543075352753 ) ) ;
#2710=EDGE_CURVE ( 'NONE', #1471, #10072, #2647, .T. ) ;
#2724=CARTESIAN_POINT ( 'NONE',  ( 0.7592463834391182109, 24.80264696524898937, -12.05220173035413112 ) ) ;
#2734=EDGE_CURVE ( 'NONE', #18318, #12686, #18638, .T. ) ;
#2736=VERTEX_POINT ( 'NONE', #10664 ) ;
#2742=ORIENTED_EDGE ( 'NONE', *, *, #14377, .F. ) ;
#2744=B_SPLINE_CURVE_WITH_KNOTS ( 'NONE', 3,
 ( #13830, #9029, #6305, #3119, #2816, #4516 ),
 .UNSPECIFIED., .F., .F.,
 ( 4, 2, 4 ),
 ( 2.586195665686417350E-07, 0.001878649493629684251, 0.003757040367692799938 ),
 .UNSPECIFIED. ) ;
#2757=DIRECTION ( 'NONE',  ( -1.000000000000000000, -0.000000000000000000, -0.000000000000000000 ) ) ;
#2766=VERTEX_POINT ( 'NONE', #10760 ) ;
#2767=EDGE_CURVE ( 'NONE', #2736, #5005, #1456, .T. ) ;
#2769=CARTESIAN_POINT ( 'NONE',  ( 0.02436607992776411782, -16.37294372382844543, -18.55949924794910544 ) ) ;
#2782=B_SPLINE_CURVE_WITH_KNOTS ( 'NONE', 3,
 ( #10099, #11397, #13092, #6775 ),
 .UNSPECIFIED., .F., .F.,
 ( 4, 4 ),
 ( 2.034713381942717888E-07, 0.0006045424356927869836 ),
 .UNSPECIFIED. ) ;
#2788=CARTESIAN_POINT ( 'NONE',  ( 2.789999999999999147, -24.63872515616080960, -2.336989772644527008 ) ) ;
#2789=EDGE_LOOP ( 'NONE', ( #15950, #5872, #15281, #4846, #8667, #14112, #484, #5555 ) ) ;
#2793=CIRCLE ( 'NONE', #13352, 2.524999999999996803 ) ;
#2798=DIRECTION ( 'NONE',  ( 0.000000000000000000, 0.000000000000000000, 1.000000000000000000 ) ) ;
#2802=ADVANCED_FACE ( 'NONE', ( #3351 ), #8707, .T. ) ;
#2805=ORIENTED_EDGE ( 'NONE', *, *, #13441, .F. ) ;
#2808=AXIS2_PLACEMENT_3D ( 'NONE', #6377, #13806, #1706 ) ;
#2812=CARTESIAN_POINT ( 'NONE',  ( 2.765633920072235075, 24.63872515616082737, -2.336989772644355590 ) ) ;
#2813=EDGE_LOOP ( 'NONE', ( #17249, #3967, #4971, #10523, #8736, #9617, #19605 ) ) ;
#2814=CARTESIAN_POINT ( 'NONE',  ( 0.000000000000000000, -24.04302995059967429, 1.991882183130232242 ) ) ;
#2816=CARTESIAN_POINT ( 'NONE',  ( 0.7589665089996495695, 24.80232951178378187, 12.05173163741731202 ) ) ;
#2818=CARTESIAN_POINT ( 'NONE',  ( -10.00000000000000000, 0.000000000000000000, 0.000000000000000000 ) ) ;
#2819=EDGE_LOOP ( 'NONE', ( #14388, #2416 ) ) ;
#2825=DIRECTION ( 'NONE',  ( -1.000000000000000000, 0.000000000000000000, 0.000000000000000000 ) ) ;
#2828=ORIENTED_EDGE ( 'NONE', *, *, #3804, .T. ) ;
#2829=B_SPLINE_CURVE_WITH_KNOTS ( 'NONE', 3,
 ( #18586, #8179, #18683, #4785 ),
 .UNSPECIFIED., .F., .F.,
 ( 4, 4 ),
 ( 0.005258105385878676132, 0.005948373736081387537 ),
 .UNSPECIFIED. ) ;
#2833=CARTESIAN_POINT ( 'NONE',  ( 0.7589665349472735079, 4.828387785248019703, 27.14933624560909919 ) ) ;
#2835=EDGE_CURVE ( 'NONE', #9369, #19326, #15464, .T. ) ;
#2841=DIRECTION ( 'NONE',  ( 0.000000000000000000, 0.000000000000000000, 1.000000000000000000 ) ) ;
#2844=ORIENTED_EDGE ( 'NONE', *, *, #9903, .F. ) ;
#2849=ORIENTED_EDGE ( 'NONE', *, *, #10988, .T. ) ;
#2850=VERTEX_POINT ( 'NONE', #13760 ) ;
#2854=EDGE_CURVE ( 'NONE', #10624, #15829, #5970, .T. ) ;
#2855=ORIENTED_EDGE ( 'NONE', *, *, #8486, .T. ) ;
#2856=AXIS2_PLACEMENT_3D ( 'NONE', #10060, #16162, #13432 ) ;
#2868=DIRECTION ( 'NONE',  ( -1.000000000000000000, 0.000000000000000000, 0.000000000000000000 ) ) ;
#2869=AXIS2_PLACEMENT_3D ( 'NONE', #10122, #16222, #3911 ) ;
#2874=FACE_OUTER_BOUND ( 'NONE', #4273, .T. ) ;
#2883=B_SPLINE_CURVE_WITH_KNOTS ( 'NONE', 3,
 ( #8110, #14219, #5208, #17221, #6301, #12525 ),
 .UNSPECIFIED., .F., .F.,
 ( 4, 2, 4 ),
 ( 2.321268216997094965E-07, 0.001878622960950492287, 0.003757013795079284547 ),
 .UNSPECIFIED. ) ;
#2894=ORIENTED_EDGE ( 'NONE', *, *, #1008, .T. ) ;
#2895=DIRECTION ( 'NONE',  ( -1.000000000000000000, -0.000000000000000000, -0.000000000000000000 ) ) ;
#2902=CYLINDRICAL_SURFACE ( 'NONE', #4530, 13.19999999999999929 ) ;
#2903=CARTESIAN_POINT ( 'NONE',  ( 1.039999999999995817, 27.76164181293051669, 4.147968289691385202 ) ) ;
#2909=EDGE_LOOP ( 'NONE', ( #185, #12171, #12080, #172, #15264, #17631, #15717, #16655 ) ) ;
#2913=CARTESIAN_POINT ( 'NONE',  ( 0.02436607992776325046, -24.15498966839958683, -5.391175441198872598 ) ) ;
#2914=ORIENTED_EDGE ( 'NONE', *, *, #2598, .F. ) ;
#2915=B_SPLINE_CURVE_WITH_KNOTS ( 'NONE', 3,
 ( #2070, #15981, #15683, #8069 ),
 .UNSPECIFIED., .F., .F.,
 ( 4, 4 ),
 ( 0.005258110598983609975, 0.005948376585272729597 ),
 .UNSPECIFIED. ) ;
#2918=B_SPLINE_CURVE_WITH_KNOTS ( 'NONE', 3,
 ( #1601, #507, #1994, #7692 ),
 .UNSPECIFIED., .F., .F.,
 ( 4, 4 ),
 ( 2.135345996541640089E-07, 0.0006888010880211291841 ),
 .UNSPECIFIED. ) ;
#2921=CARTESIAN_POINT ( 'NONE',  ( 2.179781338987520467, -23.94322454545470436, 12.96989951879399072 ) ) ;
#2928=AXIS2_PLACEMENT_3D ( 'NONE', #14727, #19714, #14823 ) ;
#2931=ORIENTED_EDGE ( 'NONE', *, *, #873, .T. ) ;
#2935=ORIENTED_EDGE ( 'NONE', *, *, #12271, .F. ) ;
#2937=DIRECTION ( 'NONE',  ( -1.000000000000000000, 0.000000000000000000, -0.000000000000000000 ) ) ;
#2938=CIRCLE ( 'NONE', #11266, 2.524999999999995914 ) ;
#2940=AXIS2_PLACEMENT_3D ( 'NONE', #14995, #13486, #2481 ) ;
#2941=CARTESIAN_POINT ( 'NONE',  ( 2.789999999999999147, 22.71065055754465689, -9.836394144775473691 ) ) ;
#2945=EDGE_LOOP ( 'NONE', ( #5707, #1193, #1893, #387 ) ) ;
#2954=DIRECTION ( 'NONE',  ( 0.000000000000000000, 0.000000000000000000, 1.000000000000000000 ) ) ;
#2957=CARTESIAN_POINT ( 'NONE',  ( 1.749999999999998002, -27.76164181293049182, -4.147968289691579713 ) ) ;
#2958=ORIENTED_EDGE ( 'NONE', *, *, #16901, .F. ) ;
#2960=AXIS2_PLACEMENT_3D ( 'NONE', #16752, #10085, #15047 ) ;
#2962=VERTEX_POINT ( 'NONE', #19147 ) ;
#2963=CIRCLE ( 'NONE', #9694, 24.12539914357697413 ) ;
#2967=FACE_OUTER_BOUND ( 'NONE', #15097, .T. ) ;
#2973=FILL_AREA_STYLE ('',( #16390 ) ) ;
#2976=CARTESIAN_POINT ( 'NONE',  ( 0.000000000000000000, 23.48180575137729775, 5.535312321042836103 ) ) ;
#2977=AXIS2_PLACEMENT_3D ( 'NONE', #2614, #4029, #16150 ) ;
#2982=VERTEX_POINT ( 'NONE', #8149 ) ;
#2986=MECHANICAL_DESIGN_GEOMETRIC_PRESENTATION_REPRESENTATION('',(#15452),#6485);
#2990=CIRCLE ( 'NONE', #9390, 2.524999999999995914 ) ;
#2992=CARTESIAN_POINT ( 'NONE',  ( 2.789999999999999147, 24.34211360614300190, 7.909232158574900140 ) ) ;
#2994=DIRECTION ( 'NONE',  ( -1.000000000000000000, -0.000000000000000000, -0.000000000000000000 ) ) ;
#2999=CARTESIAN_POINT ( 'NONE',  ( 2.604434514863826156, 10.67816411292164958, 23.63475234378986300 ) ) ;
#3000=B_SPLINE_CURVE_WITH_KNOTS ( 'NONE', 3,
 ( #5622, #2429, #17839, #13047 ),
 .UNSPECIFIED., .F., .F.,
 ( 4, 4 ),
 ( 1.981826382900813409E-07, 0.0006887856082032195850 ),
 .UNSPECIFIED. ) ;
#3003=CARTESIAN_POINT ( 'NONE',  ( 2.765633920072234631, 16.37294372382885044, -18.55949924794875017 ) ) ;
#3006=EDGE_CURVE ( 'NONE', #6920, #8766, #7103, .T. ) ;
#3020=CARTESIAN_POINT ( 'NONE',  ( 0.5321745407694743468, -26.58873630738047922, -4.993157874728098022 ) ) ;
#3021=EDGE_LOOP ( 'NONE', ( #9314, #6274, #5228, #2146, #136, #12210 ) ) ;
#3023=ADVANCED_FACE ( 'NONE', ( #13711 ), #15412, .F. ) ;
#3029=ORIENTED_EDGE ( 'NONE', *, *, #2426, .F. ) ;
#3032=B_SPLINE_CURVE_WITH_KNOTS ( 'NONE', 3,
 ( #13683, #7565, #4181, #7256 ),
 .UNSPECIFIED., .F., .F.,
 ( 4, 4 ),
 ( 0.005258110598983608240, 0.005948376585272733066 ),
 .UNSPECIFIED. ) ;
#3034=EDGE_CURVE ( 'NONE', #18102, #11367, #14166, .T. ) ;
#3038=VECTOR ( 'NONE', #658, 1000.000000000000000 ) ;
#3042=B_SPLINE_CURVE_WITH_KNOTS ( 'NONE', 3,
 ( #5003, #8202, #3892, #2390, #3796, #11207 ),
 .UNSPECIFIED., .F., .F.,
 ( 4, 2, 4 ),
 ( 4.462636682233640623E-07, 0.001879885020955585333, 0.003759323778242947261 ),
 .UNSPECIFIED. ) ;
#3050=VERTEX_POINT ( 'NONE', #10713 ) ;
#3051=ORIENTED_EDGE ( 'NONE', *, *, #14724, .T. ) ;
#3052=CARTESIAN_POINT ( 'NONE',  ( 0.1855657389739081564, 25.39738473785008210, -5.253342437939463316 ) ) ;
#3070=DIRECTION ( 'NONE',  ( 1.000000000000000000, 0.000000000000000000, 0.000000000000000000 ) ) ;
#3076=CARTESIAN_POINT ( 'NONE',  ( 2.765633920072239071, -16.37294372382844543, -18.55949924794910544 ) ) ;
#3084=CARTESIAN_POINT ( 'NONE',  ( 0.02436607992776238310, -2.336989772644097574, -24.63872515616085224 ) ) ;
#3087=EDGE_CURVE ( 'NONE', #14880, #4759, #6473, .T. ) ;
#3090=DIRECTION ( 'NONE',  ( -1.000000000000000000, 0.000000000000000000, 0.000000000000000000 ) ) ;
#3093=SURFACE_STYLE_USAGE ( .BOTH. , #4601 ) ;
#3095=EDGE_CURVE ( 'NONE', #6790, #1120, #13387, .T. ) ;
#3099=CIRCLE ( 'NONE', #14287, 24.12539914357697768 ) ;
#3115=CARTESIAN_POINT ( 'NONE',  ( 0.000000000000000000, 0.000000000000000000, 0.000000000000000000 ) ) ;
#3119=CARTESIAN_POINT ( 'NONE',  ( 0.5279272304333949561, 24.43806413951675793, 11.57956866523226580 ) ) ;
#3125=ORIENTED_EDGE ( 'NONE', *, *, #3539, .F. ) ;
#3126=CARTESIAN_POINT ( 'NONE',  ( 2.789999999999999147, -18.55949924794880346, -16.37294372382878649 ) ) ;
#3129=CIRCLE ( 'NONE', #14318, 2.524999999999995914 ) ;
#3131=CARTESIAN_POINT ( 'NONE',  ( 2.789999999999999147, 18.55949924794916228, -16.37294372382838148 ) ) ;
#3135=DIRECTION ( 'NONE',  ( -1.000000000000000000, 0.000000000000000000, 0.000000000000000000 ) ) ;
#3139=EDGE_CURVE ( 'NONE', #12686, #303, #16270, .T. ) ;
#3140=CARTESIAN_POINT ( 'NONE',  ( 2.789999999999999147, 20.62201879784912606, 12.52067188844359080 ) ) ;
#3141=LINE ( 'NONE', #18160, #2641 ) ;
#3143=ORIENTED_EDGE ( 'NONE', *, *, #13340, .F. ) ;
#3144=CARTESIAN_POINT ( 'NONE',  ( 1.749999999999998002, 12.52377138324259143, -25.12109765559640451 ) ) ;
#3146=ORIENTED_EDGE ( 'NONE', *, *, #18220, .F. ) ;
#3149=SHAPE_DEFINITION_REPRESENTATION ( #16425, #451 ) ;
#3150=CARTESIAN_POINT ( 'NONE',  ( 2.604434283110813819, 12.84444904262057818, -22.53097606932971075 ) ) ;
#3153=VERTEX_POINT ( 'NONE', #15609 ) ;
#3154=CARTESIAN_POINT ( 'NONE',  ( 0.07181523211953061425, 10.24584646439538993, 23.19431517146936983 ) ) ;
#3157=ORIENTED_EDGE ( 'NONE', *, *, #14706, .F. ) ;
#3163=FACE_OUTER_BOUND ( 'NONE', #3334, .T. ) ;
#3169=CARTESIAN_POINT ( 'NONE',  ( 1.749999999999998002, 0.000000000000000000, 0.000000000000000000 ) ) ;
#3171=DIRECTION ( 'NONE',  ( -1.000000000000000000, -0.000000000000000000, 0.000000000000000000 ) ) ;
#3175=CYLINDRICAL_SURFACE ( 'NONE', #17801, 13.19999999999999929 ) ;
#3187=CIRCLE ( 'NONE', #13107, 2.524999999999995914 ) ;
#3189=CARTESIAN_POINT ( 'NONE',  ( 2.783069004973550253, -23.92277630352791107, -5.408431875071696204 ) ) ;
#3195=CARTESIAN_POINT ( 'NONE',  ( 0.000000000000000000, 0.000000000000000000, 0.000000000000000000 ) ) ;
#3197=CARTESIAN_POINT ( 'NONE',  ( 1.394999999999998685, 25.12109765559671004, -12.52377138324198214 ) ) ;
#3198=EDGE_CURVE ( 'NONE', #13000, #17134, #3888, .T. ) ;
#3199=ORIENTED_EDGE ( 'NONE', *, *, #19720, .T. ) ;
#3208=VERTEX_POINT ( 'NONE', #7164 ) ;
#3223=CARTESIAN_POINT ( 'NONE',  ( 2.262072769566604524, -24.43806413951684320, 11.57956866523208461 ) ) ;
#3234=EDGE_LOOP ( 'NONE', ( #15468, #11160, #10435, #3496, #2654, #13520 ) ) ;
#3235=CARTESIAN_POINT ( 'NONE',  ( 0.7592463834391194322, -24.80264696524891477, 12.05220173035428921 ) ) ;
#3236=CARTESIAN_POINT ( 'NONE',  ( 2.783025228907520798, -22.53337530003396338, -9.686319561461189664 ) ) ;
#3238=CARTESIAN_POINT ( 'NONE',  ( 2.257825459230522913, 26.58873630738059290, -4.993157874727537582 ) ) ;
#3243=ORIENTED_EDGE ( 'NONE', *, *, #16183, .T. ) ;
#3248=AXIS2_PLACEMENT_3D ( 'NONE', #1415, #19415, #8816 ) ;
#3252=B_SPLINE_CURVE_WITH_KNOTS ( 'NONE', 3,
 ( #10799, #12602, #5081, #11194 ),
 .UNSPECIFIED., .F., .F.,
 ( 4, 4 ),
 ( 0.005258120783916792398, 0.005948386350302926374 ),
 .UNSPECIFIED. ) ;
#3261=EDGE_CURVE ( 'NONE', #17434, #4324, #5675, .T. ) ;
#3263=FACE_OUTER_BOUND ( 'NONE', #224, .T. ) ;
#3268=VERTEX_POINT ( 'NONE', #8687 ) ;
#3277=AXIS2_PLACEMENT_3D ( 'NONE', #3733, #6820, #12943 ) ;
#3280=DIRECTION ( 'NONE',  ( 1.000000000000000000, 0.000000000000000000, 0.000000000000000000 ) ) ;
#3288=B_SPLINE_CURVE_WITH_KNOTS ( 'NONE', 3,
 ( #17524, #13024, #11424, #1003, #10219, #19304 ),
 .UNSPECIFIED., .F., .F.,
 ( 4, 2, 4 ),
 ( 4.462636808935014747E-07, 0.001879885123572234236, 0.003759323983463574645 ),
 .UNSPECIFIED. ) ;
#3290=CARTESIAN_POINT ( 'NONE',  ( 8.000000000000000000, 0.000000000000000000, 0.000000000000000000 ) ) ;
#3292=CARTESIAN_POINT ( 'NONE',  ( 2.789999999999999147, 24.63872515616082737, 2.336989772644355146 ) ) ;
#3293=ORIENTED_EDGE ( 'NONE', *, *, #12127, .F. ) ;
#3295=CARTESIAN_POINT ( 'NONE',  ( 8.000000000000000000, 0.000000000000000000, 0.000000000000000000 ) ) ;
#3300=ORIENTED_EDGE ( 'NONE', *, *, #4939, .T. ) ;
#3303=CARTESIAN_POINT ( 'NONE',  ( 0.0001048300153468720319, 20.67846228565678146, -12.51925356660738053 ) ) ;
#3305=CYLINDRICAL_SURFACE ( 'NONE', #13803, 2.524999999999997691 ) ;
#3311=CARTESIAN_POINT ( 'NONE',  ( 2.790000000000076419, -2.133839912090968127, 24.22524813288760726 ) ) ;
#3313=CIRCLE ( 'NONE', #4913, 28.06981291497571362 ) ;
#3315=ADVANCED_FACE ( 'NONE', ( #11593 ), #13288, .T. ) ;
#3321=CARTESIAN_POINT ( 'NONE',  ( 2.765633920072235963, -24.63872515616080960, -2.336989772644527008 ) ) ;
#3324=DIRECTION ( 'NONE',  ( -1.000000000000000000, 0.000000000000000000, -0.000000000000000000 ) ) ;
#3328=CARTESIAN_POINT ( 'NONE',  ( 2.031033465052725084, -4.828387785248216879, 27.14933624560906367 ) ) ;
#3332=B_SPLINE_CURVE_WITH_KNOTS ( 'NONE', 3,
 ( #9490, #3377, #17086, #12483 ),
 .UNSPECIFIED., .F., .F.,
 ( 4, 4 ),
 ( 2.324263106244698315E-07, 0.0006888201370294716810 ),
 .UNSPECIFIED. ) ;
#3334=EDGE_LOOP ( 'NONE', ( #8820, #5201, #15772, #15557, #2606, #2299 ) ) ;
#3335=DIRECTION ( 'NONE',  ( -1.000000000000000000, 0.000000000000000000, 0.000000000000000000 ) ) ;
#3338=CARTESIAN_POINT ( 'NONE',  ( 2.789999999999999147, 18.28042085475278355, 15.74360496233388140 ) ) ;
#3339=EDGE_CURVE ( 'NONE', #11363, #17434, #14799, .T. ) ;
#3340=VERTEX_POINT ( 'NONE', #9914 ) ;
#3341=CIRCLE ( 'NONE', #15794, 28.06981291497571362 ) ;
#3342=CARTESIAN_POINT ( 'NONE',  ( 2.765633920072235519, 24.15498966839970052, -5.391175441198366336 ) ) ;
#3346=CARTESIAN_POINT ( 'NONE',  ( 0.000000000000000000, 9.324097380959415204, 22.25075486061743391 ) ) ;
#3348=CARTESIAN_POINT ( 'NONE',  ( 0.000000000000000000, -20.62201879784905501, -12.52067188844372936 ) ) ;
#3349=ORIENTED_EDGE ( 'NONE', *, *, #14817, .T. ) ;
#3351=FACE_OUTER_BOUND ( 'NONE', #10262, .T. ) ;
#3352=DIRECTION ( 'NONE',  ( 1.000000000000000000, -0.000000000000000000, -0.000000000000000000 ) ) ;
#3353=EDGE_CURVE ( 'NONE', #13895, #11363, #12291, .T. ) ;
#3357=CARTESIAN_POINT ( 'NONE',  ( 0.02436607992776498519, 9.836394144775706394, 22.71065055754456097 ) ) ;
#3360=EDGE_CURVE ( 'NONE', #10459, #5854, #7762, .T. ) ;
#3361=ADVANCED_FACE ( 'NONE', ( #18386 ), #7467, .T. ) ;
#3362=DIRECTION ( 'NONE',  ( 0.000000000000000000, -0.3090169943749406234, -0.9510565162951558627 ) ) ;
#3372=ADVANCED_FACE ( 'NONE', ( #2874 ), #3175, .T. ) ;
#3373=ORIENTED_EDGE ( 'NONE', *, *, #19677, .F. ) ;
#3375=CARTESIAN_POINT ( 'NONE',  ( 1.749999999999998002, 4.633866840649310426, -27.68468304288254345 ) ) ;
#3376=AXIS2_PLACEMENT_3D ( 'NONE', #10742, #18729, #12245 ) ;
#3377=CARTESIAN_POINT ( 'NONE',  ( 0.006974693931643255289, 16.17543236987988919, 18.43727551351037519 ) ) ;
#3383=ORIENTED_EDGE ( 'NONE', *, *, #4312, .T. ) ;
#3393=CARTESIAN_POINT ( 'NONE',  ( 2.789999999999999147, 24.34211360614310848, -7.909232158574561744 ) ) ;
#3395=VERTEX_POINT ( 'NONE', #2976 ) ;
#3397=DIRECTION ( 'NONE',  ( -1.000000000000000000, 0.000000000000000000, -0.000000000000000000 ) ) ;
#3398=DIRECTION ( 'NONE',  ( 0.000000000000000000, 0.000000000000000000, 1.000000000000000000 ) ) ;
#3408=LINE ( 'NONE', #14309, #12409 ) ;
#3409=EDGE_CURVE ( 'NONE', #758, #3208, #5875, .T. ) ;
#3412=DIRECTION ( 'NONE',  ( -1.000000000000000000, 0.000000000000000000, -0.000000000000000000 ) ) ;
#3422=EDGE_CURVE ( 'NONE', #18407, #2052, #18195, .T. ) ;
#3424=EDGE_LOOP ( 'NONE', ( #15892, #7889, #1986, #7366 ) ) ;
#3426=CARTESIAN_POINT ( 'NONE',  ( 1.749999999999998002, -25.12109765559663188, 12.52377138324213668 ) ) ;
#3427=ORIENTED_EDGE ( 'NONE', *, *, #1563, .F. ) ;
#3433=ORIENTED_EDGE ( 'NONE', *, *, #11726, .F. ) ;
#3435=DIRECTION ( 'NONE',  ( 0.000000000000000000, 0.8090169943749400128, 0.5877852522924831291 ) ) ;
#3437=ORIENTED_EDGE ( 'NONE', *, *, #6981, .F. ) ;
#3441=CARTESIAN_POINT ( 'NONE',  ( 1.039999999999997593, 0.000000000000000000, 0.000000000000000000 ) ) ;
#3445=B_SPLINE_CURVE_WITH_KNOTS ( 'NONE', 3,
 ( #16789, #9275, #1671, #13775 ),
 .UNSPECIFIED., .F., .F.,
 ( 4, 4 ),
 ( 2.324263106244698315E-07, 0.0006888201370294677779 ),
 .UNSPECIFIED. ) ;
#3446=ORIENTED_EDGE ( 'NONE', *, *, #1879, .T. ) ;
#3455=CARTESIAN_POINT ( 'NONE',  ( 0.000000000000000000, 0.000000000000000000, 0.000000000000000000 ) ) ;
#3459=EDGE_CURVE ( 'NONE', #15555, #18641, #3332, .T. ) ;
#3466=CARTESIAN_POINT ( 'NONE',  ( 0.000000000000000000, -15.04425356660744839, -18.18163861606288378 ) ) ;
#3476=CARTESIAN_POINT ( 'NONE',  ( 1.749999999999998002, 0.000000000000000000, 0.000000000000000000 ) ) ;
#3479=ORIENTED_EDGE ( 'NONE', *, *, #6249, .T. ) ;
#3486=EDGE_CURVE ( 'NONE', #608, #15823, #14130, .T. ) ;
#3490=FACE_OUTER_BOUND ( 'NONE', #5663, .T. ) ;
#3491=CARTESIAN_POINT ( 'NONE',  ( 0.000000000000000000, -23.48180575137736170, 5.535312321042622052 ) ) ;
#3493=CARTESIAN_POINT ( 'NONE',  ( 1.960886852992497653, -24.44424927289185590, 12.96989951879399072 ) ) ;
#3495=DIRECTION ( 'NONE',  ( 0.000000000000000000, 0.000000000000000000, 1.000000000000000000 ) ) ;
#3496=ORIENTED_EDGE ( 'NONE', *, *, #2355, .F. ) ;
#3497=DIRECTION ( 'NONE',  ( -1.000000000000000000, -0.000000000000000000, -0.000000000000000000 ) ) ;
#3502=ORIENTED_EDGE ( 'NONE', *, *, #18969, .F. ) ;
#3503=DIRECTION ( 'NONE',  ( -1.000000000000000000, -0.000000000000000000, -0.000000000000000000 ) ) ;
#3512=ORIENTED_EDGE ( 'NONE', *, *, #11223, .T. ) ;
#3513=CARTESIAN_POINT ( 'NONE',  ( 2.030753605846573162, -27.31305418910207905, -3.797885586973501759 ) ) ;
#3518=VERTEX_POINT ( 'NONE', #6509 ) ;
#3519=CARTESIAN_POINT ( 'NONE',  ( 2.790000000000000480, -22.37986894186679265, 9.514945144208653005 ) ) ;
#3523=CARTESIAN_POINT ( 'NONE',  ( 2.604434325169354913, 2.851997810081644769, 25.77772010606606301 ) ) ;
#3524=DIRECTION ( 'NONE',  ( -1.000000000000000000, -0.000000000000000000, -0.000000000000000000 ) ) ;
#3528=CARTESIAN_POINT ( 'NONE',  ( 2.783025336474040934, -21.08118142846912235, 12.53640742967745858 ) ) ;
#3529=CARTESIAN_POINT ( 'NONE',  ( 1.394999999999999574, 4.147968289691286614, 27.76164181293053090 ) ) ;
#3533=VECTOR ( 'NONE', #12701, 1000.000000000000000 ) ;
#3534=CARTESIAN_POINT ( 'NONE',  ( 2.789999999999999147, -7.909232158574647009, -21.81711360614308148 ) ) ;
#3539=EDGE_CURVE ( 'NONE', #725, #9066, #327, .T. ) ;
#3541=CARTESIAN_POINT ( 'NONE',  ( 0.0003207540509381473352, -20.70663861606275447, -12.51925356660783528 ) ) ;
#3545=CYLINDRICAL_SURFACE ( 'NONE', #633, 13.19999999999999929 ) ;
#3548=DIRECTION ( 'NONE',  ( 0.000000000000000000, 0.000000000000000000, 1.000000000000000000 ) ) ;
#3550=ORIENTED_EDGE ( 'NONE', *, *, #8918, .T. ) ;
#3552=EDGE_CURVE ( 'NONE', #16090, #10204, #9836, .T. ) ;
#3553=ORIENTED_EDGE ( 'NONE', *, *, #9049, .T. ) ;
#3555=AXIS2_PLACEMENT_3D ( 'NONE', #12882, #18979, #5270 ) ;
#3559=CARTESIAN_POINT ( 'NONE',  ( 2.257825477245766432, -18.57583492944434411, 19.66801664102697345 ) ) ;
#3561=ORIENTED_EDGE ( 'NONE', *, *, #4774, .F. ) ;
#3562=LINE ( 'NONE', #7115, #19080 ) ;
#3571=CIRCLE ( 'NONE', #14760, 24.12539914357697768 ) ;
#3574=AXIS2_PLACEMENT_3D ( 'NONE', #4612, #9315, #7897 ) ;
#3577=CARTESIAN_POINT ( 'NONE',  ( 2.789999999999999147, -5.391175441198450713, -24.15498966839968276 ) ) ;
#3578=EDGE_CURVE ( 'NONE', #11710, #4466, #17443, .T. ) ;
#3603=FACE_OUTER_BOUND ( 'NONE', #7503, .T. ) ;
#3604=CARTESIAN_POINT ( 'NONE',  ( 1.039999999999996261, 12.96210679857786197, 24.89775460606836788 ) ) ;
#3607=DIRECTION ( 'NONE',  ( 0.000000000000000000, 0.000000000000000000, 1.000000000000000000 ) ) ;
#3612=CARTESIAN_POINT ( 'NONE',  ( 2.789999999999999147, 1.991882183130632589, -24.04302995059963877 ) ) ;
#3620=EDGE_LOOP ( 'NONE', ( #16687, #6187, #4342, #15240, #1605, #89 ) ) ;
#3621=CARTESIAN_POINT ( 'NONE',  ( 2.604434261026088215, -5.253342437939904741, 25.39738473784999684 ) ) ;
#3622=EDGE_CURVE ( 'NONE', #19636, #15823, #11090, .T. ) ;
#3623=CARTESIAN_POINT ( 'NONE',  ( 0.1882239034349760531, 12.84621645676876867, -22.54313264454999199 ) ) ;
#3625=CARTESIAN_POINT ( 'NONE',  ( 2.030753610301994083, 19.12676442129372134, -19.86438386685639657 ) ) ;
#3626=CARTESIAN_POINT ( 'NONE',  ( 1.039999999999995595, 20.02152543075345648, 19.67366047555537278 ) ) ;
#3627=ORIENTED_EDGE ( 'NONE', *, *, #7968, .T. ) ;
#3630=ORIENTED_EDGE ( 'NONE', *, *, #2598, .T. ) ;
#3631=EDGE_CURVE ( 'NONE', #7114, #5932, #11687, .T. ) ;
#3643=CARTESIAN_POINT ( 'NONE',  ( -7.722669826818730404E-14, -20.65026423218563778, -12.51972477286604502 ) ) ;
#3647=ORIENTED_EDGE ( 'NONE', *, *, #11378, .F. ) ;
#3662=CARTESIAN_POINT ( 'NONE',  ( 0.5321745379877909077, -23.74442027961350377, -12.96514671151793507 ) ) ;
#3663=CARTESIAN_POINT ( 'NONE',  ( 0.9661342547375842971, -24.74813374239834474, 12.96725027898183669 ) ) ;
#3665=ORIENTED_EDGE ( 'NONE', *, *, #5162, .F. ) ;
#3667=EDGE_CURVE ( 'NONE', #18545, #3927, #15024, .T. ) ;
#3670=LINE ( 'NONE', #8175, #4878 ) ;
#3678=CARTESIAN_POINT ( 'NONE',  ( 1.394999999999999574, 20.02152543075346003, 19.67366047555537634 ) ) ;
#3681=CARTESIAN_POINT ( 'NONE',  ( 2.031033491000346913, -12.05173163741705444, -24.80232951178391332 ) ) ;
#3682=CARTESIAN_POINT ( 'NONE',  ( 2.765633920072241292, 18.55949924794916228, -16.37294372382838148 ) ) ;
#3691=DIRECTION ( 'NONE',  ( 0.000000000000000000, 0.000000000000000000, 1.000000000000000000 ) ) ;
#3692=CARTESIAN_POINT ( 'NONE',  ( 2.031033491000347357, 12.05173163741723030, 24.80232951178382805 ) ) ;
#3701=CARTESIAN_POINT ( 'NONE',  ( 2.789999999999999147, 9.836394144775706394, 22.71065055754456097 ) ) ;
#3705=DIRECTION ( 'NONE',  ( -1.000000000000000000, -0.000000000000000000, 0.000000000000000000 ) ) ;
#3708=EDGE_CURVE ( 'NONE', #15591, #18627, #13604, .T. ) ;
#3710=CARTESIAN_POINT ( 'NONE',  ( 0.000000000000000000, 1.991882183130315953, 24.04302995059967074 ) ) ;
#3711=ORIENTED_EDGE ( 'NONE', *, *, #14684, .F. ) ;
#3721=ORIENTED_EDGE ( 'NONE', *, *, #7803, .T. ) ;
#3724=AXIS2_PLACEMENT_3D ( 'NONE', #5371, #785, #6960 ) ;
#3731=VERTEX_POINT ( 'NONE', #19508 ) ;
#3732=CIRCLE ( 'NONE', #15235, 28.06981291497571007 ) ;
#3733=CARTESIAN_POINT ( 'NONE',  ( 2.789999999999999147, 0.2301004812057544924, 24.44424927289185590 ) ) ;
#3734=VECTOR ( 'NONE', #1828, 1000.000000000000000 ) ;
#3736=CARTESIAN_POINT ( 'NONE',  ( 2.601776105308176934, 2.857713464479052057, -25.78859396478524957 ) ) ;
#3739=CARTESIAN_POINT ( 'NONE',  ( 0.02436607992776021470, 21.30679549418649543, -12.59161484032888723 ) ) ;
#3742=ORIENTED_EDGE ( 'NONE', *, *, #1879, .F. ) ;
#3750=VERTEX_POINT ( 'NONE', #15018 ) ;
#3751=CARTESIAN_POINT ( 'NONE',  ( 0.000000000000000000, 5.535312321042724193, 23.48180575137730841 ) ) ;
#3760=B_SPLINE_CURVE_WITH_KNOTS ( 'NONE', 3,
 ( #16702, #13694, #7578, #10597 ),
 .UNSPECIFIED., .F., .F.,
 ( 4, 4 ),
 ( 0.005258120783916810613, 0.005948386350302961936 ),
 .UNSPECIFIED. ) ;
#3761=ADVANCED_FACE ( 'NONE', ( #4408 ), #9217, .T. ) ;
#3774=ORIENTED_EDGE ( 'NONE', *, *, #16433, .F. ) ;
#3782=CARTESIAN_POINT ( 'NONE',  ( 1.960886852992457241, 24.44424927289185945, 12.96989951879416125 ) ) ;
#3787=DIRECTION ( 'NONE',  ( 0.000000000000000000, 1.374038396813314756E-15, -1.000000000000000000 ) ) ;
#3791=CARTESIAN_POINT ( 'NONE',  ( 1.394999999999999574, 4.147968289691677413, -27.76164181293047761 ) ) ;
#3796=CARTESIAN_POINT ( 'NONE',  ( 0.07181525696555295102, -5.344212458769539431, 24.78695292654919768 ) ) ;
#3800=CARTESIAN_POINT ( 'NONE',  ( 0.02436607992776628623, 24.63872515616082737, -2.336989772644355590 ) ) ;
#3804=EDGE_CURVE ( 'NONE', #7952, #3208, #5936, .T. ) ;
#3805=CARTESIAN_POINT ( 'NONE',  ( 1.039999999999996483, 4.147968289691283950, 27.76164181293052735 ) ) ;
#3817=CARTESIAN_POINT ( 'NONE',  ( 2.765633920072241736, -9.836394144775550075, -22.71065055754462492 ) ) ;
#3819=CARTESIAN_POINT ( 'NONE',  ( 2.262072661820536901, 3.461047254864260125, 26.82026385750179287 ) ) ;
#3821=CARTESIAN_POINT ( 'NONE',  ( 2.718184757033982546, 16.91181672897760535, -18.89296398180173497 ) ) ;
#3825=EDGE_CURVE ( 'NONE', #13278, #9359, #19068, .T. ) ;
#3830=EDGE_CURVE ( 'NONE', #3750, #1741, #8096, .T. ) ;
#3835=CARTESIAN_POINT ( 'NONE',  ( 2.789999999999999147, -15.04425356660774682, 20.70663861606266209 ) ) ;
#3838=CARTESIAN_POINT ( 'NONE',  ( 0.02436607992775978102, 2.336989772644613161, -24.63872515616080250 ) ) ;
#3841=ORIENTED_EDGE ( 'NONE', *, *, #8446, .F. ) ;
#3845=CARTESIAN_POINT ( 'NONE',  ( 2.789999999999999147, -23.31896751603326834, -7.334849878007764445 ) ) ;
#3849=DIRECTION ( 'NONE',  ( 0.000000000000000000, 0.000000000000000000, -1.000000000000000000 ) ) ;
#3851=AXIS2_PLACEMENT_3D ( 'NONE', #10591, #17894, #13386 ) ;
#3852=AXIS2_PLACEMENT_3D ( 'NONE', #4700, #18406, #18695 ) ;
#3855=B_SPLINE_CURVE_WITH_KNOTS ( 'NONE', 3,
 ( #9751, #15842, #11040, #12546 ),
 .UNSPECIFIED., .F., .F.,
 ( 4, 4 ),
 ( 0.005258105385878685673, 0.005948373736081384068 ),
 .UNSPECIFIED. ) ;
#3864=ORIENTED_EDGE ( 'NONE', *, *, #16085, .F. ) ;
#3866=DIRECTION ( 'NONE',  ( -1.000000000000000000, -0.000000000000000000, 0.000000000000000000 ) ) ;
#3868=VERTEX_POINT ( 'NONE', #302 ) ;
#3879=CARTESIAN_POINT ( 'NONE',  ( 2.601776091974069782, -25.40949241676357317, 5.251266773802275800 ) ) ;
#3882=DIRECTION ( 'NONE',  ( 0.000000000000000000, 0.000000000000000000, 1.000000000000000000 ) ) ;
#3884=ORIENTED_EDGE ( 'NONE', *, *, #3830, .T. ) ;
#3887=AXIS2_PLACEMENT_3D ( 'NONE', #14712, #7079, #17711 ) ;
#3888=LINE ( 'NONE', #19385, #756 ) ;
#3892=CARTESIAN_POINT ( 'NONE',  ( 0.5321745407694777885, -4.993157874728001211, 26.58873630738050409 ) ) ;
#3893=B_SPLINE_CURVE_WITH_KNOTS ( 'NONE', 3,
 ( #9420, #7998, #12712, #15811 ),
 .UNSPECIFIED., .F., .F.,
 ( 4, 4 ),
 ( 0.005342776758202895035, 0.005948405594583416715 ),
 .UNSPECIFIED. ) ;
#3904=AXIS2_PLACEMENT_3D ( 'NONE', #14181, #6453, #17580 ) ;
#3906=LINE ( 'NONE', #5689, #18014 ) ;
#3908=DIRECTION ( 'NONE',  ( 0.000000000000000000, 0.000000000000000000, 1.000000000000000000 ) ) ;
#3910=AXIS2_PLACEMENT_3D ( 'NONE', #1575, #13381, #1281 ) ;
#3911=DIRECTION ( 'NONE',  ( 0.000000000000000000, 0.000000000000000000, -1.000000000000000000 ) ) ;
#3913=CARTESIAN_POINT ( 'NONE',  ( 2.789999999999999147, 18.55949924794892780, 16.37294372382865504 ) ) ;
#3924=CARTESIAN_POINT ( 'NONE',  ( 1.749999999999998002, 12.96210679857786552, 24.89775460606837143 ) ) ;
#3925=DIRECTION ( 'NONE',  ( -1.000000000000000000, -0.000000000000000000, -0.000000000000000000 ) ) ;
#3927=VERTEX_POINT ( 'NONE', #401 ) ;
#3949=CARTESIAN_POINT ( 'NONE',  ( 0.000000000000000000, -8.936381166381891568E-14, 25.59481291497571220 ) ) ;
#3957=AXIS2_PLACEMENT_3D ( 'NONE', #2992, #3090, #9205 ) ;
#3967=ORIENTED_EDGE ( 'NONE', *, *, #5488, .F. ) ;
#3968=ORIENTED_EDGE ( 'NONE', *, *, #11443, .F. ) ;
#3974=CARTESIAN_POINT ( 'NONE',  ( 1.039999999999996483, -12.96210679857803783, 24.89775460606827551 ) ) ;
#3975=ORIENTED_EDGE ( 'NONE', *, *, #5358, .F. ) ;
#3977=VECTOR ( 'NONE', #9960, 1000.000000000000000 ) ;
#3978=ORIENTED_EDGE ( 'NONE', *, *, #10697, .T. ) ;
#3979=CARTESIAN_POINT ( 'NONE',  ( 0.000000000000000000, 0.000000000000000000, 0.000000000000000000 ) ) ;
#3982=EDGE_CURVE ( 'NONE', #9010, #11813, #1834, .T. ) ;
#3983=CARTESIAN_POINT ( 'NONE',  ( 1.039999999999997815, 27.68468304288265003, -4.633866840648637186 ) ) ;
#3985=DIRECTION ( 'NONE',  ( -1.000000000000000000, -0.000000000000000000, -0.000000000000000000 ) ) ;
#3994=EDGE_CURVE ( 'NONE', #19037, #2313, #5241, .T. ) ;
#3996=CARTESIAN_POINT ( 'NONE',  ( 2.030753616560878161, -12.05220173035456632, 24.80264696524878687 ) ) ;
#4002=EDGE_CURVE ( 'NONE', #18335, #10204, #17773, .T. ) ;
#4007=CARTESIAN_POINT ( 'NONE',  ( 2.789999999999999147, 22.25075486061738772, 9.324097380959527115 ) ) ;
#4011=DIRECTION ( 'NONE',  ( 0.000000000000000000, 0.000000000000000000, 1.000000000000000000 ) ) ;
#4018=DIRECTION ( 'NONE',  ( 1.000000000000000000, -0.000000000000000000, -0.000000000000000000 ) ) ;
#4021=AXIS2_PLACEMENT_3D ( 'NONE', #15172, #12836, #3435 ) ;
#4022=EDGE_LOOP ( 'NONE', ( #17706, #2141, #14777, #12014 ) ) ;
#4026=EDGE_CURVE ( 'NONE', #13429, #540, #19091, .T. ) ;
#4027=DIRECTION ( 'NONE',  ( -1.000000000000000000, 0.000000000000000000, -0.000000000000000000 ) ) ;
#4028=EDGE_CURVE ( 'NONE', #3750, #1726, #9854, .T. ) ;
#4029=DIRECTION ( 'NONE',  ( -1.000000000000000000, -0.000000000000000000, -0.000000000000000000 ) ) ;
#4031=ORIENTED_EDGE ( 'NONE', *, *, #13132, .T. ) ;
#4046=EDGE_LOOP ( 'NONE', ( #10611, #14688, #10267, #6336 ) ) ;
#4051=B_SPLINE_CURVE_WITH_KNOTS ( 'NONE', 3,
 ( #12143, #2921, #10541, #132, #4432, #10740 ),
 .UNSPECIFIED., .F., .F.,
 ( 4, 2, 4 ),
 ( 0.0004963285629697519611, 0.002127826186449857486, 0.003759323809929962686 ),
 .UNSPECIFIED. ) ;
#4054=CARTESIAN_POINT ( 'NONE',  ( 2.765633920072236407, -2.336989772644440855, 24.63872515616082026 ) ) ;
#4060=CIRCLE ( 'NONE', #5958, 28.06981291497571362 ) ;
#4062=ADVANCED_FACE ( 'NONE', ( #351 ), #1204, .T. ) ;
#4067=CARTESIAN_POINT ( 'NONE',  ( 1.394999999999999574, -4.147968289691484678, 27.76164181293050603 ) ) ;
#4068=ORIENTED_EDGE ( 'NONE', *, *, #13316, .T. ) ;
#4070=DIRECTION ( 'NONE',  ( 0.000000000000000000, 0.000000000000000000, 1.000000000000000000 ) ) ;
#4073=EDGE_CURVE ( 'NONE', #2268, #6765, #18757, .T. ) ;
#4082=CARTESIAN_POINT ( 'NONE',  ( 2.789999999999999147, 18.28042085475301093, -15.74360496233361673 ) ) ;
#4084=B_SPLINE_CURVE_WITH_KNOTS ( 'NONE', 3,
 ( #10340, #19041, #10050, #13237, #1127, #5613 ),
 .UNSPECIFIED., .F., .F.,
 ( 4, 2, 4 ),
 ( 4.462636808902389156E-07, 0.001879885123572227514, 0.003759323983463565104 ),
 .UNSPECIFIED. ) ;
#4085=DIRECTION ( 'NONE',  ( 0.000000000000000000, 0.000000000000000000, 1.000000000000000000 ) ) ;
#4087=CARTESIAN_POINT ( 'NONE',  ( 1.749999999999998002, -24.89775460606842117, 12.96210679857777137 ) ) ;
#4097=CARTESIAN_POINT ( 'NONE',  ( 1.394999999999999574, 12.52377138324224148, 25.12109765559658570 ) ) ;
#4098=CARTESIAN_POINT ( 'NONE',  ( 0.000000000000000000, -7.909232158574647009, -24.34211360614308006 ) ) ;
#4099=ORIENTED_EDGE ( 'NONE', *, *, #5407, .T. ) ;
#4101=CARTESIAN_POINT ( 'NONE',  ( 2.765633920072234631, 5.391175441198615914, 24.15498966839965078 ) ) ;
#4103=CARTESIAN_POINT ( 'NONE',  ( 2.783068930044319433, -18.43696893154769612, 16.17493693894872564 ) ) ;
#4105=ORIENTED_EDGE ( 'NONE', *, *, #14586, .T. ) ;
#4108=CARTESIAN_POINT ( 'NONE',  ( 0.006974693931642885793, -18.43727551351043203, 16.17543236987982525 ) ) ;
#4110=DIRECTION ( 'NONE',  ( 0.000000000000000000, 0.000000000000000000, 1.000000000000000000 ) ) ;
#4112=CARTESIAN_POINT ( 'NONE',  ( 0.000000000000000000, 20.62201879784911540, 12.52067188844362100 ) ) ;
#4133=DIRECTION ( 'NONE',  ( -1.000000000000000000, 0.000000000000000000, 0.000000000000000000 ) ) ;
#4134=ORIENTED_EDGE ( 'NONE', *, *, #17837, .T. ) ;
#4137=AXIS2_PLACEMENT_3D ( 'NONE', #4457, #6237, #10566 ) ;
#4147=CARTESIAN_POINT ( 'NONE',  ( 0.5279273746168620107, 4.996265754456365116, 26.57710921259763026 ) ) ;
#4155=EDGE_LOOP ( 'NONE', ( #13488, #15124, #11388, #6997, #13579, #15531, #13777 ) ) ;
#4159=ORIENTED_EDGE ( 'NONE', *, *, #13395, .T. ) ;
#4161=CARTESIAN_POINT ( 'NONE',  ( 0.000000000000000000, 12.52067188844351442, 20.62201879784919001 ) ) ;
#4165=EDGE_CURVE ( 'NONE', #12173, #13180, #2050, .T. ) ;
#4166=CARTESIAN_POINT ( 'NONE',  ( 0.5279273746168618997, -26.57710921259763737, 4.996265754456265640 ) ) ;
#4170=EDGE_CURVE ( 'NONE', #11710, #8006, #14627, .T. ) ;
#4173=B_SPLINE_CURVE_WITH_KNOTS ( 'NONE', 3,
 ( #19609, #4108, #18215, #2596 ),
 .UNSPECIFIED., .F., .F.,
 ( 4, 4 ),
 ( 2.324263106244687463E-07, 0.0006888201370294697295 ),
 .UNSPECIFIED. ) ;
#4177=PLANE ( 'NONE',  #13191 ) ;
#4178=FACE_OUTER_BOUND ( 'NONE', #1548, .T. ) ;
#4181=CARTESIAN_POINT ( 'NONE',  ( 2.783068930044318545, 16.17493693894878604, 18.43696893154764282 ) ) ;
#4201=CARTESIAN_POINT ( 'NONE',  ( 2.789999999999999147, 24.63872515616082737, -2.336989772644355590 ) ) ;
#4203=CARTESIAN_POINT ( 'NONE',  ( 2.789999999999999147, -2.336989772644097574, -24.63872515616085224 ) ) ;
#4212=CARTESIAN_POINT ( 'NONE',  ( 0.000000000000000000, 5.535312321043032391, -23.48180575137725867 ) ) ;
#4214=EDGE_CURVE ( 'NONE', #881, #16591, #18456, .T. ) ;
#4225=DIRECTION ( 'NONE',  ( -1.000000000000000000, -0.000000000000000000, -0.000000000000000000 ) ) ;
#4230=ORIENTED_EDGE ( 'NONE', *, *, #14483, .T. ) ;
#4234=CARTESIAN_POINT ( 'NONE',  ( 0.1855656748306439008, -25.77772010606603814, -2.851997810081915663 ) ) ;
#4235=AXIS2_PLACEMENT_3D ( 'NONE', #16684, #13471, #6058 ) ;
#4236=VERTEX_POINT ( 'NONE', #10157 ) ;
#4251=FACE_OUTER_BOUND ( 'NONE', #17462, .T. ) ;
#4252=CIRCLE ( 'NONE', #11906, 24.12539914357697413 ) ;
#4254=B_SPLINE_CURVE_WITH_KNOTS ( 'NONE', 3,
 ( #3003, #12321, #12514, #15221 ),
 .UNSPECIFIED., .F., .F.,
 ( 4, 4 ),
 ( 2.324263106244727961E-07, 0.0006888201370294844746 ),
 .UNSPECIFIED. ) ;
#4256=CARTESIAN_POINT ( 'NONE',  ( 2.031033467310412011, -24.32849926382740335, -12.98167595241049277 ) ) ;
#4262=ORIENTED_EDGE ( 'NONE', *, *, #11018, .T. ) ;
#4269=ORIENTED_EDGE ( 'NONE', *, *, #18519, .F. ) ;
#4272=CARTESIAN_POINT ( 'NONE',  ( 0.07186814640506919427, -12.74240566898967764, -21.92302674874977697 ) ) ;
#4273=EDGE_LOOP ( 'NONE', ( #2483, #6898, #4493, #3550 ) ) ;
#4279=DIRECTION ( 'NONE',  ( -1.000000000000000000, -0.000000000000000000, -0.000000000000000000 ) ) ;
#4280=CARTESIAN_POINT ( 'NONE',  ( -5.209999999999999964, 0.000000000000000000, 0.000000000000000000 ) ) ;
#4306=VERTEX_POINT ( 'NONE', #7317 ) ;
#4308=ORIENTED_EDGE ( 'NONE', *, *, #5980, .T. ) ;
#4312=EDGE_CURVE ( 'NONE', #10459, #18268, #18765, .T. ) ;
#4314=LINE ( 'NONE', #12323, #16881 ) ;
#4318=CIRCLE ( 'NONE', #4644, 24.12539914357697768 ) ;
#4319=ORIENTED_EDGE ( 'NONE', *, *, #12053, .F. ) ;
#4324=VERTEX_POINT ( 'NONE', #13642 ) ;
#4328=EDGE_CURVE ( 'NONE', #11638, #16676, #10743, .T. ) ;
#4329=CARTESIAN_POINT ( 'NONE',  ( 1.039999999999996705, -20.02152543075359503, 19.67366047555523423 ) ) ;
#4337=AXIS2_PLACEMENT_3D ( 'NONE', #15887, #5272, #4070 ) ;
#4342=ORIENTED_EDGE ( 'NONE', *, *, #6423, .F. ) ;
#4345=EDGE_CURVE ( 'NONE', #6099, #2546, #7417, .T. ) ;
#4347=VERTEX_POINT ( 'NONE', #9341 ) ;
#4350=CARTESIAN_POINT ( 'NONE',  ( 2.789999999999999147, 22.25075486061738772, 9.324097380959527115 ) ) ;
#4351=EDGE_CURVE ( 'NONE', #15929, #8830, #12248, .T. ) ;
#4360=CARTESIAN_POINT ( 'NONE',  ( 1.749999999999998002, -4.633866840649122132, 27.68468304288257542 ) ) ;
#4361=EDGE_LOOP ( 'NONE', ( #16146, #10357, #7440, #4495 ) ) ;
#4367=CARTESIAN_POINT ( 'NONE',  ( 1.039999999999997593, 0.000000000000000000, 0.000000000000000000 ) ) ;
#4370=EDGE_CURVE ( 'NONE', #12759, #12346, #18780, .T. ) ;
#4371=CARTESIAN_POINT ( 'NONE',  ( 1.039999999999995373, -12.96210679857767900, -24.89775460606846380 ) ) ;
#4374=AXIS2_PLACEMENT_3D ( 'NONE', #15189, #7568, #9286 ) ;
#4379=CARTESIAN_POINT ( 'NONE',  ( 1.749999999999998002, 27.68468304288265358, -4.633866840648635410 ) ) ;
#4380=SURFACE_STYLE_FILL_AREA ( #2973 ) ;
#4382=LINE ( 'NONE', #19685, #14640 ) ;
#4388=EDGE_LOOP ( 'NONE', ( #54, #6373, #8795, #12731 ) ) ;
#4390=EDGE_CURVE ( 'NONE', #4589, #18335, #18461, .T. ) ;
#4394=DIRECTION ( 'NONE',  ( 0.000000000000000000, 0.000000000000000000, 1.000000000000000000 ) ) ;
#4398=ORIENTED_EDGE ( 'NONE', *, *, #18708, .F. ) ;
#4406=ORIENTED_EDGE ( 'NONE', *, *, #12150, .F. ) ;
#4408=FACE_OUTER_BOUND ( 'NONE', #1316, .T. ) ;
#4409=CARTESIAN_POINT ( 'NONE',  ( 2.604434261026087771, 25.39738473785002526, 5.253342437939815923 ) ) ;
#4411=ORIENTED_EDGE ( 'NONE', *, *, #2579, .F. ) ;
#4412=DIRECTION ( 'NONE',  ( 0.000000000000000000, 0.000000000000000000, 1.000000000000000000 ) ) ;
#4414=CARTESIAN_POINT ( 'NONE',  ( -5.209999999999999964, 0.000000000000000000, 0.000000000000000000 ) ) ;
#4416=ORIENTED_EDGE ( 'NONE', *, *, #13372, .F. ) ;
#4420=EDGE_CURVE ( 'NONE', #11638, #19481, #14883, .T. ) ;
#4428=AXIS2_PLACEMENT_3D ( 'NONE', #19664, #17976, #2549 ) ;
#4432=CARTESIAN_POINT ( 'NONE',  ( 2.724444381390116021, -21.84113606038314259, 12.72236714503155142 ) ) ;
#4433=ADVANCED_FACE ( 'NONE', ( #4531 ), #6317, .T. ) ;
#4439=VERTEX_POINT ( 'NONE', #14236 ) ;
#4440=CARTESIAN_POINT ( 'NONE',  ( 0.000000000000000000, 20.62201879784932856, -12.52067188844328705 ) ) ;
#4441=EDGE_CURVE ( 'NONE', #4236, #941, #6747, .T. ) ;
#4443=TOROIDAL_SURFACE ( 'NONE', #17854, 24.12539914357697413, 8.000000000000000000 ) ;
#4457=CARTESIAN_POINT ( 'NONE',  ( 1.039999999999997593, 0.000000000000000000, 0.000000000000000000 ) ) ;
#4458=EDGE_CURVE ( 'NONE', #253, #1013, #2793, .T. ) ;
#4462=CARTESIAN_POINT ( 'NONE',  ( 1.749999999999998002, -4.147968289691086774, -27.76164181293056288 ) ) ;
#4466=VERTEX_POINT ( 'NONE', #12439 ) ;
#4478=DIRECTION ( 'NONE',  ( -1.000000000000000000, 0.000000000000000000, 0.000000000000000000 ) ) ;
#4480=DIRECTION ( 'NONE',  ( -1.000000000000000000, 0.000000000000000000, 0.000000000000000000 ) ) ;
#4481=CARTESIAN_POINT ( 'NONE',  ( 0.006974663525958337516, -12.53640742967767885, 21.08118142846899801 ) ) ;
#4483=ORIENTED_EDGE ( 'NONE', *, *, #15845, .T. ) ;
#4485=DIRECTION ( 'NONE',  ( 1.000000000000000000, 0.000000000000000000, 0.000000000000000000 ) ) ;
#4493=ORIENTED_EDGE ( 'NONE', *, *, #11877, .T. ) ;
#4494=CARTESIAN_POINT ( 'NONE',  ( 0.000000000000000000, 18.28042085475278000, 15.74360496233386719 ) ) ;
#4495=ORIENTED_EDGE ( 'NONE', *, *, #3198, .F. ) ;
#4498=CARTESIAN_POINT ( 'NONE',  ( 2.789999999999999147, -7.909232158574647009, -24.34211360614308006 ) ) ;
#4505=CARTESIAN_POINT ( 'NONE',  ( 2.789999999999999147, 0.2301004812061083760, -24.44424927289185234 ) ) ;
#4506=CARTESIAN_POINT ( 'NONE',  ( 0.1855656748306453718, 25.77772010606605946, 2.851997810081739360 ) ) ;
#4509=CIRCLE ( 'NONE', #1001, 28.06981291497571362 ) ;
#4513=ORIENTED_EDGE ( 'NONE', *, *, #5448, .T. ) ;
#4516=CARTESIAN_POINT ( 'NONE',  ( 1.039999999999997371, 25.12109765559653596, 12.52377138324232675 ) ) ;
#4519=FACE_OUTER_BOUND ( 'NONE', #5574, .T. ) ;
#4523=ORIENTED_EDGE ( 'NONE', *, *, #13649, .T. ) ;
#4530=AXIS2_PLACEMENT_3D ( 'NONE', #4505, #15228, #4412 ) ;
#4531=FACE_OUTER_BOUND ( 'NONE', #3620, .T. ) ;
#4543=DIRECTION ( 'NONE',  ( 0.000000000000000000, 0.000000000000000000, 1.000000000000000000 ) ) ;
#4544=CIRCLE ( 'NONE', #13482, 2.524999999999995914 ) ;
#4549=CARTESIAN_POINT ( 'NONE',  ( 2.789999999999999147, 1.991882183130294637, 24.04302995059966364 ) ) ;
#4551=CARTESIAN_POINT ( 'NONE',  ( 2.765633920072235963, -5.391175441198450713, -24.15498966839968276 ) ) ;
#4554=CIRCLE ( 'NONE', #18298, 28.06981291497571362 ) ;
#4557=CARTESIAN_POINT ( 'NONE',  ( 2.789999999999999147, 15.74360496233381390, 18.28042085475283685 ) ) ;
#4566=ORIENTED_EDGE ( 'NONE', *, *, #4458, .F. ) ;
#4569=AXIS2_PLACEMENT_3D ( 'NONE', #4498, #13909, #8640 ) ;
#4570=CARTESIAN_POINT ( 'NONE',  ( 2.765633920072235519, 9.836394144776026138, -22.71065055754441531 ) ) ;
#4574=VECTOR ( 'NONE', #525, 1000.000000000000000 ) ;
#4575=ORIENTED_EDGE ( 'NONE', *, *, #15258, .T. ) ;
#4580=CARTESIAN_POINT ( 'NONE',  ( 2.262072625383134472, 4.996265754456739927, -26.57710921259756631 ) ) ;
#4583=AXIS2_PLACEMENT_3D ( 'NONE', #19300, #17810, #11609 ) ;
#4585=CARTESIAN_POINT ( 'NONE',  ( -7.770166132776744975E-14, -12.51293083811813389, 20.85287692521926672 ) ) ;
#4588=FACE_OUTER_BOUND ( 'NONE', #6816, .T. ) ;
#4589=VERTEX_POINT ( 'NONE', #13033 ) ;
#4594=B_SPLINE_CURVE_WITH_KNOTS ( 'NONE', 3,
 ( #10964, #12168, #12266, #18368, #3154, #3357 ),
 .UNSPECIFIED., .F., .F.,
 ( 4, 2, 4 ),
 ( 4.462636882221166670E-07, 0.001879885203074802827, 0.003759324142461383488 ),
 .UNSPECIFIED. ) ;
#4597=DIRECTION ( 'NONE',  ( -1.000000000000000000, 0.000000000000000000, 0.000000000000000000 ) ) ;
#4601=SURFACE_SIDE_STYLE ('',( #5894 ) ) ;
#4604=CYLINDRICAL_SURFACE ( 'NONE', #14396, 28.06981291497571362 ) ;
#4607=AXIS2_PLACEMENT_3D ( 'NONE', #5571, #11681, #13375 ) ;
#4608=CARTESIAN_POINT ( 'NONE',  ( 2.789999999999999147, 7.909232158575156824, -24.34211360614291664 ) ) ;
#4609=CARTESIAN_POINT ( 'NONE',  ( 1.039999999999996261, 24.89775460606850999, -12.96210679857759018 ) ) ;
#4612=CARTESIAN_POINT ( 'NONE',  ( 0.000000000000000000, 0.000000000000000000, 0.000000000000000000 ) ) ;
#4616=CYLINDRICAL_SURFACE ( 'NONE', #15853, 2.524999999999995914 ) ;
#4621=CARTESIAN_POINT ( 'NONE',  ( 0.000000000000000000, 0.000000000000000000, 0.000000000000000000 ) ) ;
#4623=EDGE_CURVE ( 'NONE', #14183, #4945, #4314, .T. ) ;
#4625=VERTEX_POINT ( 'NONE', #7699 ) ;
#4627=EDGE_LOOP ( 'NONE', ( #1062, #10444, #14744, #254 ) ) ;
#4630=CARTESIAN_POINT ( 'NONE',  ( 2.789999999999999147, 20.62201879784931435, -12.52067188844328882 ) ) ;
#4636=CARTESIAN_POINT ( 'NONE',  ( 0.02436607992776455150, 21.30679549418631780, 12.59161484032919986 ) ) ;
#4642=DIRECTION ( 'NONE',  ( -1.000000000000000000, -0.000000000000000000, -0.000000000000000000 ) ) ;
#4644=AXIS2_PLACEMENT_3D ( 'NONE', #3979, #17586, #18785 ) ;
#4647=EDGE_CURVE ( 'NONE', #1354, #8320, #8442, .T. ) ;
#4648=CIRCLE ( 'NONE', #7177, 28.06981291497571362 ) ;
#4654=ORIENTED_EDGE ( 'NONE', *, *, #14920, .F. ) ;
#4669=DIRECTION ( 'NONE',  ( 0.000000000000000000, 0.000000000000000000, 1.000000000000000000 ) ) ;
#4673=ORIENTED_EDGE ( 'NONE', *, *, #9703, .T. ) ;
#4675=DIRECTION ( 'NONE',  ( 0.000000000000000000, 0.000000000000000000, 1.000000000000000000 ) ) ;
#4676=LINE ( 'NONE', #16889, #5832 ) ;
#4691=EDGE_CURVE ( 'NONE', #2268, #1354, #5047, .T. ) ;
#4699=CARTESIAN_POINT ( 'NONE',  ( -5.209999999999999964, 0.000000000000000000, 0.000000000000000000 ) ) ;
#4700=CARTESIAN_POINT ( 'NONE',  ( 2.789999999999999147, 20.70663861606293210, -15.04425356660737556 ) ) ;
#4708=DIRECTION ( 'NONE',  ( 0.000000000000000000, 0.000000000000000000, 1.000000000000000000 ) ) ;
#4713=DIRECTION ( 'NONE',  ( 0.000000000000000000, 1.374038396813314756E-15, -1.000000000000000000 ) ) ;
#4730=DIRECTION ( 'NONE',  ( 0.000000000000000000, 0.000000000000000000, 1.000000000000000000 ) ) ;
#4732=DIRECTION ( 'NONE',  ( 0.000000000000000000, 0.8090169943749527803, -0.5877852522924655876 ) ) ;
#4737=ORIENTED_EDGE ( 'NONE', *, *, #13512, .T. ) ;
#4738=CARTESIAN_POINT ( 'NONE',  ( 1.039999999999994929, -25.12109765559662833, 12.52377138324214023 ) ) ;
#4741=ORIENTED_EDGE ( 'NONE', *, *, #8685, .F. ) ;
#4742=CARTESIAN_POINT ( 'NONE',  ( 1.749999999999998002, -27.76164181293054511, 4.147968289691195132 ) ) ;
#4745=FACE_OUTER_BOUND ( 'NONE', #10683, .T. ) ;
#4748=CARTESIAN_POINT ( 'NONE',  ( 0.006930995026450970445, 23.92277630352802831, -5.408431875071194384 ) ) ;
#4755=ORIENTED_EDGE ( 'NONE', *, *, #1859, .T. ) ;
#4758=CARTESIAN_POINT ( 'NONE',  ( 2.789999999999999147, -24.34211360614305875, 7.909232158574721616 ) ) ;
#4759=VERTEX_POINT ( 'NONE', #3604 ) ;
#4762=B_SPLINE_CURVE_WITH_KNOTS ( 'NONE', 3,
 ( #2105, #17513, #8209, #10943 ),
 .UNSPECIFIED., .F., .F.,
 ( 4, 4 ),
 ( 0.005258110598983628189, 0.005948376585272736536 ),
 .UNSPECIFIED. ) ;
#4766=CARTESIAN_POINT ( 'NONE',  ( 2.030753610301984313, -19.12676442129359700, 19.86438386685654578 ) ) ;
#4767=VECTOR ( 'NONE', #14064, 1000.000000000000000 ) ;
#4774=EDGE_CURVE ( 'NONE', #1756, #1726, #3408, .T. ) ;
#4780=ADVANCED_FACE ( 'NONE', ( #5095 ), #6486, .F. ) ;
#4782=EDGE_LOOP ( 'NONE', ( #16624, #12568, #13843, #8332 ) ) ;
#4783=CARTESIAN_POINT ( 'NONE',  ( 2.789999999999999147, -25.59481291497571220, -1.787276233276378314E-13 ) ) ;
#4784=EDGE_CURVE ( 'NONE', #2358, #15929, #3893, .T. ) ;
#4785=CARTESIAN_POINT ( 'NONE',  ( 0.02436607992775717893, -9.836394144775869819, 22.71065055754449347 ) ) ;
#4790=AXIS2_PLACEMENT_3D ( 'NONE', #17034, #3324, #4011 ) ;
#4792=CARTESIAN_POINT ( 'NONE',  ( 0.1882238946918236844, 2.857713464478689680, 25.78859396478529220 ) ) ;
#4795=CARTESIAN_POINT ( 'NONE',  ( 2.789999999999999147, 7.772527002114431482, 23.17675759782044054 ) ) ;
#4796=CARTESIAN_POINT ( 'NONE',  ( 2.789999999999999147, -7.772527002114268058, -23.17675759782048672 ) ) ;
#4797=DIRECTION ( 'NONE',  ( -1.000000000000000000, -0.000000000000000000, -0.000000000000000000 ) ) ;
#4801=EDGE_CURVE ( 'NONE', #303, #18102, #14958, .T. ) ;
#4804=DIRECTION ( 'NONE',  ( -1.000000000000000000, -0.000000000000000000, 0.000000000000000000 ) ) ;
#4805=EDGE_LOOP ( 'NONE', ( #1529, #9332, #15350, #238, #18701, #12314, #1992, #7348 ) ) ;
#4806=DIRECTION ( 'NONE',  ( 0.000000000000000000, 0.000000000000000000, -1.000000000000000000 ) ) ;
#4809=AXIS2_PLACEMENT_3D ( 'NONE', #19089, #2285, #17498 ) ;
#4811=DIRECTION ( 'NONE',  ( 0.000000000000000000, 0.000000000000000000, 1.000000000000000000 ) ) ;
#4812=CARTESIAN_POINT ( 'NONE',  ( 2.765633920072236407, -2.336989772644440855, 24.63872515616082026 ) ) ;
#4815=EDGE_CURVE ( 'NONE', #5246, #16591, #5990, .T. ) ;
#4819=CARTESIAN_POINT ( 'NONE',  ( 1.394999999999998685, 24.89775460606851354, -12.96210679857759374 ) ) ;
#4826=ORIENTED_EDGE ( 'NONE', *, *, #16536, .T. ) ;
#4827=CARTESIAN_POINT ( 'NONE',  ( 1.749999999999998002, -4.633866840649122132, 27.68468304288257542 ) ) ;
#4835=ORIENTED_EDGE ( 'NONE', *, *, #429, .T. ) ;
#4837=CARTESIAN_POINT ( 'NONE',  ( 1.394999999999998685, 12.96210679857822434, -24.89775460606818314 ) ) ;
#4839=B_SPLINE_CURVE_WITH_KNOTS ( 'NONE', 3,
 ( #19498, #5988, #18213, #11706 ),
 .UNSPECIFIED., .F., .F.,
 ( 4, 4 ),
 ( 0.005258120783916782857, 0.005948386350302925507 ),
 .UNSPECIFIED. ) ;
#4841=CARTESIAN_POINT ( 'NONE',  ( 2.257825491203657275, 11.58891744060141882, -24.44564404695831783 ) ) ;
#4845=TOROIDAL_SURFACE ( 'NONE', #18582, 24.12539914357697768, 8.000000000000000000 ) ;
#4846=ORIENTED_EDGE ( 'NONE', *, *, #8935, .T. ) ;
#4848=CIRCLE ( 'NONE', #16039, 2.524999999999996358 ) ;
#4851=DIRECTION ( 'NONE',  ( 0.000000000000000000, 0.000000000000000000, 1.000000000000000000 ) ) ;
#4861=ORIENTED_EDGE ( 'NONE', *, *, #7903, .T. ) ;
#4864=CARTESIAN_POINT ( 'NONE',  ( 1.749999999999998002, 4.633866840649310426, -27.68468304288254345 ) ) ;
#4869=CARTESIAN_POINT ( 'NONE',  ( 2.789999999999999147, 7.909232158575156824, -24.34211360614291664 ) ) ;
#4870=DIRECTION ( 'NONE',  ( 0.000000000000000000, 0.000000000000000000, 1.000000000000000000 ) ) ;
#4871=ADVANCED_FACE ( 'NONE', ( #899 ), #5394, .T. ) ;
#4873=EDGE_LOOP ( 'NONE', ( #15756, #17891, #6436, #7641 ) ) ;
#4878=VECTOR ( 'NONE', #14282, 1000.000000000000000 ) ;
#4887=ORIENTED_EDGE ( 'NONE', *, *, #4441, .F. ) ;
#4893=DIRECTION ( 'NONE',  ( -1.000000000000000000, 0.000000000000000000, -0.000000000000000000 ) ) ;
#4899=EDGE_CURVE ( 'NONE', #15823, #16071, #17260, .T. ) ;
#4901=CYLINDRICAL_SURFACE ( 'NONE', #974, 28.06981291497571362 ) ;
#4908=CARTESIAN_POINT ( 'NONE',  ( 2.789999999999999147, -7.909232158574647009, -24.34211360614308006 ) ) ;
#4913=AXIS2_PLACEMENT_3D ( 'NONE', #18016, #10411, #13500 ) ;
#4920=CARTESIAN_POINT ( 'NONE',  ( 0.02436607992776064838, 18.55949924794892780, 16.37294372382865504 ) ) ;
#4923=ORIENTED_EDGE ( 'NONE', *, *, #4002, .T. ) ;
#4924=DIRECTION ( 'NONE',  ( 1.000000000000000000, 0.000000000000000000, 0.000000000000000000 ) ) ;
#4925=ORIENTED_EDGE ( 'NONE', *, *, #9855, .F. ) ;
#4931=FACE_OUTER_BOUND ( 'NONE', #4155, .T. ) ;
#4933=ORIENTED_EDGE ( 'NONE', *, *, #16337, .T. ) ;
#4936=CYLINDRICAL_SURFACE ( 'NONE', #17124, 13.19999999999999929 ) ;
#4938=ORIENTED_EDGE ( 'NONE', *, *, #10668, .F. ) ;
#4939=EDGE_CURVE ( 'NONE', #4625, #16863, #18916, .T. ) ;
#4942=AXIS2_PLACEMENT_3D ( 'NONE', #6397, #11026, #15628 ) ;
#4943=DIRECTION ( 'NONE',  ( -1.000000000000000000, -0.000000000000000000, -0.000000000000000000 ) ) ;
#4945=VERTEX_POINT ( 'NONE', #8991 ) ;
#4946=CARTESIAN_POINT ( 'NONE',  ( 2.765633920072235519, 9.836394144776026138, -22.71065055754441531 ) ) ;
#4947=DIRECTION ( 'NONE',  ( 0.000000000000000000, 0.000000000000000000, 1.000000000000000000 ) ) ;
#4950=CIRCLE ( 'NONE', #12308, 2.524999999999995914 ) ;
#4955=EDGE_LOOP ( 'NONE', ( #12532, #11050, #5310, #8738, #4031, #13475 ) ) ;
#4957=CARTESIAN_POINT ( 'NONE',  ( 1.039999999999997815, 27.68468304288265003, -4.633866840648637186 ) ) ;
#4962=AXIS2_PLACEMENT_3D ( 'NONE', #15987, #2277, #9995 ) ;
#4964=B_SPLINE_CURVE_WITH_KNOTS ( 'NONE', 3,
 ( #82, #10887, #6173, #16992, #18198, #12293, #18390, #16896 ),
 .UNSPECIFIED., .F., .F.,
 ( 4, 2, 2, 4 ),
 ( 2.032124546189621919E-07, 0.001631739532304474910, 0.002447507692229407717, 0.003263275852154340524 ),
 .UNSPECIFIED. ) ;
#4966=CARTESIAN_POINT ( 'NONE',  ( 0.000000000000000000, -22.25075486061745167, 9.324097380959385006 ) ) ;
#4967=DIRECTION ( 'NONE',  ( 0.000000000000000000, 0.000000000000000000, 1.000000000000000000 ) ) ;
#4970=DIRECTION ( 'NONE',  ( 0.000000000000000000, 0.000000000000000000, 1.000000000000000000 ) ) ;
#4971=ORIENTED_EDGE ( 'NONE', *, *, #3667, .F. ) ;
#4973=CARTESIAN_POINT ( 'NONE',  ( 2.765633920072238627, 12.59161484032942901, -21.30679549418617924 ) ) ;
#4983=CARTESIAN_POINT ( 'NONE',  ( 0.7592463896980057303, -19.86438386685674473, 19.12676442129336252 ) ) ;
#4985=CIRCLE ( 'NONE', #8819, 2.524999999999995914 ) ;
#4989=EDGE_LOOP ( 'NONE', ( #17391, #1926, #7296, #1259 ) ) ;
#5003=CARTESIAN_POINT ( 'NONE',  ( 1.039999999999996927, -4.633866840649124796, 27.68468304288256832 ) ) ;
#5005=VERTEX_POINT ( 'NONE', #11795 ) ;
#5007=CARTESIAN_POINT ( 'NONE',  ( 0.000000000000000000, -9.324097380959319281, -22.25075486061748009 ) ) ;
#5017=EDGE_LOOP ( 'NONE', ( #8620, #6425 ) ) ;
#5018=CARTESIAN_POINT ( 'NONE',  ( 2.789999999999999147, -21.30679549418640306, 12.59161484032904887 ) ) ;
#5019=ORIENTED_EDGE ( 'NONE', *, *, #8596, .F. ) ;
#5025=FACE_OUTER_BOUND ( 'NONE', #9853, .T. ) ;
#5029=DIRECTION ( 'NONE',  ( 0.000000000000000000, 0.000000000000000000, 1.000000000000000000 ) ) ;
#5031=AXIS2_PLACEMENT_3D ( 'NONE', #19503, #10612, #3495 ) ;
#5037=ORIENTED_EDGE ( 'NONE', *, *, #1023, .F. ) ;
#5047=CIRCLE ( 'NONE', #7590, 2.524999999999997247 ) ;
#5048=DIRECTION ( 'NONE',  ( -1.000000000000000000, 0.000000000000000000, 0.000000000000000000 ) ) ;
#5049=ORIENTED_EDGE ( 'NONE', *, *, #16386, .F. ) ;
#5057=ORIENTED_EDGE ( 'NONE', *, *, #7968, .F. ) ;
#5059=EDGE_CURVE ( 'NONE', #18433, #4625, #11976, .T. ) ;
#5064=( NAMED_UNIT ( * ) SI_UNIT ( $, .STERADIAN. ) SOLID_ANGLE_UNIT ( ) );
#5066=ORIENTED_EDGE ( 'NONE', *, *, #9538, .F. ) ;
#5072=ORIENTED_EDGE ( 'NONE', *, *, #8647, .F. ) ;
#5081=CARTESIAN_POINT ( 'NONE',  ( 0.006931054464085539824, -24.42321038836781355, -2.248820353273226491 ) ) ;
#5083=CARTESIAN_POINT ( 'NONE',  ( -10.00000000000000000, 0.000000000000000000, 0.000000000000000000 ) ) ;
#5087=DIRECTION ( 'NONE',  ( -1.000000000000000000, -0.000000000000000000, -0.000000000000000000 ) ) ;
#5089=CARTESIAN_POINT ( 'NONE',  ( 0.000000000000000000, -12.52067188844364587, 20.62201879784910119 ) ) ;
#5095=FACE_OUTER_BOUND ( 'NONE', #15594, .T. ) ;
#5104=DIRECTION ( 'NONE',  ( 0.000000000000000000, 0.3090169943749544457, -0.9510565162951513107 ) ) ;
#5106=ORIENTED_EDGE ( 'NONE', *, *, #13821, .T. ) ;
#5113=AXIS2_PLACEMENT_3D ( 'NONE', #2019, #125, #13930 ) ;
#5114=CARTESIAN_POINT ( 'NONE',  ( 2.262072625383133140, -4.996265754456554298, 26.57710921259759829 ) ) ;
#5116=CARTESIAN_POINT ( 'NONE',  ( 1.039999999999995373, 12.96210679857822434, -24.89775460606817958 ) ) ;
#5117=CARTESIAN_POINT ( 'NONE',  ( 2.765633920072234631, 16.37294372382885044, -18.55949924794875017 ) ) ;
#5123=AXIS2_PLACEMENT_3D ( 'NONE', #191, #6563, #287 ) ;
#5127=EDGE_CURVE ( 'NONE', #10762, #11999, #8571, .T. ) ;
#5139=ORIENTED_EDGE ( 'NONE', *, *, #465, .F. ) ;
#5142=CARTESIAN_POINT ( 'NONE',  ( 1.394999999999999574, -20.02152543075359858, 19.67366047555523778 ) ) ;
#5144=DIRECTION ( 'NONE',  ( -1.000000000000000000, -0.000000000000000000, -0.000000000000000000 ) ) ;
#5155=B_SPLINE_CURVE_WITH_KNOTS ( 'NONE', 3,
 ( #10368, #9259, #13657, #6041 ),
 .UNSPECIFIED., .F., .F.,
 ( 4, 4 ),
 ( 1.981826382900847025E-07, 0.0006887856082032273912 ),
 .UNSPECIFIED. ) ;
#5156=DIRECTION ( 'NONE',  ( -1.000000000000000000, -0.000000000000000000, -0.000000000000000000 ) ) ;
#5159=EDGE_CURVE ( 'NONE', #6823, #15675, #13641, .T. ) ;
#5162=EDGE_CURVE ( 'NONE', #13659, #12561, #6554, .T. ) ;
#5174=CARTESIAN_POINT ( 'NONE',  ( 2.789999999999999147, 24.04302995059966364, 1.991882183130384121 ) ) ;
#5178=CARTESIAN_POINT ( 'NONE',  ( 0.02436607992776021470, 21.30679549418649543, -12.59161484032888723 ) ) ;
#5181=DIRECTION ( 'NONE',  ( -1.000000000000000000, -0.000000000000000000, -0.000000000000000000 ) ) ;
#5194=CYLINDRICAL_SURFACE ( 'NONE', #14475, 2.524999999999995914 ) ;
#5199=CARTESIAN_POINT ( 'NONE',  ( 0.07181523211952839381, -10.24584646439522828, -23.19431517146944088 ) ) ;
#5201=ORIENTED_EDGE ( 'NONE', *, *, #17761, .F. ) ;
#5208=CARTESIAN_POINT ( 'NONE',  ( 2.604434404052932805, -19.17825124759790256, 17.45907811351449368 ) ) ;
#5212=CARTESIAN_POINT ( 'NONE',  ( 1.039999999999997593, 0.000000000000000000, 0.000000000000000000 ) ) ;
#5217=ORIENTED_EDGE ( 'NONE', *, *, #456, .T. ) ;
#5218=EDGE_CURVE ( 'NONE', #1741, #1756, #9140, .T. ) ;
#5228=ORIENTED_EDGE ( 'NONE', *, *, #2168, .T. ) ;
#5241=B_SPLINE_CURVE_WITH_KNOTS ( 'NONE', 3,
 ( #605, #7043, #19265, #19363 ),
 .UNSPECIFIED., .F., .F.,
 ( 4, 4 ),
 ( 0.005258105385878670927, 0.005948373736081390140 ),
 .UNSPECIFIED. ) ;
#5246=VERTEX_POINT ( 'NONE', #14874 ) ;
#5251=B_SPLINE_CURVE_WITH_KNOTS ( 'NONE', 3,
 ( #7450, #4272, #16581, #15076, #14879, #4371 ),
 .UNSPECIFIED., .F., .F.,
 ( 4, 2, 4 ),
 ( 2.032124546189808531E-07, 0.001878594002992309232, 0.003756984793529999193 ),
 .UNSPECIFIED. ) ;
#5252=EDGE_CURVE ( 'NONE', #1773, #1219, #7671, .T. ) ;
#5266=EDGE_LOOP ( 'NONE', ( #13863, #18635, #119, #5476, #13025, #15939 ) ) ;
#5270=DIRECTION ( 'NONE',  ( 0.000000000000000000, 0.000000000000000000, 1.000000000000000000 ) ) ;
#5272=DIRECTION ( 'NONE',  ( -1.000000000000000000, -0.000000000000000000, -0.000000000000000000 ) ) ;
#5275=B_SPLINE_CURVE_WITH_KNOTS ( 'NONE', 3,
 ( #2769, #8885, #7357, #19581 ),
 .UNSPECIFIED., .F., .F.,
 ( 4, 4 ),
 ( 2.324263106244697256E-07, 0.0006888201370294697295 ),
 .UNSPECIFIED. ) ;
#5276=FACE_OUTER_BOUND ( 'NONE', #2813, .T. ) ;
#5277=ORIENTED_EDGE ( 'NONE', *, *, #15502, .T. ) ;
#5282=CARTESIAN_POINT ( 'NONE',  ( 1.039999999999996705, -20.02152543075331081, -19.67366047555552555 ) ) ;
#5289=VECTOR ( 'NONE', #12940, 1000.000000000000000 ) ;
#5291=VERTEX_POINT ( 'NONE', #2957 ) ;
#5293=CARTESIAN_POINT ( 'NONE',  ( 2.789999999999999147, 23.31896751603331808, 7.334849878007589474 ) ) ;
#5301=ORIENTED_EDGE ( 'NONE', *, *, #13494, .T. ) ;
#5310=ORIENTED_EDGE ( 'NONE', *, *, #4026, .F. ) ;
#5314=CARTESIAN_POINT ( 'NONE',  ( 0.02436607992775978102, -12.59161484032896361, -21.30679549418645280 ) ) ;
#5319=CARTESIAN_POINT ( 'NONE',  ( 0.7589665089996477931, -12.05173163741739906, 24.80232951178374279 ) ) ;
#5322=DIRECTION ( 'NONE',  ( 0.000000000000000000, 0.000000000000000000, 1.000000000000000000 ) ) ;
#5331=DIRECTION ( 'NONE',  ( 0.000000000000000000, 0.000000000000000000, 1.000000000000000000 ) ) ;
#5334=CARTESIAN_POINT ( 'NONE',  ( 0.07186814640506890284, 21.92302674874982316, -12.74240566898960303 ) ) ;
#5338=CARTESIAN_POINT ( 'NONE',  ( 0.07186811453410731076, 16.91241718342026346, -18.89333555428536826 ) ) ;
#5352=ORIENTED_EDGE ( 'NONE', *, *, #12479, .T. ) ;
#5358=EDGE_CURVE ( 'NONE', #10744, #725, #5923, .T. ) ;
#5362=VERTEX_POINT ( 'NONE', #2225 ) ;
#5363=VERTEX_POINT ( 'NONE', #14338 ) ;
#5365=EDGE_CURVE ( 'NONE', #9369, #13000, #13922, .T. ) ;
#5366=CARTESIAN_POINT ( 'NONE',  ( 2.789999999999999147, -5.535312321042889394, 23.48180575137727999 ) ) ;
#5367=CARTESIAN_POINT ( 'NONE',  ( 0.5321745379877897975, -12.96514671151783915, 23.74442027961355706 ) ) ;
#5371=CARTESIAN_POINT ( 'NONE',  ( -5.209999999999999964, 0.000000000000000000, 0.000000000000000000 ) ) ;
#5373=LINE ( 'NONE', #3678, #1449 ) ;
#5375=CARTESIAN_POINT ( 'NONE',  ( 0.009068833172775131110, 21.10834851580723992, -12.54305517365597922 ) ) ;
#5376=ADVANCED_FACE ( 'NONE', ( #17340 ), #4936, .T. ) ;
#5382=FACE_OUTER_BOUND ( 'NONE', #53, .T. ) ;
#5386=EDGE_CURVE ( 'NONE', #15383, #17455, #17444, .T. ) ;
#5394=CYLINDRICAL_SURFACE ( 'NONE', #11456, 13.19999999999999574 ) ;
#5398=AXIS2_PLACEMENT_3D ( 'NONE', #460, #8254, #17259 ) ;
#5403=DIRECTION ( 'NONE',  ( -1.000000000000000000, -0.000000000000000000, -0.000000000000000000 ) ) ;
#5404=CYLINDRICAL_SURFACE ( 'NONE', #7449, 28.06981291497571362 ) ;
#5407=EDGE_CURVE ( 'NONE', #6719, #18587, #14240, .T. ) ;
#5408=CARTESIAN_POINT ( 'NONE',  ( 2.789999999999999147, 23.17675759782041212, -7.772527002114516748 ) ) ;
#5414=CARTESIAN_POINT ( 'NONE',  ( 2.604434514863827488, 23.63475234378997314, -10.67816411292140444 ) ) ;
#5425=EDGE_CURVE ( 'NONE', #1354, #18489, #1141, .T. ) ;
#5447=CARTESIAN_POINT ( 'NONE',  ( 50.00050000000000239, 0.000000000000000000, 0.000000000000000000 ) ) ;
#5448=EDGE_CURVE ( 'NONE', #1013, #6790, #3855, .T. ) ;
#5456=ORIENTED_EDGE ( 'NONE', *, *, #15321, .T. ) ;
#5459=EDGE_CURVE ( 'NONE', #2358, #16588, #18639, .T. ) ;
#5467=CARTESIAN_POINT ( 'NONE',  ( 2.789999999999999147, -1.991882183130126549, -24.04302995059967429 ) ) ;
#5471=CARTESIAN_POINT ( 'NONE',  ( 2.604434514863827488, -10.67816411292148793, -23.63475234378993761 ) ) ;
#5476=ORIENTED_EDGE ( 'NONE', *, *, #2405, .F. ) ;
#5478=AXIS2_PLACEMENT_3D ( 'NONE', #14736, #14930, #6918 ) ;
#5484=EDGE_CURVE ( 'NONE', #15829, #10318, #4648, .T. ) ;
#5488=EDGE_CURVE ( 'NONE', #3927, #2850, #18389, .T. ) ;
#5498=FACE_OUTER_BOUND ( 'NONE', #19520, .T. ) ;
#5502=FACE_OUTER_BOUND ( 'NONE', #4873, .T. ) ;
#5505=ORIENTED_EDGE ( 'NONE', *, *, #8932, .F. ) ;
#5510=DIRECTION ( 'NONE',  ( -1.000000000000000000, 0.000000000000000000, -0.000000000000000000 ) ) ;
#5515=CARTESIAN_POINT ( 'NONE',  ( -1.381028087215756681E-16, 24.22479935914660132, 2.133490293297101381 ) ) ;
#5523=EDGE_CURVE ( 'NONE', #17548, #4589, #2418, .T. ) ;
#5534=AXIS2_PLACEMENT_3D ( 'NONE', #11790, #2673, #8590 ) ;
#5550=CARTESIAN_POINT ( 'NONE',  ( -10.00000000000000000, 0.000000000000000000, 0.000000000000000000 ) ) ;
#5552=CIRCLE ( 'NONE', #10678, 2.524999999999994582 ) ;
#5555=ORIENTED_EDGE ( 'NONE', *, *, #17208, .F. ) ;
#5560=B_SPLINE_CURVE_WITH_KNOTS ( 'NONE', 3,
 ( #11836, #16544, #4234, #8839, #14939, #5819 ),
 .UNSPECIFIED., .F., .F.,
 ( 4, 2, 4 ),
 ( 2.132675795045741476E-07, 0.001878604073277002386, 0.003756994878974500435 ),
 .UNSPECIFIED. ) ;
#5567=CARTESIAN_POINT ( 'NONE',  ( 2.783069004973548033, 23.92277630352795370, 5.408431875071527450 ) ) ;
#5568=VECTOR ( 'NONE', #9305, 1000.000000000000000 ) ;
#5569=CARTESIAN_POINT ( 'NONE',  ( 0.000000000000000000, 22.25075486061737351, 9.324097380959511128 ) ) ;
#5571=CARTESIAN_POINT ( 'NONE',  ( 1.749999999999998002, 0.000000000000000000, 0.000000000000000000 ) ) ;
#5572=DIRECTION ( 'NONE',  ( 0.000000000000000000, 0.000000000000000000, 1.000000000000000000 ) ) ;
#5574=EDGE_LOOP ( 'NONE', ( #10929, #3293, #14898, #3721 ) ) ;
#5576=DIRECTION ( 'NONE',  ( 0.000000000000000000, 0.000000000000000000, 1.000000000000000000 ) ) ;
#5577=B_SPLINE_CURVE_WITH_KNOTS ( 'NONE', 3,
 ( #8615, #2316, #14537, #4112 ),
 .UNSPECIFIED., .F., .F.,
 ( 4, 4 ),
 ( 2.034713381942770033E-07, 0.0006887909409525396235 ),
 .UNSPECIFIED. ) ;
#5581=DIRECTION ( 'NONE',  ( -1.000000000000000000, 0.000000000000000000, 0.000000000000000000 ) ) ;
#5583=ORIENTED_EDGE ( 'NONE', *, *, #18026, .T. ) ;
#5584=LINE ( 'NONE', #15098, #9323 ) ;
#5585=DIRECTION ( 'NONE',  ( 0.000000000000000000, 2.061057595219972332E-15, -1.000000000000000000 ) ) ;
#5586=ORIENTED_EDGE ( 'NONE', *, *, #14020, .T. ) ;
#5588=DIRECTION ( 'NONE',  ( 0.000000000000000000, 0.000000000000000000, 1.000000000000000000 ) ) ;
#5592=ORIENTED_EDGE ( 'NONE', *, *, #11944, .F. ) ;
#5595=DIRECTION ( 'NONE',  ( -1.000000000000000000, -0.000000000000000000, -0.000000000000000000 ) ) ;
#5604=TOROIDAL_SURFACE ( 'NONE', #1775, 24.12539914357697768, 8.000000000000000000 ) ;
#5606=EDGE_CURVE ( 'NONE', #10821, #5291, #12023, .T. ) ;
#5608=ORIENTED_EDGE ( 'NONE', *, *, #4458, .T. ) ;
#5611=ORIENTED_EDGE ( 'NONE', *, *, #15175, .F. ) ;
#5613=CARTESIAN_POINT ( 'NONE',  ( 0.02436607992776368414, 18.55949924794916228, -16.37294372382838148 ) ) ;
#5619=AXIS2_PLACEMENT_3D ( 'NONE', #4414, #19718, #15327 ) ;
#5622=CARTESIAN_POINT ( 'NONE',  ( 2.765633920072235519, 24.15498966839970052, -5.391175441198366336 ) ) ;
#5626=DIRECTION ( 'NONE',  ( -1.000000000000000000, -0.000000000000000000, -0.000000000000000000 ) ) ;
#5627=CYLINDRICAL_SURFACE ( 'NONE', #6670, 2.524999999999996358 ) ;
#5637=CIRCLE ( 'NONE', #16838, 28.06981291497571362 ) ;
#5640=B_SPLINE_CURVE_WITH_KNOTS ( 'NONE', 3,
 ( #13755, #6597, #16862, #621 ),
 .UNSPECIFIED., .F., .F.,
 ( 4, 4 ),
 ( 2.135345996175604595E-07, 0.0006888010880210905865 ),
 .UNSPECIFIED. ) ;
#5642=DIRECTION ( 'NONE',  ( 0.000000000000000000, 0.000000000000000000, 1.000000000000000000 ) ) ;
#5644=CARTESIAN_POINT ( 'NONE',  ( 2.789999999999999147, -15.04425356660774682, 20.70663861606266209 ) ) ;
#5647=CARTESIAN_POINT ( 'NONE',  ( 0.000000000000000000, -18.28042085475288303, 15.74360496233377305 ) ) ;
#5656=VERTEX_POINT ( 'NONE', #10819 ) ;
#5659=EDGE_LOOP ( 'NONE', ( #8614, #5583, #1587, #9564 ) ) ;
#5663=EDGE_LOOP ( 'NONE', ( #15210, #15689, #11315, #17278, #18478, #14582, #11414, #10463 ) ) ;
#5665=AXIS2_PLACEMENT_3D ( 'NONE', #14305, #5749, #2551 ) ;
#5669=CARTESIAN_POINT ( 'NONE',  ( 1.749999999999998002, 0.000000000000000000, 0.000000000000000000 ) ) ;
#5670=CARTESIAN_POINT ( 'NONE',  ( 2.790000000000077307, 20.65026423218591844, -12.51972477286559027 ) ) ;
#5672=VERTEX_POINT ( 'NONE', #8921 ) ;
#5673=CARTESIAN_POINT ( 'NONE',  ( 2.789999999999999147, 0.000000000000000000, 0.000000000000000000 ) ) ;
#5675=LINE ( 'NONE', #3791, #8417 ) ;
#5685=ADVANCED_FACE ( 'NONE', ( #7703 ), #4616, .F. ) ;
#5688=CARTESIAN_POINT ( 'NONE',  ( 1.039999999999995817, 27.76164181293051669, 4.147968289691385202 ) ) ;
#5689=CARTESIAN_POINT ( 'NONE',  ( 2.789999999999999147, 24.44424927289185945, 12.96989951879416125 ) ) ;
#5692=DIRECTION ( 'NONE',  ( 0.000000000000000000, 0.000000000000000000, 1.000000000000000000 ) ) ;
#5693=ADVANCED_FACE ( 'NONE', ( #7807 ), #16623, .T. ) ;
#5701=TOROIDAL_SURFACE ( 'NONE', #15633, 24.12539914357697413, 8.000000000000000000 ) ;
#5702=ADVANCED_FACE ( 'NONE', ( #15229 ), #11701, .T. ) ;
#5707=ORIENTED_EDGE ( 'NONE', *, *, #8237, .T. ) ;
#5724=DIRECTION ( 'NONE',  ( 0.000000000000000000, 0.000000000000000000, 1.000000000000000000 ) ) ;
#5730=EDGE_CURVE ( 'NONE', #7686, #18594, #14138, .T. ) ;
#5736=EDGE_CURVE ( 'NONE', #479, #15528, #4985, .T. ) ;
#5746=ORIENTED_EDGE ( 'NONE', *, *, #378, .T. ) ;
#5748=VECTOR ( 'NONE', #15490, 1000.000000000000000 ) ;
#5749=DIRECTION ( 'NONE',  ( 1.000000000000000000, 0.000000000000000000, 0.000000000000000000 ) ) ;
#5755=DIRECTION ( 'NONE',  ( -1.000000000000000000, -0.000000000000000000, 0.000000000000000000 ) ) ;
#5765=CARTESIAN_POINT ( 'NONE',  ( -10.00000000000000000, 0.000000000000000000, 0.000000000000000000 ) ) ;
#5768=CARTESIAN_POINT ( 'NONE',  ( 1.749999999999998002, 27.68468304288259318, 4.633866840649019103 ) ) ;
#5774=AXIS2_PLACEMENT_3D ( 'NONE', #13650, #7530, #7832 ) ;
#5784=CARTESIAN_POINT ( 'NONE',  ( 2.789999999999999147, 9.324097380959445402, 22.25075486061742325 ) ) ;
#5792=CARTESIAN_POINT ( 'NONE',  ( 0.02436607992776064838, 12.59161484032912171, 21.30679549418635688 ) ) ;
#5797=EDGE_CURVE ( 'NONE', #2850, #7268, #17930, .T. ) ;
#5816=ORIENTED_EDGE ( 'NONE', *, *, #8190, .T. ) ;
#5819=CARTESIAN_POINT ( 'NONE',  ( 1.039999999999995817, -27.76164181293048472, -4.147968289691575272 ) ) ;
#5829=B_SPLINE_CURVE_WITH_KNOTS ( 'NONE', 3,
 ( #8547, #2432, #1038, #8456, #17460, #19240 ),
 .UNSPECIFIED., .F., .F.,
 ( 4, 2, 4 ),
 ( 4.462636882155291330E-07, 0.001879885203074804561, 0.003759324142461393896 ),
 .UNSPECIFIED. ) ;
#5832=VECTOR ( 'NONE', #3171, 1000.000000000000000 ) ;
#5835=CARTESIAN_POINT ( 'NONE',  ( 2.030753605846573606, -3.797885586973408056, 27.31305418910209326 ) ) ;
#5836=VERTEX_POINT ( 'NONE', #14416 ) ;
#5845=CARTESIAN_POINT ( 'NONE',  ( 2.789999999999999591, 2.133490293297010343, 24.22479935914660132 ) ) ;
#5849=ADVANCED_FACE ( 'NONE', ( #12620 ), #6390, .T. ) ;
#5854=VERTEX_POINT ( 'NONE', #6296 ) ;
#5862=B_SPLINE_CURVE_WITH_KNOTS ( 'NONE', 3,
 ( #7080, #2493, #17425, #4007 ),
 .UNSPECIFIED., .F., .F.,
 ( 4, 4 ),
 ( 3.059063720746937335E-07, 0.0006888942284914101538 ),
 .UNSPECIFIED. ) ;
#5872=ORIENTED_EDGE ( 'NONE', *, *, #13403, .T. ) ;
#5875=LINE ( 'NONE', #10495, #7557 ) ;
#5880=ORIENTED_EDGE ( 'NONE', *, *, #5386, .T. ) ;
#5881=CARTESIAN_POINT ( 'NONE',  ( 1.039999999999996927, -25.12109765559644714, -12.52377138324250438 ) ) ;
#5883=CYLINDRICAL_SURFACE ( 'NONE', #12992, 28.06981291497571362 ) ;
#5884=ORIENTED_EDGE ( 'NONE', *, *, #17932, .F. ) ;
#5888=CARTESIAN_POINT ( 'NONE',  ( 2.789999999999999147, -5.535312321042889394, 23.48180575137727999 ) ) ;
#5891=VERTEX_POINT ( 'NONE', #5007 ) ;
#5894=SURFACE_STYLE_FILL_AREA ( #12206 ) ;
#5900=EDGE_CURVE ( 'NONE', #1741, #13180, #2639, .T. ) ;
#5912=CARTESIAN_POINT ( 'NONE',  ( 2.031033471609898555, 27.31260702007175567, -3.797536611356413516 ) ) ;
#5914=CARTESIAN_POINT ( 'NONE',  ( 2.765633920072238183, -18.55949924794904504, 16.37294372382852004 ) ) ;
#5917=CARTESIAN_POINT ( 'NONE',  ( 2.765633920072235963, -24.63872515616080960, -2.336989772644527008 ) ) ;
#5918=ORIENTED_EDGE ( 'NONE', *, *, #14122, .T. ) ;
#5922=CARTESIAN_POINT ( 'NONE',  ( 0.1882238552569850676, 23.64332819722396195, -10.68696068830383084 ) ) ;
#5923=CIRCLE ( 'NONE', #4021, 2.524999999999998135 ) ;
#5927=CARTESIAN_POINT ( 'NONE',  ( 2.262072706628475149, 19.66369668717060293, -18.56460150496918260 ) ) ;
#5932=VERTEX_POINT ( 'NONE', #11014 ) ;
#5934=CARTESIAN_POINT ( 'NONE',  ( 0.1882238552569851786, -23.64332819722389090, 10.68696068830398360 ) ) ;
#5936=B_SPLINE_CURVE_WITH_KNOTS ( 'NONE', 3,
 ( #1802, #17112, #3303, #10812 ),
 .UNSPECIFIED., .F., .F.,
 ( 4, 4 ),
 ( 0.005258139959819257275, 0.005342776758202955750 ),
 .UNSPECIFIED. ) ;
#5937=VERTEX_POINT ( 'NONE', #12813 ) ;
#5940=CARTESIAN_POINT ( 'NONE',  ( 0.000000000000000000, 0.000000000000000000, 0.000000000000000000 ) ) ;
#5941=ORIENTED_EDGE ( 'NONE', *, *, #3034, .T. ) ;
#5956=DIRECTION ( 'NONE',  ( 0.000000000000000000, 0.000000000000000000, -1.000000000000000000 ) ) ;
#5958=AXIS2_PLACEMENT_3D ( 'NONE', #9086, #16887, #6351 ) ;
#5965=VERTEX_POINT ( 'NONE', #11213 ) ;
#5968=PRODUCT_DEFINITION_CONTEXT ( 'detailed design', #16983, 'design' ) ;
#5970=B_SPLINE_CURVE_WITH_KNOTS ( 'NONE', 3,
 ( #1850, #7941, #3150, #15366, #14051, #7748 ),
 .UNSPECIFIED., .F., .F.,
 ( 4, 2, 4 ),
 ( 2.032124546189621919E-07, 0.001878594002992312268, 0.003756984793530005265 ),
 .UNSPECIFIED. ) ;
#5971=CARTESIAN_POINT ( 'NONE',  ( 2.789999999999999147, -9.836394144775869819, 22.71065055754449347 ) ) ;
#5980=EDGE_CURVE ( 'NONE', #17548, #19081, #1699, .T. ) ;
#5982=EDGE_CURVE ( 'NONE', #19487, #14187, #16264, .T. ) ;
#5984=FACE_OUTER_BOUND ( 'NONE', #14049, .T. ) ;
#5988=CARTESIAN_POINT ( 'NONE',  ( 2.790000000000000036, 24.22479935914659777, -2.133490293297098273 ) ) ;
#5990=CIRCLE ( 'NONE', #17187, 24.12539914357697768 ) ;
#5994=DIRECTION ( 'NONE',  ( -1.000000000000000000, 0.000000000000000000, -0.000000000000000000 ) ) ;
#5998=DIRECTION ( 'NONE',  ( 0.000000000000000000, 0.9510565162951498674, 0.3090169943749583870 ) ) ;
#6001=EDGE_CURVE ( 'NONE', #5891, #10126, #13631, .T. ) ;
#6015=ORIENTED_EDGE ( 'NONE', *, *, #2581, .T. ) ;
#6017=VECTOR ( 'NONE', #2825, 1000.000000000000000 ) ;
#6026=ORIENTED_EDGE ( 'NONE', *, *, #17169, .T. ) ;
#6032=EDGE_CURVE ( 'NONE', #19214, #5836, #16409, .T. ) ;
#6034=CARTESIAN_POINT ( 'NONE',  ( 2.765633920072236851, -22.71065055754445439, -9.836394144775947979 ) ) ;
#6035=VERTEX_POINT ( 'NONE', #14805 ) ;
#6041=CARTESIAN_POINT ( 'NONE',  ( 0.000000000000000000, -5.535312321042921369, 23.48180575137728354 ) ) ;
#6046=ORIENTED_EDGE ( 'NONE', *, *, #9784, .T. ) ;
#6051=CIRCLE ( 'NONE', #1591, 24.12539914357697413 ) ;
#6056=ORIENTED_EDGE ( 'NONE', *, *, #5606, .F. ) ;
#6058=DIRECTION ( 'NONE',  ( 0.000000000000000000, 0.000000000000000000, 1.000000000000000000 ) ) ;
#6060=CARTESIAN_POINT ( 'NONE',  ( 0.000000000000000000, 22.25075486061751207, -9.324097380959241121 ) ) ;
#6069=CARTESIAN_POINT ( 'NONE',  ( 0.02436607992775934733, -21.30679549418640306, 12.59161484032904887 ) ) ;
#6071=CARTESIAN_POINT ( 'NONE',  ( 0.5321745326902582729, -26.83036154824997155, 3.467596033028195635 ) ) ;
#6079=CARTESIAN_POINT ( 'NONE',  ( 2.765633920072235519, -18.55949924794880346, -16.37294372382878649 ) ) ;
#6083=CYLINDRICAL_SURFACE ( 'NONE', #15140, 13.20000000000000107 ) ;
#6089=ORIENTED_EDGE ( 'NONE', *, *, #5484, .T. ) ;
#6091=AXIS2_PLACEMENT_3D ( 'NONE', #14906, #13598, #4394 ) ;
#6095=EDGE_CURVE ( 'NONE', #10294, #3268, #3760, .T. ) ;
#6099=VERTEX_POINT ( 'NONE', #6177 ) ;
#6105=CIRCLE ( 'NONE', #5774, 24.12539914357697768 ) ;
#6110=ORIENTED_EDGE ( 'NONE', *, *, #8375, .F. ) ;
#6117=CARTESIAN_POINT ( 'NONE',  ( 2.789999999999999147, -20.62201879784904079, -12.52067188844374179 ) ) ;
#6118=VERTEX_POINT ( 'NONE', #16902 ) ;
#6121=CARTESIAN_POINT ( 'NONE',  ( 2.789999999999999147, -24.04302995059966719, 1.991882183130210482 ) ) ;
#6122=AXIS2_PLACEMENT_3D ( 'NONE', #14644, #7009, #13133 ) ;
#6124=CARTESIAN_POINT ( 'NONE',  ( 2.718131885465890463, 18.89333555428578748, -16.91241718341978029 ) ) ;
#6126=CIRCLE ( 'NONE', #16040, 4.000000000000000000 ) ;
#6130=ADVANCED_FACE ( 'NONE', ( #4588 ), #5883, .T. ) ;
#6134=ORIENTED_EDGE ( 'NONE', *, *, #3631, .F. ) ;
#6147=LINE ( 'NONE', #7649, #7932 ) ;
#6148=EDGE_CURVE ( 'NONE', #11483, #17227, #18104, .T. ) ;
#6153=ORIENTED_EDGE ( 'NONE', *, *, #1271, .T. ) ;
#6159=CARTESIAN_POINT ( 'NONE',  ( 0.000000000000000000, 4.898587196589412829E-16, -4.000000000000000000 ) ) ;
#6167=CARTESIAN_POINT ( 'NONE',  ( 1.039999999999996039, 24.89775460606832169, 12.96210679857795256 ) ) ;
#6172=VECTOR ( 'NONE', #4597, 1000.000000000000000 ) ;
#6173=CARTESIAN_POINT ( 'NONE',  ( 2.632969638839692372, 22.37100459959346566, 12.81671916049022641 ) ) ;
#6176=DIRECTION ( 'NONE',  ( 0.000000000000000000, 0.000000000000000000, 1.000000000000000000 ) ) ;
#6177=CARTESIAN_POINT ( 'NONE',  ( 1.039999999999996705, -20.02152543075331081, -19.67366047555552555 ) ) ;
#6180=CARTESIAN_POINT ( 'NONE',  ( 0.5321745227542252765, -19.66801664102716884, 18.57583492944412384 ) ) ;
#6181=CARTESIAN_POINT ( 'NONE',  ( 1.039999999999997371, 25.12109765559653596, 12.52377138324232675 ) ) ;
#6186=FACE_OUTER_BOUND ( 'NONE', #6911, .T. ) ;
#6187=ORIENTED_EDGE ( 'NONE', *, *, #9883, .F. ) ;
#6190=AXIS2_PLACEMENT_3D ( 'NONE', #10147, #16245, #8636 ) ;
#6195=ORIENTED_EDGE ( 'NONE', *, *, #977, .F. ) ;
#6197=DIRECTION ( 'NONE',  ( -1.000000000000000000, -0.000000000000000000, 0.000000000000000000 ) ) ;
#6198=ORIENTED_EDGE ( 'NONE', *, *, #16620, .F. ) ;
#6203=DIRECTION ( 'NONE',  ( 0.000000000000000000, 0.000000000000000000, -1.000000000000000000 ) ) ;
#6208=CYLINDRICAL_SURFACE ( 'NONE', #8451, 13.19999999999999929 ) ;
#6210=CARTESIAN_POINT ( 'NONE',  ( 2.789999999999999147, 15.04425356660760293, 20.70663861606276868 ) ) ;
#6216=FACE_OUTER_BOUND ( 'NONE', #1627, .T. ) ;
#6230=DIRECTION ( 'NONE',  ( 1.000000000000000000, 0.000000000000000000, 0.000000000000000000 ) ) ;
#6231=ORIENTED_EDGE ( 'NONE', *, *, #6249, .F. ) ;
#6237=DIRECTION ( 'NONE',  ( -1.000000000000000000, -0.000000000000000000, -0.000000000000000000 ) ) ;
#6242=CARTESIAN_POINT ( 'NONE',  ( 1.749999999999998002, 0.000000000000000000, 0.000000000000000000 ) ) ;
#6249=EDGE_CURVE ( 'NONE', #10962, #14651, #2829, .T. ) ;
#6256=ORIENTED_EDGE ( 'NONE', *, *, #16644, .F. ) ;
#6258=DIRECTION ( 'NONE',  ( -1.000000000000000000, -0.000000000000000000, -0.000000000000000000 ) ) ;
#6273=AXIS2_PLACEMENT_3D ( 'NONE', #4795, #18309, #13703 ) ;
#6274=ORIENTED_EDGE ( 'NONE', *, *, #14703, .F. ) ;
#6282=CARTESIAN_POINT ( 'NONE',  ( 0.7592463896980037319, 19.12676442129342647, 19.86438386685667368 ) ) ;
#6284=DIRECTION ( 'NONE',  ( 0.000000000000000000, 0.000000000000000000, 1.000000000000000000 ) ) ;
#6291=CARTESIAN_POINT ( 'NONE',  ( 2.790000000000076863, -23.69897269326681055, 5.456611084821764379 ) ) ;
#6295=EDGE_CURVE ( 'NONE', #12478, #6099, #16507, .T. ) ;
#6296=CARTESIAN_POINT ( 'NONE',  ( 0.000000000000000000, 12.52067188844351442, 20.62201879784919001 ) ) ;
#6301=CARTESIAN_POINT ( 'NONE',  ( 2.031033479673592268, -19.86422722021325882, 19.12621924769859660 ) ) ;
#6305=CARTESIAN_POINT ( 'NONE',  ( 0.1855654851361731306, 23.63475234378982748, 10.67816411292173306 ) ) ;
#6306=ORIENTED_EDGE ( 'NONE', *, *, #4691, .T. ) ;
#6308=ORIENTED_EDGE ( 'NONE', *, *, #5484, .F. ) ;
#6309=DIRECTION ( 'NONE',  ( -1.000000000000000000, -0.000000000000000000, -0.000000000000000000 ) ) ;
#6315=AXIS2_PLACEMENT_3D ( 'NONE', #5293, #11592, #3691 ) ;
#6317=TOROIDAL_SURFACE ( 'NONE', #2172, 24.12539914357697768, 8.000000000000000000 ) ;
#6320=CARTESIAN_POINT ( 'NONE',  ( 1.039999999999997593, 0.000000000000000000, 0.000000000000000000 ) ) ;
#6323=CARTESIAN_POINT ( 'NONE',  ( 1.749999999999998002, 4.147968289691672084, -27.76164181293047406 ) ) ;
#6327=CARTESIAN_POINT ( 'NONE',  ( 0.000000000000000000, 0.000000000000000000, 0.000000000000000000 ) ) ;
#6336=ORIENTED_EDGE ( 'NONE', *, *, #13205, .T. ) ;
#6351=DIRECTION ( 'NONE',  ( 0.000000000000000000, 0.000000000000000000, 1.000000000000000000 ) ) ;
#6355=CARTESIAN_POINT ( 'NONE',  ( 2.718131847775120402, 5.344160105509049963, -24.78765742476133482 ) ) ;
#6364=CARTESIAN_POINT ( 'NONE',  ( 0.006974674093432157128, -2.249040938978327908, -24.42374957165208116 ) ) ;
#6368=AXIS2_PLACEMENT_3D ( 'NONE', #9337, #15539, #1826 ) ;
#6372=CARTESIAN_POINT ( 'NONE',  ( 0.02436607992776108206, -24.15498966839966855, 5.391175441198523544 ) ) ;
#6373=ORIENTED_EDGE ( 'NONE', *, *, #11743, .T. ) ;
#6376=ORIENTED_EDGE ( 'NONE', *, *, #14904, .T. ) ;
#6377=CARTESIAN_POINT ( 'NONE',  ( 2.789999999999999147, 0.000000000000000000, 0.000000000000000000 ) ) ;
#6383=ADVANCED_FACE ( 'NONE', ( #5276 ), #9803, .T. ) ;
#6390=CYLINDRICAL_SURFACE ( 'NONE', #12980, 28.06981291497571362 ) ;
#6391=ORIENTED_EDGE ( 'NONE', *, *, #7081, .F. ) ;
#6392=DIRECTION ( 'NONE',  ( -1.000000000000000000, -0.000000000000000000, -0.000000000000000000 ) ) ;
#6397=CARTESIAN_POINT ( 'NONE',  ( -10.00000000000000000, 0.000000000000000000, 0.000000000000000000 ) ) ;
#6409=EDGE_LOOP ( 'NONE', ( #75, #7566, #946, #14750, #3446, #14521 ) ) ;
#6410=CARTESIAN_POINT ( 'NONE',  ( 0.1587402281127123227, 22.38003579136345067, 12.81821841996081801 ) ) ;
#6423=EDGE_CURVE ( 'NONE', #18627, #17326, #17468, .T. ) ;
#6424=CIRCLE ( 'NONE', #14113, 2.524999999999996358 ) ;
#6425=ORIENTED_EDGE ( 'NONE', *, *, #5365, .F. ) ;
#6426=PRODUCT_CONTEXT ( 'NONE', #9843, 'mechanical' ) ;
#6433=FACE_OUTER_BOUND ( 'NONE', #13692, .T. ) ;
#6435=EDGE_CURVE ( 'NONE', #15675, #1756, #5251, .T. ) ;
#6436=ORIENTED_EDGE ( 'NONE', *, *, #14703, .T. ) ;
#6449=CARTESIAN_POINT ( 'NONE',  ( 2.601776096565022289, -12.84621645676828372, -22.54313264455027976 ) ) ;
#6453=DIRECTION ( 'NONE',  ( 1.000000000000000000, 0.000000000000000000, 0.000000000000000000 ) ) ;
#6454=TOROIDAL_SURFACE ( 'NONE', #12247, 24.12539914357697413, 8.000000000000000000 ) ;
#6457=CARTESIAN_POINT ( 'NONE',  ( 2.604434261026090880, -25.39738473784997552, -5.253342437939998888 ) ) ;
#6469=VECTOR ( 'NONE', #9453, 1000.000000000000000 ) ;
#6470=FACE_OUTER_BOUND ( 'NONE', #17872, .T. ) ;
#6473=CIRCLE ( 'NONE', #9376, 28.06981291497571007 ) ;
#6477=EDGE_CURVE ( 'NONE', #13404, #7114, #471, .T. ) ;
#6485=( GEOMETRIC_REPRESENTATION_CONTEXT ( 3 ) GLOBAL_UNCERTAINTY_ASSIGNED_CONTEXT ( ( #14991 ) ) GLOBAL_UNIT_ASSIGNED_CONTEXT ( ( #10803, #10708, #15312 ) ) REPRESENTATION_CONTEXT ( 'NONE', 'WORKASPACE' ) );
#6486=CYLINDRICAL_SURFACE ( 'NONE', #10484, 2.524999999999995914 ) ;
#6489=B_SPLINE_CURVE_WITH_KNOTS ( 'NONE', 3,
 ( #5366, #15254, #9146, #12250 ),
 .UNSPECIFIED., .F., .F.,
 ( 4, 4 ),
 ( 0.005258214619651955385, 0.005948481662034169927 ),
 .UNSPECIFIED. ) ;
#6491=ORIENTED_EDGE ( 'NONE', *, *, #13098, .F. ) ;
#6494=ADVANCED_FACE ( 'NONE', ( #7245 ), #19469, .F. ) ;
#6497=ORIENTED_EDGE ( 'NONE', *, *, #16183, .F. ) ;
#6499=ADVANCED_FACE ( 'NONE', ( #11871 ), #17304, .T. ) ;
#6505=CARTESIAN_POINT ( 'NONE',  ( 2.789999999999999147, -22.25075486061744812, 9.324097380959361914 ) ) ;
#6509=CARTESIAN_POINT ( 'NONE',  ( 2.765633920072235963, 24.63872515616082737, 2.336989772644355146 ) ) ;
#6514=CARTESIAN_POINT ( 'NONE',  ( 2.789999999999999147, 0.000000000000000000, 0.000000000000000000 ) ) ;
#6515=AXIS2_PLACEMENT_3D ( 'NONE', #18473, #18669, #4967 ) ;
#6522=ORIENTED_EDGE ( 'NONE', *, *, #7803, .F. ) ;
#6527=CIRCLE ( 'NONE', #12623, 28.06981291497571007 ) ;
#6529=B_SPLINE_CURVE_WITH_KNOTS ( 'NONE', 3,
 ( #12636, #18630, #3523, #3819, #14632, #18926 ),
 .UNSPECIFIED., .F., .F.,
 ( 4, 2, 4 ),
 ( 2.132675795051084930E-07, 0.001878604073277006722, 0.003756994878974508241 ),
 .UNSPECIFIED. ) ;
#6537=EDGE_LOOP ( 'NONE', ( #10450, #1639, #10173, #10534 ) ) ;
#6540=ORIENTED_EDGE ( 'NONE', *, *, #1951, .F. ) ;
#6544=DIRECTION ( 'NONE',  ( 0.000000000000000000, 0.000000000000000000, 1.000000000000000000 ) ) ;
#6545=CARTESIAN_POINT ( 'NONE',  ( 2.601776121706764311, -17.47009390565504816, 19.18368891937484477 ) ) ;
#6547=CARTESIAN_POINT ( 'NONE',  ( 0.006931054464084583991, -2.248820353273142558, 24.42321038836782776 ) ) ;
#6553=ADVANCED_FACE ( 'NONE', ( #13250 ), #11744, .T. ) ;
#6554=CIRCLE ( 'NONE', #4337, 28.06981291497571007 ) ;
#6560=B_SPLINE_CURVE_WITH_KNOTS ( 'NONE', 3,
 ( #14089, #495, #6568, #4792, #13901, #14294 ),
 .UNSPECIFIED., .F., .F.,
 ( 4, 2, 4 ),
 ( 4.462636732176736601E-07, 0.001879885066974997356, 0.003759323870276777037 ),
 .UNSPECIFIED. ) ;
#6563=DIRECTION ( 'NONE',  ( -1.000000000000000000, -0.000000000000000000, -0.000000000000000000 ) ) ;
#6567=CYLINDRICAL_SURFACE ( 'NONE', #16693, 13.19999999999999929 ) ;
#6568=CARTESIAN_POINT ( 'NONE',  ( 0.5321745326902584949, 3.467596033028283564, 26.83036154824995023 ) ) ;
#6575=DIRECTION ( 'NONE',  ( 0.000000000000000000, 0.000000000000000000, 1.000000000000000000 ) ) ;
#6587=ADVANCED_FACE ( 'NONE', ( #10253 ), #852, .F. ) ;
#6597=CARTESIAN_POINT ( 'NONE',  ( 2.783025325906568259, 24.42374957165205629, 2.249040938978581927 ) ) ;
#6600=ORIENTED_EDGE ( 'NONE', *, *, #16003, .F. ) ;
#6602=ORIENTED_EDGE ( 'NONE', *, *, #6847, .F. ) ;
#6604=B_SPLINE_CURVE_WITH_KNOTS ( 'NONE', 3,
 ( #6167, #8984, #18192, #18287 ),
 .UNSPECIFIED., .F., .F.,
 ( 4, 4 ),
 ( 4.462636695653741059E-07, 0.0004963285629696456008 ),
 .UNSPECIFIED. ) ;
#6607=FACE_OUTER_BOUND ( 'NONE', #3424, .T. ) ;
#6608=CARTESIAN_POINT ( 'NONE',  ( 0.1855655959470679794, 19.17825124759777822, 17.45907811351462158 ) ) ;
#6617=DIRECTION ( 'NONE',  ( -1.000000000000000000, 0.000000000000000000, 0.000000000000000000 ) ) ;
#6634=FACE_OUTER_BOUND ( 'NONE', #14288, .T. ) ;
#6639=CARTESIAN_POINT ( 'NONE',  ( 2.765633920072235963, 22.71065055754452544, 9.836394144775786330 ) ) ;
#6641=VECTOR ( 'NONE', #13457, 1000.000000000000000 ) ;
#6647=CARTESIAN_POINT ( 'NONE',  ( 1.039999999999997149, -24.89775460606822577, -12.96210679857813730 ) ) ;
#6651=ORIENTED_EDGE ( 'NONE', *, *, #2579, .T. ) ;
#6652=ORIENTED_EDGE ( 'NONE', *, *, #11909, .T. ) ;
#6667=DIRECTION ( 'NONE',  ( 0.000000000000000000, 0.000000000000000000, 1.000000000000000000 ) ) ;
#6668=CARTESIAN_POINT ( 'NONE',  ( 2.790000000000000036, 18.34424029220134500, -15.96500990068104997 ) ) ;
#6670=AXIS2_PLACEMENT_3D ( 'NONE', #10151, #11741, #6929 ) ;
#6675=ORIENTED_EDGE ( 'NONE', *, *, #7117, .F. ) ;
#6683=DIRECTION ( 'NONE',  ( 0.000000000000000000, 0.000000000000000000, 1.000000000000000000 ) ) ;
#6698=CARTESIAN_POINT ( 'NONE',  ( 2.765633920072236851, 24.15498966839963302, 5.391175441198700291 ) ) ;
#6699=ORIENTED_EDGE ( 'NONE', *, *, #3353, .T. ) ;
#6711=EDGE_CURVE ( 'NONE', #10395, #3050, #4051, .T. ) ;
#6715=VERTEX_POINT ( 'NONE', #16848 ) ;
#6717=CYLINDRICAL_SURFACE ( 'NONE', #18566, 4.000000000000000000 ) ;
#6719=VERTEX_POINT ( 'NONE', #15347 ) ;
#6720=CARTESIAN_POINT ( 'NONE',  ( 0.7589665326895898012, 24.32849926382769468, -12.98167595240995986 ) ) ;
#6722=DIRECTION ( 'NONE',  ( 0.000000000000000000, 0.000000000000000000, 1.000000000000000000 ) ) ;
#6728=DIRECTION ( 'NONE',  ( 0.000000000000000000, 0.000000000000000000, 1.000000000000000000 ) ) ;
#6729=ORIENTED_EDGE ( 'NONE', *, *, #2311, .T. ) ;
#6731=CARTESIAN_POINT ( 'NONE',  ( 0.1570303611602991700, -22.37100459959352605, 12.81671916049007365 ) ) ;
#6732=DIRECTION ( 'NONE',  ( 0.000000000000000000, 0.000000000000000000, 1.000000000000000000 ) ) ;
#6735=EDGE_LOOP ( 'NONE', ( #420, #1321, #4068, #6110 ) ) ;
#6742=CARTESIAN_POINT ( 'NONE',  ( 1.394999999999999574, -4.633866840648735774, -27.68468304288263582 ) ) ;
#6747=B_SPLINE_CURVE_WITH_KNOTS ( 'NONE', 3,
 ( #11232, #17236, #6608, #539, #12738, #3626 ),
 .UNSPECIFIED., .F., .F.,
 ( 4, 2, 4 ),
 ( 2.321268216996908089E-07, 0.001878622960950487733, 0.003757013795079275874 ),
 .UNSPECIFIED. ) ;
#6752=CARTESIAN_POINT ( 'NONE',  ( 0.8291131470075020493, -24.44424927289185590, 12.96989951879399072 ) ) ;
#6754=ORIENTED_EDGE ( 'NONE', *, *, #1271, .F. ) ;
#6756=B_SPLINE_CURVE_WITH_KNOTS ( 'NONE', 3,
 ( #6505, #3519, #9636, #12730 ),
 .UNSPECIFIED., .F., .F.,
 ( 4, 4 ),
 ( 0.005258105385878687407, 0.005948373736081388405 ),
 .UNSPECIFIED. ) ;
#6759=CARTESIAN_POINT ( 'NONE',  ( 2.789999999999999147, -24.15498966839958683, -5.391175441198872598 ) ) ;
#6761=VERTEX_POINT ( 'NONE', #1234 ) ;
#6765=VERTEX_POINT ( 'NONE', #19640 ) ;
#6766=LINE ( 'NONE', #3577, #12327 ) ;
#6769=CARTESIAN_POINT ( 'NONE',  ( 0.5279272933715204452, -19.66369668717018726, -18.56460150496961248 ) ) ;
#6775=CARTESIAN_POINT ( 'NONE',  ( 2.789679245949058917, 20.70663861606308487, -12.51925356660738053 ) ) ;
#6781=LINE ( 'NONE', #19003, #11191 ) ;
#6787=DIRECTION ( 'NONE',  ( -1.000000000000000000, 0.000000000000000000, 0.000000000000000000 ) ) ;
#6790=VERTEX_POINT ( 'NONE', #13433 ) ;
#6795=DIRECTION ( 'NONE',  ( 0.000000000000000000, 1.776356839400252831E-15, -1.000000000000000000 ) ) ;
#6803=CARTESIAN_POINT ( 'NONE',  ( 1.749999999999998002, 20.02152543075346003, 19.67366047555537634 ) ) ;
#6805=CARTESIAN_POINT ( 'NONE',  ( 1.749999999999998002, 0.000000000000000000, 0.000000000000000000 ) ) ;
#6808=CARTESIAN_POINT ( 'NONE',  ( 0.5321745326902582729, -3.467596033028097935, -26.83036154824997510 ) ) ;
#6815=DIRECTION ( 'NONE',  ( 1.000000000000000000, 0.000000000000000000, 0.000000000000000000 ) ) ;
#6816=EDGE_LOOP ( 'NONE', ( #10059, #3864, #18474, #12427 ) ) ;
#6819=B_SPLINE_CURVE_WITH_KNOTS ( 'NONE', 3,
 ( #2401, #11513, #2205, #999 ),
 .UNSPECIFIED., .F., .F.,
 ( 4, 4 ),
 ( 2.324263106244727961E-07, 0.0006888201370294890283 ),
 .UNSPECIFIED. ) ;
#6820=DIRECTION ( 'NONE',  ( -1.000000000000000000, 0.000000000000000000, 0.000000000000000000 ) ) ;
#6823=VERTEX_POINT ( 'NONE', #15141 ) ;
#6827=VECTOR ( 'NONE', #17787, 1000.000000000000000 ) ;
#6828=ORIENTED_EDGE ( 'NONE', *, *, #6711, .T. ) ;
#6829=CARTESIAN_POINT ( 'NONE',  ( 0.02436607992776151574, -18.55949924794880346, -16.37294372382878649 ) ) ;
#6830=ORIENTED_EDGE ( 'NONE', *, *, #11474, .F. ) ;
#6833=DIRECTION ( 'NONE',  ( 0.000000000000000000, 0.000000000000000000, 1.000000000000000000 ) ) ;
#6839=VERTEX_POINT ( 'NONE', #18245 ) ;
#6841=AXIS2_PLACEMENT_3D ( 'NONE', #15133, #1428, #13727 ) ;
#6845=FACE_OUTER_BOUND ( 'NONE', #10945, .T. ) ;
#6847=EDGE_CURVE ( 'NONE', #10551, #9218, #7608, .T. ) ;
#6855=VECTOR ( 'NONE', #14593, 1000.000000000000000 ) ;
#6856=CARTESIAN_POINT ( 'NONE',  ( 0.006931038682727856497, -12.53626894672812853, -21.08061549536629187 ) ) ;
#6857=ORIENTED_EDGE ( 'NONE', *, *, #14724, .F. ) ;
#6860=EDGE_LOOP ( 'NONE', ( #13176, #9129, #3433, #2742, #15787, #6872 ) ) ;
#6866=FACE_OUTER_BOUND ( 'NONE', #19628, .T. ) ;
#6868=CARTESIAN_POINT ( 'NONE',  ( 0.000000000000000000, -15.04425356660744839, -20.70663861606288236 ) ) ;
#6870=AXIS2_PLACEMENT_3D ( 'NONE', #6514, #439, #332 ) ;
#6872=ORIENTED_EDGE ( 'NONE', *, *, #11042, .T. ) ;
#6876=ADVANCED_FACE ( 'NONE', ( #10040 ), #15936, .F. ) ;
#6877=EDGE_CURVE ( 'NONE', #7268, #2962, #9747, .T. ) ;
#6881=ORIENTED_EDGE ( 'NONE', *, *, #14085, .T. ) ;
#6893=ORIENTED_EDGE ( 'NONE', *, *, #3422, .F. ) ;
#6894=DIRECTION ( 'NONE',  ( 1.000000000000000000, 0.000000000000000000, 0.000000000000000000 ) ) ;
#6897=DIRECTION ( 'NONE',  ( -1.000000000000000000, 0.000000000000000000, -0.000000000000000000 ) ) ;
#6898=ORIENTED_EDGE ( 'NONE', *, *, #985, .T. ) ;
#6901=ORIENTED_EDGE ( 'NONE', *, *, #7821, .T. ) ;
#6902=CARTESIAN_POINT ( 'NONE',  ( 0.07181525068722535710, -2.576941577947229334, -25.22524549359953383 ) ) ;
#6905=ADVANCED_FACE ( 'NONE', ( #6607 ), #831, .T. ) ;
#6909=CARTESIAN_POINT ( 'NONE',  ( 2.030753603471114666, 12.98165646470082457, 24.32906614999620132 ) ) ;
#6911=EDGE_LOOP ( 'NONE', ( #3561, #7917, #10246, #13836 ) ) ;
#6918=DIRECTION ( 'NONE',  ( 0.000000000000000000, 0.000000000000000000, 1.000000000000000000 ) ) ;
#6920=VERTEX_POINT ( 'NONE', #632 ) ;
#6926=CYLINDRICAL_SURFACE ( 'NONE', #6190, 13.19999999999999929 ) ;
#6929=DIRECTION ( 'NONE',  ( 0.000000000000000000, 0.000000000000000000, 1.000000000000000000 ) ) ;
#6933=DIRECTION ( 'NONE',  ( -1.000000000000000000, 0.000000000000000000, 0.000000000000000000 ) ) ;
#6939=DIRECTION ( 'NONE',  ( 0.000000000000000000, 0.000000000000000000, 1.000000000000000000 ) ) ;
#6941=CARTESIAN_POINT ( 'NONE',  ( 2.030753605846571386, 27.31305418910209326, 3.797885586973312133 ) ) ;
#6947=CARTESIAN_POINT ( 'NONE',  ( 1.039999999999996039, 27.68468304288258963, 4.633866840649018215 ) ) ;
#6949=EDGE_CURVE ( 'NONE', #14221, #17740, #14762, .T. ) ;
#6952=CARTESIAN_POINT ( 'NONE',  ( 2.783068888626320625, -9.685942809246897767, -22.53293026234513619 ) ) ;
#6957=ORIENTED_EDGE ( 'NONE', *, *, #5900, .T. ) ;
#6960=DIRECTION ( 'NONE',  ( 0.000000000000000000, 0.000000000000000000, 1.000000000000000000 ) ) ;
#6964=FACE_OUTER_BOUND ( 'NONE', #6537, .T. ) ;
#6976=DIRECTION ( 'NONE',  ( 0.000000000000000000, 0.000000000000000000, 1.000000000000000000 ) ) ;
#6977=DIRECTION ( 'NONE',  ( 0.000000000000000000, 0.000000000000000000, 1.000000000000000000 ) ) ;
#6980=FACE_OUTER_BOUND ( 'NONE', #11078, .T. ) ;
#6981=EDGE_CURVE ( 'NONE', #8643, #13582, #12020, .T. ) ;
#6989=DIRECTION ( 'NONE',  ( -1.000000000000000000, 0.000000000000000000, 0.000000000000000000 ) ) ;
#6997=ORIENTED_EDGE ( 'NONE', *, *, #15052, .F. ) ;
#6999=CARTESIAN_POINT ( 'NONE',  ( 0.02436607992775717893, -9.836394144775869819, 22.71065055754449347 ) ) ;
#7000=CARTESIAN_POINT ( 'NONE',  ( 0.006974657972266078837, 5.408388659524427489, -23.92335783895632417 ) ) ;
#7004=ORIENTED_EDGE ( 'NONE', *, *, #17208, .T. ) ;
#7006=DIRECTION ( 'NONE',  ( -1.000000000000000000, 0.000000000000000000, 0.000000000000000000 ) ) ;
#7009=DIRECTION ( 'NONE',  ( -1.000000000000000000, 0.000000000000000000, -0.000000000000000000 ) ) ;
#7012=CIRCLE ( 'NONE', #6368, 24.12539914357697413 ) ;
#7013=CARTESIAN_POINT ( 'NONE',  ( 5.366045694719498695E-16, 9.514945144209063344, -22.37986894186662923 ) ) ;
#7015=AXIS2_PLACEMENT_3D ( 'NONE', #7913, #17131, #17228 ) ;
#7027=ORIENTED_EDGE ( 'NONE', *, *, #10838, .T. ) ;
#7043=CARTESIAN_POINT ( 'NONE',  ( 1.998465710409312357E-16, 22.37986894186671805, 9.514945144208807548 ) ) ;
#7045=CARTESIAN_POINT ( 'NONE',  ( 0.000000000000000000, -12.52067188844335988, -20.62201879784928238 ) ) ;
#7046=ORIENTED_EDGE ( 'NONE', *, *, #4312, .F. ) ;
#7049=CIRCLE ( 'NONE', #1635, 28.06981291497571362 ) ;
#7058=DIRECTION ( 'NONE',  ( 0.000000000000000000, 0.000000000000000000, 1.000000000000000000 ) ) ;
#7060=CARTESIAN_POINT ( 'NONE',  ( 2.790000000000076863, -12.51293083811783191, -20.85287692521943015 ) ) ;
#7070=CARTESIAN_POINT ( 'NONE',  ( 0.1855654851361725199, -23.63475234378974577, -10.67816411292190004 ) ) ;
#7074=ADVANCED_FACE ( 'NONE', ( #8617 ), #8040, .T. ) ;
#7079=DIRECTION ( 'NONE',  ( -1.000000000000000000, -0.000000000000000000, -0.000000000000000000 ) ) ;
#7080=CARTESIAN_POINT ( 'NONE',  ( 2.765633920072235963, 22.71065055754452544, 9.836394144775786330 ) ) ;
#7081=EDGE_CURVE ( 'NONE', #1705, #12785, #17861, .T. ) ;
#7083=LINE ( 'NONE', #15824, #12669 ) ;
#7084=LINE ( 'NONE', #17621, #142 ) ;
#7085=CIRCLE ( 'NONE', #7751, 24.12539914357697768 ) ;
#7089=CARTESIAN_POINT ( 'NONE',  ( 2.790000000000077751, 5.456611084821854085, 23.69897269326679279 ) ) ;
#7092=CARTESIAN_POINT ( 'NONE',  ( 0.02436607992776194942, -5.391175441198450713, -24.15498966839968276 ) ) ;
#7093=CARTESIAN_POINT ( 'NONE',  ( 1.394999999999999574, -19.67366047555544739, 20.02152543075338897 ) ) ;
#7096=VERTEX_POINT ( 'NONE', #10520 ) ;
#7099=EDGE_CURVE ( 'NONE', #5891, #6823, #14115, .T. ) ;
#7103=CIRCLE ( 'NONE', #1056, 2.524999999999995914 ) ;
#7106=CARTESIAN_POINT ( 'NONE',  ( 0.000000000000000000, -20.62201879784905501, -12.52067188844372936 ) ) ;
#7113=CARTESIAN_POINT ( 'NONE',  ( 0.1855655959470668692, 17.45907811351482763, -19.17825124759758282 ) ) ;
#7114=VERTEX_POINT ( 'NONE', #1212 ) ;
#7115=CARTESIAN_POINT ( 'NONE',  ( 2.789999999999999147, -24.44424927289185590, 12.96989951879399072 ) ) ;
#7116=ORIENTED_EDGE ( 'NONE', *, *, #4214, .F. ) ;
#7117=EDGE_CURVE ( 'NONE', #8320, #15591, #8915, .T. ) ;
#7127=EDGE_CURVE ( 'NONE', #18731, #17165, #9256, .T. ) ;
#7133=CARTESIAN_POINT ( 'NONE',  ( 0.02436607992775978102, 16.37294372382885044, -18.55949924794875017 ) ) ;
#7135=ORIENTED_EDGE ( 'NONE', *, *, #19103, .F. ) ;
#7136=DIRECTION ( 'NONE',  ( -1.000000000000000000, -0.000000000000000000, -0.000000000000000000 ) ) ;
#7139=EDGE_LOOP ( 'NONE', ( #13216, #10976, #853, #16176, #7459, #8499, #4566, #11971, #7358, #3711, #2935, #14709, #13370, #4925, #19022, #19411, #17279, #15960, #12520, #10578, #7390, #339, #18325, #13093, #12089, #523, #3742, #12075, #11543, #11496, #17171, #5019, #9196, #18025, #2043, #9154, #11218, #3975, #215, #1811, #3146, #11921, #661, #12589, #7661 ) ) ;
#7144=VECTOR ( 'NONE', #1302, 1000.000000000000000 ) ;
#7148=DIRECTION ( 'NONE',  ( -1.000000000000000000, 0.000000000000000000, 0.000000000000000000 ) ) ;
#7150=AXIS2_PLACEMENT_3D ( 'NONE', #8656, #16079, #11374 ) ;
#7151=ORIENTED_EDGE ( 'NONE', *, *, #2405, .T. ) ;
#7162=CARTESIAN_POINT ( 'NONE',  ( 2.789999999999999147, 7.909232158575156824, -24.34211360614291664 ) ) ;
#7164=CARTESIAN_POINT ( 'NONE',  ( 0.0003207540509378258692, 20.70663861606293921, -12.51925356660738053 ) ) ;
#7169=EDGE_LOOP ( 'NONE', ( #7293, #7939, #11548, #7849, #5505, #4673, #15272, #11913, #4398, #14646, #6881, #14144, #11143, #13501, #7212, #14581, #4105, #8728, #9759, #15577, #9789, #848, #14212, #9881, #4523, #1133, #12517, #12241, #12862, #12275, #1032, #11650, #5352, #9688, #16455, #15714, #19262, #7116, #8651, #7046, #11450, #5884, #4134, #16417, #3630 ) ) ;
#7170=DIRECTION ( 'NONE',  ( 0.000000000000000000, 0.000000000000000000, 1.000000000000000000 ) ) ;
#7171=CARTESIAN_POINT ( 'NONE',  ( 0.1882238946918237121, 25.78859396478527799, -2.857713464478781162 ) ) ;
#7177=AXIS2_PLACEMENT_3D ( 'NONE', #543, #2128, #5029 ) ;
#7179=FACE_OUTER_BOUND ( 'NONE', #6409, .T. ) ;
#7180=ORIENTED_EDGE ( 'NONE', *, *, #2854, .F. ) ;
#7190=EDGE_CURVE ( 'NONE', #19316, #18335, #1975, .T. ) ;
#7196=CARTESIAN_POINT ( 'NONE',  ( 2.718131885465892239, 16.91241718341998634, 18.89333555428560274 ) ) ;
#7203=CIRCLE ( 'NONE', #16504, 2.524999999999996358 ) ;
#7205=CARTESIAN_POINT ( 'NONE',  ( 2.765633920072238627, 12.59161484032942901, -21.30679549418617924 ) ) ;
#7209=DIRECTION ( 'NONE',  ( 0.000000000000000000, 0.000000000000000000, 1.000000000000000000 ) ) ;
#7212=ORIENTED_EDGE ( 'NONE', *, *, #15668, .F. ) ;
#7215=CARTESIAN_POINT ( 'NONE',  ( 1.749999999999998002, 0.000000000000000000, 0.000000000000000000 ) ) ;
#7219=TOROIDAL_SURFACE ( 'NONE', #7859, 24.12539914357697768, 8.000000000000000000 ) ;
#7222=EDGE_CURVE ( 'NONE', #6920, #5362, #12208, .T. ) ;
#7223=ORIENTED_EDGE ( 'NONE', *, *, #9784, .F. ) ;
#7225=CARTESIAN_POINT ( 'NONE',  ( 2.789999999999999147, 22.71065055754452544, 9.836394144775786330 ) ) ;
#7226=CARTESIAN_POINT ( 'NONE',  ( 8.000000000000000000, 0.000000000000000000, 0.000000000000000000 ) ) ;
#7227=EDGE_CURVE ( 'NONE', #9218, #10744, #4254, .T. ) ;
#7236=ORIENTED_EDGE ( 'NONE', *, *, #2465, .T. ) ;
#7238=EDGE_CURVE ( 'NONE', #19326, #17134, #6126, .T. ) ;
#7240=ADVANCED_FACE ( 'NONE', ( #10618 ), #3305, .F. ) ;
#7243=ORIENTED_EDGE ( 'NONE', *, *, #14483, .F. ) ;
#7245=FACE_OUTER_BOUND ( 'NONE', #4022, .T. ) ;
#7250=DIRECTION ( 'NONE',  ( -1.000000000000000000, -0.000000000000000000, -0.000000000000000000 ) ) ;
#7251=EDGE_CURVE ( 'NONE', #5965, #8006, #436, .T. ) ;
#7253=CYLINDRICAL_SURFACE ( 'NONE', #7455, 2.524999999999995914 ) ;
#7256=CARTESIAN_POINT ( 'NONE',  ( 2.765633920072239516, 16.37294372382858398, 18.55949924794898465 ) ) ;
#7258=CARTESIAN_POINT ( 'NONE',  ( 2.789999999999999147, -12.52067188844336165, -20.62201879784926462 ) ) ;
#7266=B_SPLINE_CURVE_WITH_KNOTS ( 'NONE', 3,
 ( #15955, #2240, #14454, #6829 ),
 .UNSPECIFIED., .F., .F.,
 ( 4, 4 ),
 ( 0.005258110598983623853, 0.005948376585272730464 ),
 .UNSPECIFIED. ) ;
#7268=VERTEX_POINT ( 'NONE', #14516 ) ;
#7276=CARTESIAN_POINT ( 'NONE',  ( 2.718131864678288601, -25.22589920183363432, 2.577209017046923289 ) ) ;
#7280=DIRECTION ( 'NONE',  ( -1.000000000000000000, 0.000000000000000000, -0.000000000000000000 ) ) ;
#7283=EDGE_LOOP ( 'NONE', ( #18557, #10303, #9872, #1854, #8912, #18296 ) ) ;
#7286=CARTESIAN_POINT ( 'NONE',  ( 0.02436607992776368414, 18.55949924794916228, -16.37294372382838148 ) ) ;
#7293=ORIENTED_EDGE ( 'NONE', *, *, #9080, .F. ) ;
#7296=ORIENTED_EDGE ( 'NONE', *, *, #1228, .T. ) ;
#7299=EDGE_CURVE ( 'NONE', #19316, #312, #3042, .T. ) ;
#7300=DIRECTION ( 'NONE',  ( 1.000000000000000000, 0.000000000000000000, 0.000000000000000000 ) ) ;
#7317=CARTESIAN_POINT ( 'NONE',  ( 2.789999999999999147, -15.74360496233394002, 18.28042085475272671 ) ) ;
#7326=CARTESIAN_POINT ( 'NONE',  ( 2.789999999999999147, 19.91106274590533687, -14.18181402625721077 ) ) ;
#7327=DIRECTION ( 'NONE',  ( -1.000000000000000000, -0.000000000000000000, -0.000000000000000000 ) ) ;
#7334=EDGE_CURVE ( 'NONE', #993, #3395, #17162, .T. ) ;
#7348=ORIENTED_EDGE ( 'NONE', *, *, #3982, .T. ) ;
#7349=AXIS2_PLACEMENT_3D ( 'NONE', #7326, #2937, #2841 ) ;
#7350=ADVANCED_FACE ( 'NONE', ( #17508 ), #1039, .T. ) ;
#7356=FACE_OUTER_BOUND ( 'NONE', #5266, .T. ) ;
#7357=CARTESIAN_POINT ( 'NONE',  ( -7.841635642041319107E-14, -15.96555658743749717, -18.34439787333524663 ) ) ;
#7358=ORIENTED_EDGE ( 'NONE', *, *, #18562, .F. ) ;
#7359=CARTESIAN_POINT ( 'NONE',  ( 0.000000000000000000, 0.000000000000000000, 0.000000000000000000 ) ) ;
#7363=CARTESIAN_POINT ( 'NONE',  ( 1.039999999999997593, 0.000000000000000000, 0.000000000000000000 ) ) ;
#7366=ORIENTED_EDGE ( 'NONE', *, *, #19688, .F. ) ;
#7367=CARTESIAN_POINT ( 'NONE',  ( 2.783025306068355853, -18.43727551351019045, -16.17543236988008815 ) ) ;
#7374=CARTESIAN_POINT ( 'NONE',  ( 2.604434325169353137, -25.77772010606608077, 2.851997810081559503 ) ) ;
#7390=ORIENTED_EDGE ( 'NONE', *, *, #10817, .F. ) ;
#7397=ADVANCED_FACE ( 'NONE', ( #3603 ), #13007, .T. ) ;
#7400=FACE_OUTER_BOUND ( 'NONE', #11256, .T. ) ;
#7406=DIRECTION ( 'NONE',  ( -1.000000000000000000, -0.000000000000000000, 0.000000000000000000 ) ) ;
#7417=LINE ( 'NONE', #16851, #8865 ) ;
#7422=AXIS2_PLACEMENT_3D ( 'NONE', #5940, #8858, #10462 ) ;
#7424=ADVANCED_FACE ( 'NONE', ( #12807 ), #5194, .F. ) ;
#7427=ORIENTED_EDGE ( 'NONE', *, *, #12479, .F. ) ;
#7435=ORIENTED_EDGE ( 'NONE', *, *, #14270, .F. ) ;
#7440=ORIENTED_EDGE ( 'NONE', *, *, #7238, .T. ) ;
#7444=ADVANCED_FACE ( 'NONE', ( #19288 ), #13199, .F. ) ;
#7448=DIRECTION ( 'NONE',  ( 0.000000000000000000, 0.000000000000000000, 1.000000000000000000 ) ) ;
#7449=AXIS2_PLACEMENT_3D ( 'NONE', #13301, #19112, #19017 ) ;
#7450=CARTESIAN_POINT ( 'NONE',  ( 0.02436607992775978102, -12.59161484032896361, -21.30679549418645280 ) ) ;
#7452=ORIENTED_EDGE ( 'NONE', *, *, #12892, .F. ) ;
#7453=ADVANCED_FACE ( 'NONE', ( #10105 ), #19485, .T. ) ;
#7455=AXIS2_PLACEMENT_3D ( 'NONE', #15993, #14692, #978 ) ;
#7457=CARTESIAN_POINT ( 'NONE',  ( 1.039999999999996039, 24.89775460606832169, 12.96210679857795256 ) ) ;
#7459=ORIENTED_EDGE ( 'NONE', *, *, #15502, .F. ) ;
#7465=EDGE_CURVE ( 'NONE', #16071, #7096, #17372, .T. ) ;
#7467=CYLINDRICAL_SURFACE ( 'NONE', #4374, 13.19999999999999929 ) ;
#7471=AXIS2_PLACEMENT_3D ( 'NONE', #17990, #19576, #16586 ) ;
#7477=ORIENTED_EDGE ( 'NONE', *, *, #879, .T. ) ;
#7482=CARTESIAN_POINT ( 'NONE',  ( 0.5279273381794611364, 3.461047254864636713, -26.82026385750174668 ) ) ;
#7484=ORIENTED_EDGE ( 'NONE', *, *, #10697, .F. ) ;
#7489=EDGE_CURVE ( 'NONE', #10072, #12340, #12227, .T. ) ;
#7503=EDGE_LOOP ( 'NONE', ( #16156, #5057, #3968, #1677 ) ) ;
#7504=DIRECTION ( 'NONE',  ( -1.000000000000000000, -0.000000000000000000, -0.000000000000000000 ) ) ;
#7507=CARTESIAN_POINT ( 'NONE',  ( -7.765813458258934317E-14, -24.22524813288764278, 2.133839912090720325 ) ) ;
#7512=DIRECTION ( 'NONE',  ( -1.000000000000000000, 0.000000000000000000, 0.000000000000000000 ) ) ;
#7516=CARTESIAN_POINT ( 'NONE',  ( 0.02436607992776411782, 22.71065055754465689, -9.836394144775473691 ) ) ;
#7519=CARTESIAN_POINT ( 'NONE',  ( 1.949486339718610296E-19, -22.37986894186666831, -9.514945144208986960 ) ) ;
#7521=CARTESIAN_POINT ( 'NONE',  ( 1.749999999999998002, 20.02152543075374069, -19.67366047555509212 ) ) ;
#7524=DIRECTION ( 'NONE',  ( 0.000000000000000000, 0.000000000000000000, 1.000000000000000000 ) ) ;
#7530=DIRECTION ( 'NONE',  ( -1.000000000000000000, -0.000000000000000000, -0.000000000000000000 ) ) ;
#7538=ORIENTED_EDGE ( 'NONE', *, *, #1846, .T. ) ;
#7540=CARTESIAN_POINT ( 'NONE',  ( 2.257825459230522913, -4.993157874727630841, -26.58873630738057159 ) ) ;
#7542=ORIENTED_EDGE ( 'NONE', *, *, #6295, .T. ) ;
#7545=TOROIDAL_SURFACE ( 'NONE', #1492, 24.12539914357697413, 8.000000000000000000 ) ;
#7549=ORIENTED_EDGE ( 'NONE', *, *, #17414, .T. ) ;
#7550=DIRECTION ( 'NONE',  ( 0.000000000000000000, 0.000000000000000000, 1.000000000000000000 ) ) ;
#7557=VECTOR ( 'NONE', #11989, 1000.000000000000000 ) ;
#7565=CARTESIAN_POINT ( 'NONE',  ( 2.790000000000000480, 15.96500990068124715, 18.34424029220116736 ) ) ;
#7566=ORIENTED_EDGE ( 'NONE', *, *, #4028, .F. ) ;
#7568=DIRECTION ( 'NONE',  ( -1.000000000000000000, 0.000000000000000000, -0.000000000000000000 ) ) ;
#7578=CARTESIAN_POINT ( 'NONE',  ( 2.783068945535914551, -24.42321038836784197, 2.248820353272884542 ) ) ;
#7583=CARTESIAN_POINT ( 'NONE',  ( 1.039999999999995595, 20.02152543075345648, 19.67366047555537278 ) ) ;
#7586=AXIS2_PLACEMENT_3D ( 'NONE', #8684, #16496, #14794 ) ;
#7588=( NAMED_UNIT ( * ) SI_UNIT ( $, .STERADIAN. ) SOLID_ANGLE_UNIT ( ) );
#7590=AXIS2_PLACEMENT_3D ( 'NONE', #9016, #1416, #5998 ) ;
#7601=CARTESIAN_POINT ( 'NONE',  ( 2.765633920072238627, 5.391175441198956086, -24.15498966839956907 ) ) ;
#7608=B_SPLINE_CURVE_WITH_KNOTS ( 'NONE', 3,
 ( #17334, #3625, #12736, #9944, #3821, #5117 ),
 .UNSPECIFIED., .F., .F.,
 ( 4, 2, 4 ),
 ( 4.462636793130641501E-07, 0.001879885123570645879, 0.003759323983461978699 ),
 .UNSPECIFIED. ) ;
#7611=ORIENTED_EDGE ( 'NONE', *, *, #9703, .F. ) ;
#7613=EDGE_CURVE ( 'NONE', #5363, #1292, #4964, .T. ) ;
#7615=ORIENTED_EDGE ( 'NONE', *, *, #4623, .F. ) ;
#7616=CARTESIAN_POINT ( 'NONE',  ( 2.789999999999999147, -7.334849878007332791, -23.31896751603339979 ) ) ;
#7623=DIRECTION ( 'NONE',  ( 0.000000000000000000, 0.000000000000000000, 1.000000000000000000 ) ) ;
#7624=DIRECTION ( 'NONE',  ( -1.000000000000000000, 0.000000000000000000, -0.000000000000000000 ) ) ;
#7626=PRODUCT_DEFINITION_FORMATION_WITH_SPECIFIED_SOURCE ( 'ANY', '', #9709, .NOT_KNOWN. ) ;
#7632=EDGE_CURVE ( 'NONE', #16071, #14651, #17089, .T. ) ;
#7634=CARTESIAN_POINT ( 'NONE',  ( 2.030753605846574494, 3.797885586973597682, -27.31305418910206129 ) ) ;
#7637=CARTESIAN_POINT ( 'NONE',  ( 2.789999999999999147, 22.25075486061751207, -9.324097380959219805 ) ) ;
#7641=ORIENTED_EDGE ( 'NONE', *, *, #8935, .F. ) ;
#7645=DIRECTION ( 'NONE',  ( -1.000000000000000000, -0.000000000000000000, -0.000000000000000000 ) ) ;
#7649=CARTESIAN_POINT ( 'NONE',  ( 1.394999999999998685, 27.68468304288265358, -4.633866840648637186 ) ) ;
#7650=DIRECTION ( 'NONE',  ( -1.000000000000000000, -0.000000000000000000, -0.000000000000000000 ) ) ;
#7652=ORIENTED_EDGE ( 'NONE', *, *, #12307, .F. ) ;
#7661=ORIENTED_EDGE ( 'NONE', *, *, #6949, .F. ) ;
#7662=B_SPLINE_CURVE_WITH_KNOTS ( 'NONE', 3,
 ( #17869, #7946, #1463, #55, #10862, #255 ),
 .UNSPECIFIED., .F., .F.,
 ( 4, 2, 4 ),
 ( 4.462636808949230078E-07, 0.001879885123572232067, 0.003759323983463569441 ),
 .UNSPECIFIED. ) ;
#7663=CARTESIAN_POINT ( 'NONE',  ( 0.1855655959470664251, -17.45907811351468553, 19.17825124759772493 ) ) ;
#7667=DIRECTION ( 'NONE',  ( 0.000000000000000000, 6.870191984066573782E-16, -1.000000000000000000 ) ) ;
#7671=B_SPLINE_CURVE_WITH_KNOTS ( 'NONE', 3,
 ( #18179, #12074, #1069, #4166, #10380, #1168 ),
 .UNSPECIFIED., .F., .F.,
 ( 4, 2, 4 ),
 ( 1.979325885420574018E-07, 0.001878588715165606469, 0.003756979497742670565 ),
 .UNSPECIFIED. ) ;
#7672=CARTESIAN_POINT ( 'NONE',  ( 0.000000000000000000, -12.52067188844364587, 20.62201879784910119 ) ) ;
#7673=EDGE_LOOP ( 'NONE', ( #19372, #10560, #4575, #13926 ) ) ;
#7684=CARTESIAN_POINT ( 'NONE',  ( 1.749999999999998002, -27.76164181293054511, 4.147968289691195132 ) ) ;
#7685=DIRECTION ( 'NONE',  ( 0.000000000000000000, 0.000000000000000000, 1.000000000000000000 ) ) ;
#7686=VERTEX_POINT ( 'NONE', #15192 ) ;
#7689=CARTESIAN_POINT ( 'NONE',  ( 1.394999999999999574, -24.89775460606841406, 12.96210679857778025 ) ) ;
#7692=CARTESIAN_POINT ( 'NONE',  ( 2.789999999999999147, -24.04302995059964587, -1.991882183130548878 ) ) ;
#7693=AXIS2_PLACEMENT_3D ( 'NONE', #15152, #10554, #10751 ) ;
#7699=CARTESIAN_POINT ( 'NONE',  ( 0.02436607992776238310, -12.59161484032927092, 21.30679549418627161 ) ) ;
#7703=FACE_OUTER_BOUND ( 'NONE', #8586, .T. ) ;
#7713=DIRECTION ( 'NONE',  ( 1.000000000000000000, -0.000000000000000000, 0.000000000000000000 ) ) ;
#7716=FACE_OUTER_BOUND ( 'NONE', #8750, .T. ) ;
#7717=VERTEX_POINT ( 'NONE', #9693 ) ;
#7725=DIRECTION ( 'NONE',  ( -1.000000000000000000, -0.000000000000000000, 0.000000000000000000 ) ) ;
#7731=EDGE_CURVE ( 'NONE', #9581, #9713, #18599, .T. ) ;
#7736=ORIENTED_EDGE ( 'NONE', *, *, #7227, .T. ) ;
#7738=CARTESIAN_POINT ( 'NONE',  ( 2.601776091974071115, 25.40949241676360515, -5.251266773802107934 ) ) ;
#7746=ORIENTED_EDGE ( 'NONE', *, *, #16534, .T. ) ;
#7748=CARTESIAN_POINT ( 'NONE',  ( 1.749999999999998002, 12.96210679857822257, -24.89775460606818669 ) ) ;
#7751=AXIS2_PLACEMENT_3D ( 'NONE', #11376, #14376, #14766 ) ;
#7759=DIRECTION ( 'NONE',  ( -1.000000000000000000, 0.000000000000000000, 0.000000000000000000 ) ) ;
#7762=CIRCLE ( 'NONE', #19371, 24.12539914357697768 ) ;
#7763=DIRECTION ( 'NONE',  ( 0.000000000000000000, 0.000000000000000000, 1.000000000000000000 ) ) ;
#7769=CARTESIAN_POINT ( 'NONE',  ( 0.5279272933715191130, -18.56460150496952366, 19.66369668717026897 ) ) ;
#7787=AXIS2_PLACEMENT_3D ( 'NONE', #8342, #9274, #6722 ) ;
#7789=FACE_OUTER_BOUND ( 'NONE', #12328, .T. ) ;
#7799=DIRECTION ( 'NONE',  ( 0.000000000000000000, 0.000000000000000000, -1.000000000000000000 ) ) ;
#7801=CARTESIAN_POINT ( 'NONE',  ( 0.02436607992775674525, 9.836394144776026138, -22.71065055754441531 ) ) ;
#7803=EDGE_CURVE ( 'NONE', #16718, #11385, #4509, .T. ) ;
#7804=ORIENTED_EDGE ( 'NONE', *, *, #5407, .F. ) ;
#7807=FACE_OUTER_BOUND ( 'NONE', #395, .T. ) ;
#7818=EDGE_CURVE ( 'NONE', #5672, #17130, #2915, .T. ) ;
#7821=EDGE_CURVE ( 'NONE', #4759, #7944, #3670, .T. ) ;
#7832=DIRECTION ( 'NONE',  ( 0.000000000000000000, 0.000000000000000000, 1.000000000000000000 ) ) ;
#7833=DIRECTION ( 'NONE',  ( -1.000000000000000000, -0.000000000000000000, -0.000000000000000000 ) ) ;
#7835=TOROIDAL_SURFACE ( 'NONE', #519, 24.12539914357697413, 8.000000000000000000 ) ;
#7844=FACE_OUTER_BOUND ( 'NONE', #8339, .T. ) ;
#7846=ORIENTED_EDGE ( 'NONE', *, *, #13962, .F. ) ;
#7847=CARTESIAN_POINT ( 'NONE',  ( 0.7589665349472715095, 27.14933624560914893, -4.828387785247743480 ) ) ;
#7849=ORIENTED_EDGE ( 'NONE', *, *, #17638, .T. ) ;
#7850=ADVANCED_FACE ( 'NONE', ( #14384 ), #680, .F. ) ;
#7851=EDGE_CURVE ( 'NONE', #17509, #7960, #6489, .T. ) ;
#7853=CARTESIAN_POINT ( 'NONE',  ( 1.039999999999997593, 0.000000000000000000, 0.000000000000000000 ) ) ;
#7858=CARTESIAN_POINT ( 'NONE',  ( 1.039999999999996039, 27.68468304288258963, 4.633866840649018215 ) ) ;
#7859=AXIS2_PLACEMENT_3D ( 'NONE', #3295, #1793, #7885 ) ;
#7863=FACE_OUTER_BOUND ( 'NONE', #12012, .T. ) ;
#7865=EDGE_LOOP ( 'NONE', ( #4861, #12948, #19515, #18277 ) ) ;
#7879=CARTESIAN_POINT ( 'NONE',  ( 0.02436607992776325046, -18.55949924794904504, 16.37294372382852004 ) ) ;
#7885=DIRECTION ( 'NONE',  ( 0.000000000000000000, 0.000000000000000000, 1.000000000000000000 ) ) ;
#7888=DIRECTION ( 'NONE',  ( 0.000000000000000000, 0.000000000000000000, 1.000000000000000000 ) ) ;
#7889=ORIENTED_EDGE ( 'NONE', *, *, #16802, .T. ) ;
#7896=ORIENTED_EDGE ( 'NONE', *, *, #9623, .T. ) ;
#7897=DIRECTION ( 'NONE',  ( 0.000000000000000000, 0.000000000000000000, 1.000000000000000000 ) ) ;
#7903=EDGE_CURVE ( 'NONE', #17130, #9276, #12218, .T. ) ;
#7906=FACE_OUTER_BOUND ( 'NONE', #11724, .T. ) ;
#7909=CARTESIAN_POINT ( 'NONE',  ( 0.000000000000000000, 18.28042085475278000, 15.74360496233386719 ) ) ;
#7913=CARTESIAN_POINT ( 'NONE',  ( 2.789999999999999147, 7.909232158574813099, 24.34211360614303388 ) ) ;
#7914=ORIENTED_EDGE ( 'NONE', *, *, #15222, .F. ) ;
#7916=CARTESIAN_POINT ( 'NONE',  ( 2.718131914667132776, -23.19485392143220182, 10.24630254990507083 ) ) ;
#7917=ORIENTED_EDGE ( 'NONE', *, *, #5218, .F. ) ;
#7929=B_SPLINE_CURVE_WITH_KNOTS ( 'NONE', 3,
 ( #6647, #17377, #3662, #9787, #15879, #16743 ),
 .UNSPECIFIED., .F., .F.,
 ( 4, 2, 4 ),
 ( 4.462636695690012598E-07, 0.001879885036799766119, 0.003759323809929963553 ),
 .UNSPECIFIED. ) ;
#7930=FACE_OUTER_BOUND ( 'NONE', #4361, .T. ) ;
#7932=VECTOR ( 'NONE', #16874, 1000.000000000000000 ) ;
#7938=DIRECTION ( 'NONE',  ( -1.000000000000000000, 0.000000000000000000, 0.000000000000000000 ) ) ;
#7939=ORIENTED_EDGE ( 'NONE', *, *, #9972, .T. ) ;
#7941=CARTESIAN_POINT ( 'NONE',  ( 2.718131853594927261, 12.74240566899015903, -21.92302674874949986 ) ) ;
#7944=VERTEX_POINT ( 'NONE', #1240 ) ;
#7946=CARTESIAN_POINT ( 'NONE',  ( 0.7592463896980118365, -19.12676442129330212, -19.86438386685682644 ) ) ;
#7951=ADVANCED_FACE ( 'NONE', ( #16088 ), #10546, .F. ) ;
#7952=VERTEX_POINT ( 'NONE', #4440 ) ;
#7957=ORIENTED_EDGE ( 'NONE', *, *, #429, .F. ) ;
#7959=CARTESIAN_POINT ( 'NONE',  ( 8.000000000000000000, 0.000000000000000000, 0.000000000000000000 ) ) ;
#7960=VERTEX_POINT ( 'NONE', #19647 ) ;
#7966=B_SPLINE_CURVE_WITH_KNOTS ( 'NONE', 3,
 ( #3491, #291, #12499, #6372 ),
 .UNSPECIFIED., .F., .F.,
 ( 4, 4 ),
 ( 0.005258214619651976202, 0.005948481662034167325 ),
 .UNSPECIFIED. ) ;
#7968=EDGE_CURVE ( 'NONE', #8477, #16209, #15062, .T. ) ;
#7973=DIRECTION ( 'NONE',  ( 0.000000000000000000, 1.000000000000000000, 1.099230717450651647E-14 ) ) ;
#7980=AXIS2_PLACEMENT_3D ( 'NONE', #10347, #4133, #2620 ) ;
#7985=CARTESIAN_POINT ( 'NONE',  ( 1.824075699840007170, -24.74770846292491910, 12.96726489871182153 ) ) ;
#7987=CYLINDRICAL_SURFACE ( 'NONE', #12945, 13.19999999999999929 ) ;
#7990=CARTESIAN_POINT ( 'NONE',  ( 8.000000000000000000, 0.000000000000000000, 0.000000000000000000 ) ) ;
#7996=CARTESIAN_POINT ( 'NONE',  ( 2.789999999999999147, -23.48180575137734039, 5.535312321042630934 ) ) ;
#7998=CARTESIAN_POINT ( 'NONE',  ( 2.788134175425139194, -20.90825775245756191, -12.51925356660783528 ) ) ;
#8002=CARTESIAN_POINT ( 'NONE',  ( -10.00000000000000000, 0.000000000000000000, 0.000000000000000000 ) ) ;
#8006=VERTEX_POINT ( 'NONE', #10452 ) ;
#8014=VERTEX_POINT ( 'NONE', #8945 ) ;
#8015=CARTESIAN_POINT ( 'NONE',  ( 0.02436607992776411782, 22.71065055754465689, -9.836394144775473691 ) ) ;
#8017=FACE_OUTER_BOUND ( 'NONE', #141, .T. ) ;
#8019=ORIENTED_EDGE ( 'NONE', *, *, #6949, .T. ) ;
#8026=B_SPLINE_CURVE_WITH_KNOTS ( 'NONE', 3,
 ( #2058, #10974, #18471, #4966 ),
 .UNSPECIFIED., .F., .F.,
 ( 4, 4 ),
 ( 3.059063720746923042E-07, 0.0006888942284913959508 ),
 .UNSPECIFIED. ) ;
#8028=CARTESIAN_POINT ( 'NONE',  ( 1.394999999999998685, 24.89775460606832524, 12.96210679857795256 ) ) ;
#8040=TOROIDAL_SURFACE ( 'NONE', #2928, 24.12539914357697768, 8.000000000000000000 ) ;
#8065=FACE_OUTER_BOUND ( 'NONE', #13725, .T. ) ;
#8069=CARTESIAN_POINT ( 'NONE',  ( 2.765633920072239071, -16.37294372382844543, -18.55949924794910544 ) ) ;
#8080=CARTESIAN_POINT ( 'NONE',  ( 1.394999999999999574, -12.96210679857803960, 24.89775460606827551 ) ) ;
#8082=DIRECTION ( 'NONE',  ( 0.000000000000000000, -6.870191984066573782E-16, -1.000000000000000000 ) ) ;
#8084=ORIENTED_EDGE ( 'NONE', *, *, #11353, .T. ) ;
#8096=LINE ( 'NONE', #12319, #12051 ) ;
#8098=EDGE_LOOP ( 'NONE', ( #11464, #19061, #10051, #12656 ) ) ;
#8101=DIRECTION ( 'NONE',  ( 0.000000000000000000, 0.000000000000000000, 1.000000000000000000 ) ) ;
#8105=ADVANCED_FACE ( 'NONE', ( #1738 ), #1927, .T. ) ;
#8108=CIRCLE ( 'NONE', #19283, 2.524999999999995914 ) ;
#8110=CARTESIAN_POINT ( 'NONE',  ( 2.765633920072238183, -18.55949924794904504, 16.37294372382852004 ) ) ;
#8113=CIRCLE ( 'NONE', #4607, 28.06981291497571362 ) ;
#8123=EDGE_CURVE ( 'NONE', #4347, #18719, #8171, .T. ) ;
#8135=AXIS2_PLACEMENT_3D ( 'NONE', #5212, #9632, #14120 ) ;
#8145=EDGE_CURVE ( 'NONE', #3050, #5656, #18660, .T. ) ;
#8149=CARTESIAN_POINT ( 'NONE',  ( 0.000000000000000000, -15.74360496233395956, 18.28042085475273026 ) ) ;
#8150=ADVANCED_FACE ( 'NONE', ( #15742 ), #16950, .T. ) ;
#8157=EDGE_CURVE ( 'NONE', #7944, #19214, #12715, .T. ) ;
#8162=LINE ( 'NONE', #262, #4767 ) ;
#8166=DIRECTION ( 'NONE',  ( -1.000000000000000000, 0.000000000000000000, 0.000000000000000000 ) ) ;
#8169=ORIENTED_EDGE ( 'NONE', *, *, #12035, .T. ) ;
#8170=ORIENTED_EDGE ( 'NONE', *, *, #12460, .T. ) ;
#8171=B_SPLINE_CURVE_WITH_KNOTS ( 'NONE', 3,
 ( #331, #12643, #12347, #6410, #18440, #4636 ),
 .UNSPECIFIED., .F., .F.,
 ( 4, 2, 4 ),
 ( 0.0004963285629696456008, 0.002127826186449799806, 0.003759323809929954012 ),
 .UNSPECIFIED. ) ;
#8173=TOROIDAL_SURFACE ( 'NONE', #15849, 24.12539914357697768, 8.000000000000000000 ) ;
#8175=CARTESIAN_POINT ( 'NONE',  ( 1.394999999999999574, 12.96210679857786552, 24.89775460606837143 ) ) ;
#8179=CARTESIAN_POINT ( 'NONE',  ( -5.435144416706554624E-16, -9.514945144208892813, 22.37986894186668962 ) ) ;
#8188=LINE ( 'NONE', #694, #13309 ) ;
#8189=CARTESIAN_POINT ( 'NONE',  ( 1.039999999999996705, 19.67366047555530173, 20.02152543075352398 ) ) ;
#8190=EDGE_CURVE ( 'NONE', #9359, #7686, #14126, .T. ) ;
#8193=ORIENTED_EDGE ( 'NONE', *, *, #16891, .T. ) ;
#8201=VERTEX_POINT ( 'NONE', #2324 ) ;
#8202=CARTESIAN_POINT ( 'NONE',  ( 0.7592463977762147209, -4.828194074574546413, 27.14986936243572657 ) ) ;
#8209=CARTESIAN_POINT ( 'NONE',  ( 0.006931069955678739909, -16.17493693894892104, 18.43696893154752914 ) ) ;
#8220=EDGE_LOOP ( 'NONE', ( #9158, #12419, #3774, #18379, #2346, #13879 ) ) ;
#8226=CARTESIAN_POINT ( 'NONE',  ( 0.5279272304333944010, -11.57956866523235462, 24.43806413951671530 ) ) ;
#8227=CARTESIAN_POINT ( 'NONE',  ( 0.02436607992776541887, 12.59161484032942901, -21.30679549418617924 ) ) ;
#8233=DIRECTION ( 'NONE',  ( -1.000000000000000000, -0.000000000000000000, -0.000000000000000000 ) ) ;
#8235=VECTOR ( 'NONE', #8257, 1000.000000000000000 ) ;
#8237=EDGE_CURVE ( 'NONE', #9816, #18407, #8626, .T. ) ;
#8241=DIRECTION ( 'NONE',  ( -1.000000000000000000, 0.000000000000000000, 0.000000000000000000 ) ) ;
#8254=DIRECTION ( 'NONE',  ( 1.000000000000000000, 0.000000000000000000, 0.000000000000000000 ) ) ;
#8256=B_SPLINE_CURVE_WITH_KNOTS ( 'NONE', 3,
 ( #4549, #5845, #16468, #1455 ),
 .UNSPECIFIED., .F., .F.,
 ( 4, 4 ),
 ( 0.005258120783916788929, 0.005948386350302939385 ),
 .UNSPECIFIED. ) ;
#8257=DIRECTION ( 'NONE',  ( -1.000000000000000000, -0.000000000000000000, 0.000000000000000000 ) ) ;
#8261=CIRCLE ( 'NONE', #4428, 24.12539914357697413 ) ;
#8265=CARTESIAN_POINT ( 'NONE',  ( 2.718184757033984766, -16.91181672897746324, 18.89296398180185932 ) ) ;
#8280=EDGE_LOOP ( 'NONE', ( #15169, #2560, #375, #4654, #14592, #16995 ) ) ;
#8282=ADVANCED_FACE ( 'NONE', ( #8821 ), #2902, .T. ) ;
#8294=CARTESIAN_POINT ( 'NONE',  ( 0.006974771092478172958, -9.686319561460797090, -22.53337530003413747 ) ) ;
#8299=ORIENTED_EDGE ( 'NONE', *, *, #162, .T. ) ;
#8311=DIRECTION ( 'NONE',  ( 0.000000000000000000, 0.000000000000000000, 1.000000000000000000 ) ) ;
#8314=CARTESIAN_POINT ( 'NONE',  ( 1.749999999999998002, -27.68468304288255766, -4.633866840649213614 ) ) ;
#8320=VERTEX_POINT ( 'NONE', #10621 ) ;
#8330=CARTESIAN_POINT ( 'NONE',  ( 2.789999999999999147, -23.17675759782035172, -7.772527002114682837 ) ) ;
#8332=ORIENTED_EDGE ( 'NONE', *, *, #879, .F. ) ;
#8334=ADVANCED_FACE ( 'NONE', ( #113 ), #15520, .T. ) ;
#8335=CIRCLE ( 'NONE', #8657, 24.12539914357697413 ) ;
#8337=LINE ( 'NONE', #4837, #1957 ) ;
#8339=EDGE_LOOP ( 'NONE', ( #10831, #8922, #12824, #12446 ) ) ;
#8342=CARTESIAN_POINT ( 'NONE',  ( -5.209999999999999964, 0.000000000000000000, 0.000000000000000000 ) ) ;
#8349=DIRECTION ( 'NONE',  ( 0.000000000000000000, 0.000000000000000000, 1.000000000000000000 ) ) ;
#8373=ORIENTED_EDGE ( 'NONE', *, *, #12078, .T. ) ;
#8375=EDGE_CURVE ( 'NONE', #6790, #619, #11212, .T. ) ;
#8377=AXIS2_PLACEMENT_3D ( 'NONE', #19111, #5403, #16125 ) ;
#8378=DIRECTION ( 'NONE',  ( -1.000000000000000000, -0.000000000000000000, 0.000000000000000000 ) ) ;
#8382=AXIS2_PLACEMENT_3D ( 'NONE', #14308, #3503, #806 ) ;
#8386=AXIS2_PLACEMENT_3D ( 'NONE', #17594, #17791, #3882 ) ;
#8388=CARTESIAN_POINT ( 'NONE',  ( 0.02436607992776151574, -18.55949924794880346, -16.37294372382878649 ) ) ;
#8397=ORIENTED_EDGE ( 'NONE', *, *, #6001, .T. ) ;
#8410=CARTESIAN_POINT ( 'NONE',  ( 0.5321745326902588280, 26.83036154824994668, -3.467596033028380376 ) ) ;
#8413=CARTESIAN_POINT ( 'NONE',  ( 2.789999999999999147, -24.63872515616084513, 2.336989772644183283 ) ) ;
#8414=ADVANCED_FACE ( 'NONE', ( #6980 ), #14415, .T. ) ;
#8416=CIRCLE ( 'NONE', #19586, 28.06981291497571007 ) ;
#8417=VECTOR ( 'NONE', #11498, 1000.000000000000000 ) ;
#8423=DIRECTION ( 'NONE',  ( -1.000000000000000000, 0.000000000000000000, 0.000000000000000000 ) ) ;
#8429=VERTEX_POINT ( 'NONE', #11504 ) ;
#8436=B_SPLINE_CURVE_WITH_KNOTS ( 'NONE', 3,
 ( #12585, #6355, #16796, #4580, #13983, #3375 ),
 .UNSPECIFIED., .F., .F.,
 ( 4, 2, 4 ),
 ( 1.979325885420663486E-07, 0.001878588715165612974, 0.003756979497742683576 ),
 .UNSPECIFIED. ) ;
#8442=B_SPLINE_CURVE_WITH_KNOTS ( 'NONE', 3,
 ( #9220, #1608, #18226, #7601 ),
 .UNSPECIFIED., .F., .F.,
 ( 4, 4 ),
 ( 0.005258214619651957987, 0.005948481662034167325 ),
 .UNSPECIFIED. ) ;
#8446=EDGE_CURVE ( 'NONE', #9696, #9010, #17957, .T. ) ;
#8451=AXIS2_PLACEMENT_3D ( 'NONE', #19, #10439, #12334 ) ;
#8456=CARTESIAN_POINT ( 'NONE',  ( 2.601776144743014996, -23.64332819722373813, -10.68696068830432466 ) ) ;
#8460=CARTESIAN_POINT ( 'NONE',  ( 0.6180618139040615633, -23.93436800624301242, 12.96259772325168314 ) ) ;
#8461=FACE_OUTER_BOUND ( 'NONE', #6735, .T. ) ;
#8466=CIRCLE ( 'NONE', #9745, 2.524999999999996358 ) ;
#8471=ORIENTED_EDGE ( 'NONE', *, *, #11689, .T. ) ;
#8475=EDGE_CURVE ( 'NONE', #1120, #14880, #11797, .T. ) ;
#8477=VERTEX_POINT ( 'NONE', #13391 ) ;
#8484=ORIENTED_EDGE ( 'NONE', *, *, #11969, .T. ) ;
#8486=EDGE_CURVE ( 'NONE', #2766, #12340, #11505, .T. ) ;
#8490=EDGE_CURVE ( 'NONE', #12340, #15059, #5584, .T. ) ;
#8497=DIRECTION ( 'NONE',  ( -1.000000000000000000, -0.000000000000000000, 0.000000000000000000 ) ) ;
#8499=ORIENTED_EDGE ( 'NONE', *, *, #16475, .F. ) ;
#8523=ORIENTED_EDGE ( 'NONE', *, *, #9282, .T. ) ;
#8526=DIRECTION ( 'NONE',  ( 0.000000000000000000, 0.000000000000000000, 1.000000000000000000 ) ) ;
#8533=AXIS2_PLACEMENT_3D ( 'NONE', #3169, #9279, #4675 ) ;
#8534=EDGE_CURVE ( 'NONE', #12283, #8429, #16257, .T. ) ;
#8536=FACE_OUTER_BOUND ( 'NONE', #10028, .T. ) ;
#8539=B_SPLINE_CURVE_WITH_KNOTS ( 'NONE', 3,
 ( #9809, #2381, #14791, #15901 ),
 .UNSPECIFIED., .F., .F.,
 ( 4, 4 ),
 ( 2.135345996173297489E-07, 0.0006888010880210770339 ),
 .UNSPECIFIED. ) ;
#8545=ORIENTED_EDGE ( 'NONE', *, *, #17565, .T. ) ;
#8547=CARTESIAN_POINT ( 'NONE',  ( 1.749999999999998002, -25.12109765559643648, -12.52377138324252570 ) ) ;
#8548=DIRECTION ( 'NONE',  ( -1.000000000000000000, -0.000000000000000000, -0.000000000000000000 ) ) ;
#8559=CARTESIAN_POINT ( 'NONE',  ( 2.601776105308174269, 25.78859396478527799, 2.857713464478781162 ) ) ;
#8571=LINE ( 'NONE', #6759, #13600 ) ;
#8573=LINE ( 'NONE', #19467, #2611 ) ;
#8575=ADVANCED_FACE ( 'NONE', ( #19488 ), #2580, .T. ) ;
#8580=CARTESIAN_POINT ( 'NONE',  ( 0.001865824574860882289, 20.90825775245787455, -12.51925356660738053 ) ) ;
#8581=CARTESIAN_POINT ( 'NONE',  ( 2.718184743034447237, -24.78695292654925808, 5.344212458769271201 ) ) ;
#8585=CARTESIAN_POINT ( 'NONE',  ( 2.789999999999999147, -12.52067188844336165, -20.62201879784926462 ) ) ;
#8586=EDGE_LOOP ( 'NONE', ( #10724, #14001, #10235, #2849, #7896, #2931 ) ) ;
#8590=DIRECTION ( 'NONE',  ( 0.000000000000000000, 0.000000000000000000, 1.000000000000000000 ) ) ;
#8596=EDGE_CURVE ( 'NONE', #18489, #9581, #4848, .T. ) ;
#8601=ORIENTED_EDGE ( 'NONE', *, *, #3552, .T. ) ;
#8605=CARTESIAN_POINT ( 'NONE',  ( -5.209999999999999964, 0.000000000000000000, 0.000000000000000000 ) ) ;
#8610=ADVANCED_FACE ( 'NONE', ( #19465 ), #12489, .F. ) ;
#8611=CARTESIAN_POINT ( 'NONE',  ( 0.000000000000000000, 2.680914349914567470E-13, -25.59481291497571220 ) ) ;
#8614=ORIENTED_EDGE ( 'NONE', *, *, #2854, .T. ) ;
#8615=CARTESIAN_POINT ( 'NONE',  ( 0.02436607992776455150, 21.30679549418631780, 12.59161484032919986 ) ) ;
#8617=FACE_OUTER_BOUND ( 'NONE', #16078, .T. ) ;
#8620=ORIENTED_EDGE ( 'NONE', *, *, #12769, .F. ) ;
#8621=CARTESIAN_POINT ( 'NONE',  ( 2.257825462012206685, 12.96514671151767395, 23.74442027961364943 ) ) ;
#8626=B_SPLINE_CURVE_WITH_KNOTS ( 'NONE', 3,
 ( #16430, #7196, #8920, #15023, #9018, #2704 ),
 .UNSPECIFIED., .F., .F.,
 ( 4, 2, 4 ),
 ( 2.321268216997094965E-07, 0.001878622960950493588, 0.003757013795079287150 ),
 .UNSPECIFIED. ) ;
#8627=ORIENTED_EDGE ( 'NONE', *, *, #892, .T. ) ;
#8636=DIRECTION ( 'NONE',  ( 0.000000000000000000, 0.000000000000000000, 1.000000000000000000 ) ) ;
#8640=DIRECTION ( 'NONE',  ( 0.000000000000000000, 0.9510565162951567508, -0.3090169943749379589 ) ) ;
#8643=VERTEX_POINT ( 'NONE', #376 ) ;
#8645=CARTESIAN_POINT ( 'NONE',  ( 1.039999999999997149, -24.89775460606822577, -12.96210679857813730 ) ) ;
#8647=EDGE_CURVE ( 'NONE', #10762, #10821, #18414, .T. ) ;
#8648=VERTEX_POINT ( 'NONE', #10987 ) ;
#8651=ORIENTED_EDGE ( 'NONE', *, *, #10749, .T. ) ;
#8652=EDGE_CURVE ( 'NONE', #9276, #12478, #16701, .T. ) ;
#8655=EDGE_LOOP ( 'NONE', ( #10174, #13317, #747, #14702 ) ) ;
#8656=CARTESIAN_POINT ( 'NONE',  ( 2.789999999999999147, -25.59481291497571220, -1.787276233276378314E-13 ) ) ;
#8657=AXIS2_PLACEMENT_3D ( 'NONE', #1296, #18013, #1496 ) ;
#8659=FACE_OUTER_BOUND ( 'NONE', #10430, .T. ) ;
#8666=DIRECTION ( 'NONE',  ( -1.000000000000000000, -0.000000000000000000, -0.000000000000000000 ) ) ;
#8667=ORIENTED_EDGE ( 'NONE', *, *, #7334, .T. ) ;
#8679=CARTESIAN_POINT ( 'NONE',  ( 2.789999999999999147, 14.55412442567645215, -19.64056340710859772 ) ) ;
#8682=CARTESIAN_POINT ( 'NONE',  ( 0.02436607992775761261, 22.71065055754452544, 9.836394144775786330 ) ) ;
#8684=CARTESIAN_POINT ( 'NONE',  ( 2.790000000000000924, 0.000000000000000000, 0.000000000000000000 ) ) ;
#8685=EDGE_CURVE ( 'NONE', #7717, #11676, #3571, .T. ) ;
#8687=CARTESIAN_POINT ( 'NONE',  ( 2.765633920072239516, -24.63872515616084513, 2.336989772644183283 ) ) ;
#8692=CARTESIAN_POINT ( 'NONE',  ( 1.749999999999998002, -12.52377138324241734, 25.12109765559649688 ) ) ;
#8694=CARTESIAN_POINT ( 'NONE',  ( 2.789999999999999147, 7.772527002114753003, -23.17675759782032685 ) ) ;
#8696=CARTESIAN_POINT ( 'NONE',  ( 2.765633920072237295, 12.59161484032912171, 21.30679549418635688 ) ) ;
#8697=ORIENTED_EDGE ( 'NONE', *, *, #9093, .F. ) ;
#8701=CARTESIAN_POINT ( 'NONE',  ( -5.209999999999999964, 0.000000000000000000, 0.000000000000000000 ) ) ;
#8706=DIRECTION ( 'NONE',  ( 0.000000000000000000, 0.000000000000000000, 1.000000000000000000 ) ) ;
#8707=TOROIDAL_SURFACE ( 'NONE', #741, 24.12539914357697413, 8.000000000000000000 ) ;
#8710=FACE_OUTER_BOUND ( 'NONE', #4627, .T. ) ;
#8713=CARTESIAN_POINT ( 'NONE',  ( 0.1855657389739094887, -5.253342437939553022, -25.39738473785006079 ) ) ;
#8715=CARTESIAN_POINT ( 'NONE',  ( 2.262072625383131363, 26.57710921259761960, 4.996265754456460151 ) ) ;
#8722=CLOSED_SHELL ( 'NONE', ( #18105, #2545, #17318, #6876, #10307, #4780, #10227, #12644, #15569, #7424, #2802, #5702, #11346, #19619, #18550, #10898, #1637, #10274, #11412, #1461, #18607, #13331, #638, #746, #1993, #6499, #19281, #13349, #6383, #244, #13426, #11299, #7397, #11165, #15868, #8908, #1739, #3761, #6130, #3315, #5849, #19122, #17776, #5693, #15820, #13971, #14827, #811, #12281, #15401, #16509, #7350, #10373, #17113, #18947, #17507, #9776, #19134, #18535, #4062, #2556, #10282, #7074, #19352, #17280, #4433, #16283, #11130, #10412, #12400, #17277, #19184, #9008, #12885, #16256, #1094, #18261, #6905, #7444, #1191, #3361, #938, #18252, #11716, #3023, #2069, #17292, #5685, #14547, #8334, #17002, #1078, #8575, #7850, #8282, #6553, #6494, #15275, #15336, #7951, #18870, #1625, #8610, #950, #3372, #14570, #5376, #7453, #15081, #2513, #8105, #13991, #26, #8414, #1376, #16138, #11127, #15297, #16163, #15213, #15485, #8150, #10131, #6587, #12596, #4871, #7240, #2443, #2351, #2601, #1801, #966, #9248 ) ) ;
#8726=DIRECTION ( 'NONE',  ( -1.000000000000000000, -0.000000000000000000, -0.000000000000000000 ) ) ;
#8728=ORIENTED_EDGE ( 'NONE', *, *, #1048, .F. ) ;
#8736=ORIENTED_EDGE ( 'NONE', *, *, #18220, .T. ) ;
#8737=CARTESIAN_POINT ( 'NONE',  ( 2.789999999999999147, -0.2301004812055740811, -24.44424927289185590 ) ) ;
#8738=ORIENTED_EDGE ( 'NONE', *, *, #12144, .F. ) ;
#8746=B_SPLINE_CURVE_WITH_KNOTS ( 'NONE', 3,
 ( #12953, #849, #3020, #16445, #14937, #2913 ),
 .UNSPECIFIED., .F., .F.,
 ( 4, 2, 4 ),
 ( 4.462636678184503380E-07, 0.001879885020955184395, 0.003759323778242550443 ),
 .UNSPECIFIED. ) ;
#8750=EDGE_LOOP ( 'NONE', ( #13870, #740, #15832, #16935, #19267, #7736 ) ) ;
#8756=DIRECTION ( 'NONE',  ( 0.000000000000000000, 0.000000000000000000, 1.000000000000000000 ) ) ;
#8766=VERTEX_POINT ( 'NONE', #683 ) ;
#8775=CARTESIAN_POINT ( 'NONE',  ( 0.02436607992776194942, -5.391175441198450713, -24.15498966839968276 ) ) ;
#8781=CARTESIAN_POINT ( 'NONE',  ( 2.783025228907523019, 9.686319561461266048, -22.53337530003393141 ) ) ;
#8784=DIRECTION ( 'NONE',  ( -1.000000000000000000, -0.000000000000000000, -0.000000000000000000 ) ) ;
#8787=ORIENTED_EDGE ( 'NONE', *, *, #4784, .F. ) ;
#8789=AXIS2_PLACEMENT_3D ( 'NONE', #5447, #1047, #6939 ) ;
#8795=ORIENTED_EDGE ( 'NONE', *, *, #2648, .T. ) ;
#8806=LINE ( 'NONE', #2788, #13213 ) ;
#8808=LINE ( 'NONE', #4203, #19374 ) ;
#8809=DIRECTION ( 'NONE',  ( 0.000000000000000000, 0.000000000000000000, 1.000000000000000000 ) ) ;
#8812=CARTESIAN_POINT ( 'NONE',  ( 2.789999999999999147, -12.52067188844365830, 20.62201879784908698 ) ) ;
#8816=DIRECTION ( 'NONE',  ( 0.000000000000000000, 0.000000000000000000, 1.000000000000000000 ) ) ;
#8819=AXIS2_PLACEMENT_3D ( 'NONE', #9223, #1612, #4713 ) ;
#8820=ORIENTED_EDGE ( 'NONE', *, *, #14554, .F. ) ;
#8821=FACE_OUTER_BOUND ( 'NONE', #13264, .T. ) ;
#8825=ORIENTED_EDGE ( 'NONE', *, *, #15331, .T. ) ;
#8830=VERTEX_POINT ( 'NONE', #10089 ) ;
#8832=CARTESIAN_POINT ( 'NONE',  ( 0.02436607992776411782, -24.63872515616084513, 2.336989772644183283 ) ) ;
#8837=DIRECTION ( 'NONE',  ( -1.000000000000000000, 0.000000000000000000, -0.000000000000000000 ) ) ;
#8839=CARTESIAN_POINT ( 'NONE',  ( 0.5279273381794601372, -26.82026385750175734, -3.461047254864539457 ) ) ;
#8856=DIRECTION ( 'NONE',  ( -0.000000000000000000, 0.000000000000000000, 1.000000000000000000 ) ) ;
#8858=DIRECTION ( 'NONE',  ( -1.000000000000000000, -0.000000000000000000, -0.000000000000000000 ) ) ;
#8865=VECTOR ( 'NONE', #10448, 1000.000000000000000 ) ;
#8871=ORIENTED_EDGE ( 'NONE', *, *, #8375, .T. ) ;
#8875=CARTESIAN_POINT ( 'NONE',  ( 9.603018496175287840E-16, -5.456805104200934231, -23.69843731927176123 ) ) ;
#8878=VECTOR ( 'NONE', #7725, 1000.000000000000000 ) ;
#8879=CARTESIAN_POINT ( 'NONE',  ( 2.790000000000076419, 9.515416771311512534, -22.38018801136466251 ) ) ;
#8880=CYLINDRICAL_SURFACE ( 'NONE', #9088, 2.524999999999995914 ) ;
#8883=DIRECTION ( 'NONE',  ( -1.000000000000000000, -0.000000000000000000, 0.000000000000000000 ) ) ;
#8885=CARTESIAN_POINT ( 'NONE',  ( 0.006974693931642682830, -16.17543236987975064, -18.43727551351049598 ) ) ;
#8908=ADVANCED_FACE ( 'NONE', ( #16482 ), #8971, .T. ) ;
#8911=CARTESIAN_POINT ( 'NONE',  ( 0.07186814640506923590, 12.74240566898984284, 21.92302674874967749 ) ) ;
#8912=ORIENTED_EDGE ( 'NONE', *, *, #1981, .F. ) ;
#8915=LINE ( 'NONE', #15417, #9344 ) ;
#8918=EDGE_CURVE ( 'NONE', #16209, #5291, #8573, .T. ) ;
#8920=CARTESIAN_POINT ( 'NONE',  ( 2.604434404052933694, 17.45907811351455408, 19.17825124759784572 ) ) ;
#8921=CARTESIAN_POINT ( 'NONE',  ( 2.789999999999999147, -15.74360496233368245, -18.28042085475295409 ) ) ;
#8922=ORIENTED_EDGE ( 'NONE', *, *, #7632, .T. ) ;
#8932=EDGE_CURVE ( 'NONE', #14603, #2736, #2938, .T. ) ;
#8935=EDGE_CURVE ( 'NONE', #1705, #993, #18079, .T. ) ;
#8938=AXIS2_PLACEMENT_3D ( 'NONE', #17402, #15903, #11860 ) ;
#8942=CARTESIAN_POINT ( 'NONE',  ( 1.749999999999998002, -4.147968289691484678, 27.76164181293050603 ) ) ;
#8945=CARTESIAN_POINT ( 'NONE',  ( 1.749999999999998002, 25.12109765559653596, 12.52377138324232675 ) ) ;
#8955=DIRECTION ( 'NONE',  ( -1.000000000000000000, -0.000000000000000000, -0.000000000000000000 ) ) ;
#8961=CARTESIAN_POINT ( 'NONE',  ( 1.749999999999998002, -4.633866840648726004, -27.68468304288263582 ) ) ;
#8965=VECTOR ( 'NONE', #10264, 1000.000000000000000 ) ;
#8971=CYLINDRICAL_SURFACE ( 'NONE', #19238, 28.06981291497571362 ) ;
#8972=CARTESIAN_POINT ( 'NONE',  ( 0.000000000000000000, 0.000000000000000000, 0.000000000000000000 ) ) ;
#8984=CARTESIAN_POINT ( 'NONE',  ( 0.9659243001600011924, 24.74770846292485516, 12.96726489871199028 ) ) ;
#8991=CARTESIAN_POINT ( 'NONE',  ( 1.039999999999996483, -27.76164181293054511, 4.147968289691193355 ) ) ;
#8994=CARTESIAN_POINT ( 'NONE',  ( 2.765633920072235519, -18.55949924794880346, -16.37294372382878649 ) ) ;
#8998=B_SPLINE_CURVE_WITH_KNOTS ( 'NONE', 3,
 ( #8388, #18991, #691, #6769, #12893, #5282 ),
 .UNSPECIFIED., .F., .F.,
 ( 4, 2, 4 ),
 ( 2.321268216997177022E-07, 0.001878622960950496190, 0.003757013795079292354 ),
 .UNSPECIFIED. ) ;
#9007=CARTESIAN_POINT ( 'NONE',  ( 1.039999999999996705, 19.67366047555530173, 20.02152543075352398 ) ) ;
#9008=ADVANCED_FACE ( 'NONE', ( #1565 ), #164, .T. ) ;
#9010=VERTEX_POINT ( 'NONE', #13873 ) ;
#9012=CARTESIAN_POINT ( 'NONE',  ( 2.790000000000000036, -20.65025570340076655, -12.51972505885016140 ) ) ;
#9016=CARTESIAN_POINT ( 'NONE',  ( 2.789999999999999147, 7.909232158575156824, -24.34211360614291664 ) ) ;
#9018=CARTESIAN_POINT ( 'NONE',  ( 2.031033479673589159, 19.12621924769867121, 19.86422722021319487 ) ) ;
#9029=CARTESIAN_POINT ( 'NONE',  ( 0.07186808533286681566, 23.19485392143213431, 10.24630254990524314 ) ) ;
#9032=CYLINDRICAL_SURFACE ( 'NONE', #14383, 13.19999999999999929 ) ;
#9036=ORIENTED_EDGE ( 'NONE', *, *, #7465, .T. ) ;
#9039=CARTESIAN_POINT ( 'NONE',  ( 1.039999999999994929, -25.12109765559662833, 12.52377138324214023 ) ) ;
#9043=ORIENTED_EDGE ( 'NONE', *, *, #14663, .T. ) ;
#9049=EDGE_CURVE ( 'NONE', #17165, #19497, #15406, .T. ) ;
#9066=VERTEX_POINT ( 'NONE', #9372 ) ;
#9070=CARTESIAN_POINT ( 'NONE',  ( 2.718131864678289933, -2.577209017046833583, -25.22589920183363787 ) ) ;
#9071=EDGE_LOOP ( 'NONE', ( #7538, #4933, #19684, #13761 ) ) ;
#9075=TOROIDAL_SURFACE ( 'NONE', #15459, 24.12539914357697413, 8.000000000000000000 ) ;
#9080=EDGE_CURVE ( 'NONE', #3395, #19037, #4544, .T. ) ;
#9085=ORIENTED_EDGE ( 'NONE', *, *, #13512, .F. ) ;
#9086=CARTESIAN_POINT ( 'NONE',  ( 1.749999999999998002, 0.000000000000000000, 0.000000000000000000 ) ) ;
#9088=AXIS2_PLACEMENT_3D ( 'NONE', #14981, #67, #4669 ) ;
#9091=CARTESIAN_POINT ( 'NONE',  ( 1.394999999999999574, 19.67366047555530528, 20.02152543075352753 ) ) ;
#9093=EDGE_CURVE ( 'NONE', #1584, #8643, #1682, .T. ) ;
#9096=ORIENTED_EDGE ( 'NONE', *, *, #1104, .T. ) ;
#9099=DIRECTION ( 'NONE',  ( -1.000000000000000000, -0.000000000000000000, -0.000000000000000000 ) ) ;
#9118=DIRECTION ( 'NONE',  ( -1.000000000000000000, -0.000000000000000000, -0.000000000000000000 ) ) ;
#9120=EDGE_LOOP ( 'NONE', ( #16837, #17978, #18380, #17729 ) ) ;
#9122=CARTESIAN_POINT ( 'NONE',  ( 2.765633920072235963, 21.30679549418649543, -12.59161484032888723 ) ) ;
#9127=DIRECTION ( 'NONE',  ( 0.000000000000000000, 0.8090169943749527803, -0.5877852522924655876 ) ) ;
#9129=ORIENTED_EDGE ( 'NONE', *, *, #14437, .F. ) ;
#9133=DIRECTION ( 'NONE',  ( -1.000000000000000000, -0.000000000000000000, 0.000000000000000000 ) ) ;
#9134=ORIENTED_EDGE ( 'NONE', *, *, #11621, .T. ) ;
#9137=VERTEX_POINT ( 'NONE', #18864 ) ;
#9138=B_SPLINE_CURVE_WITH_KNOTS ( 'NONE', 3,
 ( #4161, #10276, #15370, #13667 ),
 .UNSPECIFIED., .F., .F.,
 ( 4, 4 ),
 ( 0.005258139959819246867, 0.005948405594583413246 ),
 .UNSPECIFIED. ) ;
#9140=CIRCLE ( 'NONE', #16481, 28.06981291497571007 ) ;
#9144=CARTESIAN_POINT ( 'NONE',  ( 0.02436607992775934733, -2.336989772644440855, 24.63872515616082026 ) ) ;
#9146=CARTESIAN_POINT ( 'NONE',  ( 2.783069004973548921, -5.408431875071614492, 23.92277630352793238 ) ) ;
#9149=AXIS2_PLACEMENT_3D ( 'NONE', #4621, #12627, #14024 ) ;
#9150=ORIENTED_EDGE ( 'NONE', *, *, #14020, .F. ) ;
#9154=ORIENTED_EDGE ( 'NONE', *, *, #10260, .F. ) ;
#9155=CARTESIAN_POINT ( 'NONE',  ( 2.790000000000000036, 0.000000000000000000, 0.000000000000000000 ) ) ;
#9156=CARTESIAN_POINT ( 'NONE',  ( 1.960886852992497653, -24.44424927289185590, 12.96989951879399072 ) ) ;
#9158=ORIENTED_EDGE ( 'NONE', *, *, #9282, .F. ) ;
#9169=AXIS2_PLACEMENT_3D ( 'NONE', #18009, #4485, #18202 ) ;
#9170=ORIENTED_EDGE ( 'NONE', *, *, #17494, .F. ) ;
#9174=DIRECTION ( 'NONE',  ( -1.000000000000000000, -0.000000000000000000, -0.000000000000000000 ) ) ;
#9175=ORIENTED_EDGE ( 'NONE', *, *, #11867, .F. ) ;
#9176=AXIS2_PLACEMENT_3D ( 'NONE', #8737, #1033, #15778 ) ;
#9185=FACE_OUTER_BOUND ( 'NONE', #14557, .T. ) ;
#9190=CARTESIAN_POINT ( 'NONE',  ( 0.7592463941534255412, -27.31305418910211813, 3.797885586973120287 ) ) ;
#9192=EDGE_CURVE ( 'NONE', #8014, #6715, #19119, .T. ) ;
#9196=ORIENTED_EDGE ( 'NONE', *, *, #5425, .F. ) ;
#9205=DIRECTION ( 'NONE',  ( 0.000000000000000000, 0.000000000000000000, 1.000000000000000000 ) ) ;
#9208=AXIS2_PLACEMENT_3D ( 'NONE', #5673, #17793, #16295 ) ;
#9217=CYLINDRICAL_SURFACE ( 'NONE', #1512, 28.06981291497571362 ) ;
#9218=VERTEX_POINT ( 'NONE', #13061 ) ;
#9220=CARTESIAN_POINT ( 'NONE',  ( 2.789999999999999147, 5.535312321043049266, -23.48180575137724446 ) ) ;
#9223=CARTESIAN_POINT ( 'NONE',  ( 0.000000000000000000, -20.70663861606260170, -15.04425356660783031 ) ) ;
#9239=CARTESIAN_POINT ( 'NONE',  ( 2.790000000000076419, 2.133839912091138213, -24.22524813288759660 ) ) ;
#9242=CARTESIAN_POINT ( 'NONE',  ( 2.789999999999999147, -21.30679549418621832, -12.59161484032935618 ) ) ;
#9248=ADVANCED_FACE ( 'NONE', ( #14664 ), #17956, .F. ) ;
#9250=CARTESIAN_POINT ( 'NONE',  ( 0.000000000000000000, 7.909232158575156824, -24.34211360614291664 ) ) ;
#9256=B_SPLINE_CURVE_WITH_KNOTS ( 'NONE', 3,
 ( #11008, #9419, #6291, #7996 ),
 .UNSPECIFIED., .F., .F.,
 ( 4, 4 ),
 ( 1.981826382900813409E-07, 0.0006887856082032219702 ),
 .UNSPECIFIED. ) ;
#9259=CARTESIAN_POINT ( 'NONE',  ( 0.006974657972265168107, -5.408388659524262287, 23.92335783895635970 ) ) ;
#9269=AXIS2_PLACEMENT_3D ( 'NONE', #15139, #10351, #1628 ) ;
#9271=DIRECTION ( 'NONE',  ( -1.000000000000000000, -0.000000000000000000, -0.000000000000000000 ) ) ;
#9274=DIRECTION ( 'NONE',  ( -1.000000000000000000, -0.000000000000000000, -0.000000000000000000 ) ) ;
#9275=CARTESIAN_POINT ( 'NONE',  ( 0.006974693931641778172, 18.43727551351055283, -16.17543236987968669 ) ) ;
#9276=VERTEX_POINT ( 'NONE', #10359 ) ;
#9279=DIRECTION ( 'NONE',  ( -1.000000000000000000, -0.000000000000000000, -0.000000000000000000 ) ) ;
#9282=EDGE_CURVE ( 'NONE', #10204, #17548, #2147, .T. ) ;
#9286=DIRECTION ( 'NONE',  ( 0.000000000000000000, 0.000000000000000000, 1.000000000000000000 ) ) ;
#9290=ORIENTED_EDGE ( 'NONE', *, *, #4073, .F. ) ;
#9291=CARTESIAN_POINT ( 'NONE',  ( 1.749999999999998002, -27.68468304288255766, -4.633866840649213614 ) ) ;
#9293=TOROIDAL_SURFACE ( 'NONE', #6091, 24.12539914357697768, 8.000000000000000000 ) ;
#9303=CYLINDRICAL_SURFACE ( 'NONE', #6273, 13.19999999999999929 ) ;
#9304=SHAPE_REPRESENTATION_RELATIONSHIP ( 'NONE' , 'NONE' ,  #451, #2068 ) ;
#9305=DIRECTION ( 'NONE',  ( 1.000000000000000000, -0.000000000000000000, -0.000000000000000000 ) ) ;
#9307=ORIENTED_EDGE ( 'NONE', *, *, #4170, .F. ) ;
#9309=AXIS2_PLACEMENT_3D ( 'NONE', #17395, #16461, #19350 ) ;
#9310=DIRECTION ( 'NONE',  ( 0.000000000000000000, -1.374038396813314756E-15, -1.000000000000000000 ) ) ;
#9311=DIRECTION ( 'NONE',  ( -1.000000000000000000, 0.000000000000000000, -0.000000000000000000 ) ) ;
#9314=ORIENTED_EDGE ( 'NONE', *, *, #7334, .F. ) ;
#9315=DIRECTION ( 'NONE',  ( -1.000000000000000000, -0.000000000000000000, -0.000000000000000000 ) ) ;
#9317=ORIENTED_EDGE ( 'NONE', *, *, #9460, .T. ) ;
#9323=VECTOR ( 'NONE', #10305, 1000.000000000000000 ) ;
#9325=CARTESIAN_POINT ( 'NONE',  ( 2.789999999999999147, 15.04425356660790136, -18.18163861606255338 ) ) ;
#9329=EDGE_CURVE ( 'NONE', #17360, #569, #1188, .T. ) ;
#9331=CARTESIAN_POINT ( 'NONE',  ( 0.000000000000000000, -18.28042085475266632, -15.74360496233403239 ) ) ;
#9332=ORIENTED_EDGE ( 'NONE', *, *, #5459, .T. ) ;
#9337=CARTESIAN_POINT ( 'NONE',  ( 2.789999999999999147, 0.000000000000000000, 0.000000000000000000 ) ) ;
#9341=CARTESIAN_POINT ( 'NONE',  ( 0.8291131470075423504, 24.44424927289185945, 12.96989951879416125 ) ) ;
#9344=VECTOR ( 'NONE', #1606, 1000.000000000000000 ) ;
#9359=VERTEX_POINT ( 'NONE', #10454 ) ;
#9369=VERTEX_POINT ( 'NONE', #1340 ) ;
#9372=CARTESIAN_POINT ( 'NONE',  ( 0.000000000000000000, 15.04425356660790136, -18.18163861606255338 ) ) ;
#9376=AXIS2_PLACEMENT_3D ( 'NONE', #19336, #5626, #10613 ) ;
#9381=ORIENTED_EDGE ( 'NONE', *, *, #11018, .F. ) ;
#9384=CARTESIAN_POINT ( 'NONE',  ( 1.749999999999998002, -20.02152543075331081, -19.67366047555553266 ) ) ;
#9385=ORIENTED_EDGE ( 'NONE', *, *, #12390, .F. ) ;
#9387=CARTESIAN_POINT ( 'NONE',  ( 2.789999999999999147, 12.52067188844381107, -20.62201879784899461 ) ) ;
#9389=LINE ( 'NONE', #80, #5748 ) ;
#9390=AXIS2_PLACEMENT_3D ( 'NONE', #10117, #10027, #6795 ) ;
#9394=EDGE_LOOP ( 'NONE', ( #19157, #6153, #13221, #7804 ) ) ;
#9400=CARTESIAN_POINT ( 'NONE',  ( 2.765633920072235075, 24.63872515616082737, -2.336989772644355590 ) ) ;
#9401=EDGE_CURVE ( 'NONE', #17188, #5932, #6527, .T. ) ;
#9404=DIRECTION ( 'NONE',  ( -1.000000000000000000, -0.000000000000000000, -0.000000000000000000 ) ) ;
#9418=ORIENTED_EDGE ( 'NONE', *, *, #11042, .F. ) ;
#9419=CARTESIAN_POINT ( 'NONE',  ( 2.783025342027734439, -23.92335783895641299, 5.408388659523998498 ) ) ;
#9420=CARTESIAN_POINT ( 'NONE',  ( 2.789679245949062913, -20.70663861606260525, -12.51925356660783528 ) ) ;
#9426=EDGE_CURVE ( 'NONE', #6765, #13330, #4950, .T. ) ;
#9442=EDGE_CURVE ( 'NONE', #6035, #15913, #486, .T. ) ;
#9448=DIRECTION ( 'NONE',  ( 0.000000000000000000, 0.000000000000000000, -1.000000000000000000 ) ) ;
#9453=DIRECTION ( 'NONE',  ( -1.000000000000000000, 0.000000000000000000, 0.000000000000000000 ) ) ;
#9460=EDGE_CURVE ( 'NONE', #2982, #17056, #4762, .T. ) ;
#9468=CARTESIAN_POINT ( 'NONE',  ( 0.07186815222488118771, 24.78765742476146272, -5.344160105508446001 ) ) ;
#9472=ORIENTED_EDGE ( 'NONE', *, *, #14224, .T. ) ;
#9476=ORIENTED_EDGE ( 'NONE', *, *, #3198, .T. ) ;
#9478=CARTESIAN_POINT ( 'NONE',  ( 0.000000000000000000, -20.70663861606282197, 15.04425356660753188 ) ) ;
#9486=VERTEX_POINT ( 'NONE', #10112 ) ;
#9487=ORIENTED_EDGE ( 'NONE', *, *, #2767, .F. ) ;
#9490=CARTESIAN_POINT ( 'NONE',  ( 0.02436607992776325046, 16.37294372382858398, 18.55949924794898465 ) ) ;
#9497=VECTOR ( 'NONE', #1179, 1000.000000000000000 ) ;
#9506=CARTESIAN_POINT ( 'NONE',  ( 1.749999999999998002, -24.89775460606842117, 12.96210679857777137 ) ) ;
#9528=CARTESIAN_POINT ( 'NONE',  ( 1.960886852992457241, 24.44424927289185945, 12.96989951879416125 ) ) ;
#9529=ORIENTED_EDGE ( 'NONE', *, *, #12078, .F. ) ;
#9537=CARTESIAN_POINT ( 'NONE',  ( 2.765633920072238183, -5.391175441198789109, 24.15498966839961170 ) ) ;
#9538=EDGE_CURVE ( 'NONE', #3268, #3153, #15917, .T. ) ;
#9546=CARTESIAN_POINT ( 'NONE',  ( 2.789999999999999147, -20.70663861606260170, -12.51925356660783528 ) ) ;
#9549=CARTESIAN_POINT ( 'NONE',  ( 2.765633920072236407, 2.336989772644613161, -24.63872515616080250 ) ) ;
#9561=CARTESIAN_POINT ( 'NONE',  ( 0.000000000000000000, 23.48180575137739368, -5.535312321042471062 ) ) ;
#9564=ORIENTED_EDGE ( 'NONE', *, *, #16891, .F. ) ;
#9567=DIRECTION ( 'NONE',  ( 0.000000000000000000, 0.000000000000000000, 1.000000000000000000 ) ) ;
#9568=ORIENTED_EDGE ( 'NONE', *, *, #8145, .F. ) ;
#9572=ORIENTED_EDGE ( 'NONE', *, *, #7851, .T. ) ;
#9575=FACE_OUTER_BOUND ( 'NONE', #17898, .T. ) ;
#9580=ORIENTED_EDGE ( 'NONE', *, *, #5252, .T. ) ;
#9581=VERTEX_POINT ( 'NONE', #19599 ) ;
#9583=CARTESIAN_POINT ( 'NONE',  ( 2.718184745196086549, -12.74223776959184207, -21.92234060054359901 ) ) ;
#9585=DIRECTION ( 'NONE',  ( 0.000000000000000000, 0.000000000000000000, 1.000000000000000000 ) ) ;
#9593=DIRECTION ( 'NONE',  ( -1.000000000000000000, 0.000000000000000000, 0.000000000000000000 ) ) ;
#9596=B_SPLINE_CURVE_WITH_KNOTS ( 'NONE', 3,
 ( #1590, #4983, #6180, #15501, #17193, #7879 ),
 .UNSPECIFIED., .F., .F.,
 ( 4, 2, 4 ),
 ( 4.462636793144160676E-07, 0.001879885123570646096, 0.003759323983461977832 ),
 .UNSPECIFIED. ) ;
#9606=EDGE_LOOP ( 'NONE', ( #16234, #1792, #18139, #9134 ) ) ;
#9612=ORIENTED_EDGE ( 'NONE', *, *, #14569, .F. ) ;
#9617=ORIENTED_EDGE ( 'NONE', *, *, #11353, .F. ) ;
#9618=CARTESIAN_POINT ( 'NONE',  ( 2.789999999999999147, -14.55412442567604003, -19.64056340710890325 ) ) ;
#9623=EDGE_CURVE ( 'NONE', #10783, #3731, #11217, .T. ) ;
#9624=CARTESIAN_POINT ( 'NONE',  ( 1.039999999999996483, -12.96210679857803783, 24.89775460606827551 ) ) ;
#9627=VERTEX_POINT ( 'NONE', #9400 ) ;
#9630=CARTESIAN_POINT ( 'NONE',  ( 2.257825467309738876, -26.83036154824992536, -3.467596033028569114 ) ) ;
#9632=DIRECTION ( 'NONE',  ( -1.000000000000000000, -0.000000000000000000, -0.000000000000000000 ) ) ;
#9636=CARTESIAN_POINT ( 'NONE',  ( 2.783068888626319293, -22.53293026234510776, 9.685942809246967045 ) ) ;
#9637=ORIENTED_EDGE ( 'NONE', *, *, #7613, .T. ) ;
#9644=CARTESIAN_POINT ( 'NONE',  ( 2.789999999999999147, -20.62201879784921843, 12.52067188844344336 ) ) ;
#9657=ORIENTED_EDGE ( 'NONE', *, *, #1863, .T. ) ;
#9660=VERTEX_POINT ( 'NONE', #15399 ) ;
#9663=DIRECTION ( 'NONE',  ( -1.000000000000000000, 0.000000000000000000, 0.000000000000000000 ) ) ;
#9664=CARTESIAN_POINT ( 'NONE',  ( 2.789999999999999147, -19.91106274590524094, 14.18181402625735466 ) ) ;
#9667=CARTESIAN_POINT ( 'NONE',  ( 2.765633920072239516, -2.336989772644097574, -24.63872515616085224 ) ) ;
#9682=DIRECTION ( 'NONE',  ( 0.000000000000000000, 0.8090169943749400128, 0.5877852522924831291 ) ) ;
#9683=CARTESIAN_POINT ( 'NONE',  ( 0.1882239080259275332, 25.40949241676353410, 5.251266773802457877 ) ) ;
#9684=VERTEX_POINT ( 'NONE', #17192 ) ;
#9688=ORIENTED_EDGE ( 'NONE', *, *, #2465, .F. ) ;
#9691=CIRCLE ( 'NONE', #1366, 2.524999999999995914 ) ;
#9693=CARTESIAN_POINT ( 'NONE',  ( 0.000000000000000000, -23.48180575137727288, -5.535312321042949790 ) ) ;
#9694=AXIS2_PLACEMENT_3D ( 'NONE', #18447, #7833, #18255 ) ;
#9696=VERTEX_POINT ( 'NONE', #6079 ) ;
#9703=EDGE_CURVE ( 'NONE', #14603, #7952, #4318, .T. ) ;
#9709=PRODUCT ( 'short pitch roller chain wheel_s_iso_Chain wheel ISO - 20Z 05B-1 --20SA8.0N', 'short pitch roller chain wheel_s_iso_Chain wheel ISO - 20Z 05B-1 --20SA8.0N', '', ( #6426 ) ) ;
#9713=VERTEX_POINT ( 'NONE', #5467 ) ;
#9715=CARTESIAN_POINT ( 'NONE',  ( -7.682766964941417370E-14, -9.515416771311052457, -22.38018801136486502 ) ) ;
#9720=ORIENTED_EDGE ( 'NONE', *, *, #12742, .T. ) ;
#9721=CARTESIAN_POINT ( 'NONE',  ( -7.680503837993603605E-14, 23.69897269326676437, 5.456611084821939350 ) ) ;
#9731=DIRECTION ( 'NONE',  ( 0.000000000000000000, 0.000000000000000000, 1.000000000000000000 ) ) ;
#9735=AXIS2_PLACEMENT_3D ( 'NONE', #5669, #1178, #7058 ) ;
#9736=CARTESIAN_POINT ( 'NONE',  ( 1.394999999999999574, 27.76164181293051669, -4.147968289691385202 ) ) ;
#9740=LINE ( 'NONE', #13117, #5 ) ;
#9745=AXIS2_PLACEMENT_3D ( 'NONE', #419, #14425, #17226 ) ;
#9747=LINE ( 'NONE', #14435, #64 ) ;
#9751=CARTESIAN_POINT ( 'NONE',  ( 2.789999999999999147, 9.324097380959445402, 22.25075486061742325 ) ) ;
#9759=ORIENTED_EDGE ( 'NONE', *, *, #6001, .F. ) ;
#9760=CARTESIAN_POINT ( 'NONE',  ( 0.1855657168891852171, 22.53097606933003405, -12.84444904262000975 ) ) ;
#9769=CARTESIAN_POINT ( 'NONE',  ( 1.394999999999999574, 27.76164181293051669, 4.147968289691385202 ) ) ;
#9772=ORIENTED_EDGE ( 'NONE', *, *, #9442, .T. ) ;
#9773=CARTESIAN_POINT ( 'NONE',  ( 0.02436607992775934733, -21.30679549418640306, 12.59161484032904887 ) ) ;
#9774=CARTESIAN_POINT ( 'NONE',  ( 0.000000000000000000, -7.909232158574647009, -21.81711360614308148 ) ) ;
#9776=ADVANCED_FACE ( 'NONE', ( #882 ), #15507, .T. ) ;
#9781=AXIS2_PLACEMENT_3D ( 'NONE', #15942, #8233, #637 ) ;
#9784=EDGE_CURVE ( 'NONE', #8006, #10318, #17392, .T. ) ;
#9787=CARTESIAN_POINT ( 'NONE',  ( 0.1882239034349769691, -22.54313264455003463, -12.84621645676869939 ) ) ;
#9788=CARTESIAN_POINT ( 'NONE',  ( 1.039999999999997593, -24.89775460606841051, 12.96210679857778025 ) ) ;
#9789=ORIENTED_EDGE ( 'NONE', *, *, #12270, .F. ) ;
#9794=DIRECTION ( 'NONE',  ( -1.000000000000000000, -0.000000000000000000, -0.000000000000000000 ) ) ;
#9795=CARTESIAN_POINT ( 'NONE',  ( 0.07181525480391370841, -12.74223776959215826, 21.92234060054341427 ) ) ;
#9799=ORIENTED_EDGE ( 'NONE', *, *, #17074, .F. ) ;
#9803=TOROIDAL_SURFACE ( 'NONE', #3724, 24.12539914357697413, 8.000000000000000000 ) ;
#9804=CARTESIAN_POINT ( 'NONE',  ( 2.789999999999999147, -1.991882183130462503, 24.04302995059964942 ) ) ;
#9806=EDGE_CURVE ( 'NONE', #941, #15571, #5373, .T. ) ;
#9809=CARTESIAN_POINT ( 'NONE',  ( 0.02436607992776281678, 2.336989772644269436, 24.63872515616083447 ) ) ;
#9816=VERTEX_POINT ( 'NONE', #688 ) ;
#9817=EDGE_CURVE ( 'NONE', #12686, #7114, #6766, .T. ) ;
#9831=VERTEX_POINT ( 'NONE', #15792 ) ;
#9833=DIRECTION ( 'NONE',  ( 0.000000000000000000, 0.000000000000000000, 1.000000000000000000 ) ) ;
#9836=CIRCLE ( 'NONE', #19391, 28.06981291497571362 ) ;
#9838=ORIENTED_EDGE ( 'NONE', *, *, #4370, .T. ) ;
#9839=CARTESIAN_POINT ( 'NONE',  ( 0.02436607992776455150, 5.391175441198956086, -24.15498966839956907 ) ) ;
#9842=ORIENTED_EDGE ( 'NONE', *, *, #5159, .T. ) ;
#9843=APPLICATION_CONTEXT ( 'automotive_design' ) ;
#9846=DIRECTION ( 'NONE',  ( -1.000000000000000000, -0.000000000000000000, 0.000000000000000000 ) ) ;
#9853=EDGE_LOOP ( 'NONE', ( #623, #2553, #16628, #15986, #12069, #13558 ) ) ;
#9854=CIRCLE ( 'NONE', #13973, 28.06981291497571362 ) ;
#9855=EDGE_CURVE ( 'NONE', #19204, #4306, #13585, .T. ) ;
#9865=CARTESIAN_POINT ( 'NONE',  ( 0.000000000000000000, 12.52067188844379864, -20.62201879784900882 ) ) ;
#9867=ORIENTED_EDGE ( 'NONE', *, *, #10663, .F. ) ;
#9872=ORIENTED_EDGE ( 'NONE', *, *, #9426, .T. ) ;
#9874=CARTESIAN_POINT ( 'NONE',  ( 0.006930995026448713570, 5.408431875071442185, 23.92277630352796791 ) ) ;
#9877=ORIENTED_EDGE ( 'NONE', *, *, #14920, .T. ) ;
#9881=ORIENTED_EDGE ( 'NONE', *, *, #5736, .F. ) ;
#9883=EDGE_CURVE ( 'NONE', #17326, #1519, #323, .T. ) ;
#9886=ORIENTED_EDGE ( 'NONE', *, *, #607, .T. ) ;
#9890=ORIENTED_EDGE ( 'NONE', *, *, #17541, .T. ) ;
#9899=ORIENTED_EDGE ( 'NONE', *, *, #14085, .F. ) ;
#9903=EDGE_CURVE ( 'NONE', #14221, #1705, #16067, .T. ) ;
#9907=FACE_OUTER_BOUND ( 'NONE', #8098, .T. ) ;
#9914=CARTESIAN_POINT ( 'NONE',  ( 1.749999999999998002, 4.633866840648922292, 27.68468304288260384 ) ) ;
#9917=CARTESIAN_POINT ( 'NONE',  ( 0.02436607992776758727, 24.15498966839963302, 5.391175441198700291 ) ) ;
#9919=ORIENTED_EDGE ( 'NONE', *, *, #17579, .T. ) ;
#9928=CARTESIAN_POINT ( 'NONE',  ( 0.5321745407694753460, 4.993157874728185952, -26.58873630738046501 ) ) ;
#9937=ORIENTED_EDGE ( 'NONE', *, *, #222, .F. ) ;
#9944=CARTESIAN_POINT ( 'NONE',  ( 2.601776121706765199, 17.47009390565519382, -19.18368891937472043 ) ) ;
#9947=CARTESIAN_POINT ( 'NONE',  ( 0.02436607992775978102, 24.63872515616082737, 2.336989772644355146 ) ) ;
#9949=ORIENTED_EDGE ( 'NONE', *, *, #4420, .T. ) ;
#9960=DIRECTION ( 'NONE',  ( -1.000000000000000000, 0.000000000000000000, 0.000000000000000000 ) ) ;
#9964=CARTESIAN_POINT ( 'NONE',  ( 2.789999999999999147, 15.04425356660760293, 20.70663861606276868 ) ) ;
#9972=EDGE_CURVE ( 'NONE', #3395, #9359, #16797, .T. ) ;
#9973=ORIENTED_EDGE ( 'NONE', *, *, #8534, .F. ) ;
#9974=TOROIDAL_SURFACE ( 'NONE', #3887, 24.12539914357697413, 8.000000000000000000 ) ;
#9976=DIRECTION ( 'NONE',  ( -1.000000000000000000, -0.000000000000000000, -0.000000000000000000 ) ) ;
#9978=ORIENTED_EDGE ( 'NONE', *, *, #9401, .F. ) ;
#9983=ORIENTED_EDGE ( 'NONE', *, *, #14341, .F. ) ;
#9995=DIRECTION ( 'NONE',  ( 0.000000000000000000, 0.000000000000000000, 1.000000000000000000 ) ) ;
#9998=DIRECTION ( 'NONE',  ( 0.000000000000000000, 0.000000000000000000, 1.000000000000000000 ) ) ;
#10002=CARTESIAN_POINT ( 'NONE',  ( 0.000000000000000000, 20.70663861606293210, -15.04425356660737556 ) ) ;
#10017=EDGE_CURVE ( 'NONE', #11614, #1584, #948, .T. ) ;
#10021=TOROIDAL_SURFACE ( 'NONE', #16086, 24.12539914357697413, 8.000000000000000000 ) ;
#10022=EDGE_LOOP ( 'NONE', ( #9799, #14259, #11079, #11564, #12666, #3512 ) ) ;
#10026=CARTESIAN_POINT ( 'NONE',  ( 1.039999999999995373, 25.12109765559670649, -12.52377138324197681 ) ) ;
#10027=DIRECTION ( 'NONE',  ( -1.000000000000000000, -0.000000000000000000, -0.000000000000000000 ) ) ;
#10028=EDGE_LOOP ( 'NONE', ( #12493, #8825, #13934, #14011 ) ) ;
#10040=FACE_OUTER_BOUND ( 'NONE', #4805, .T. ) ;
#10050=CARTESIAN_POINT ( 'NONE',  ( 0.5321745227542316048, 19.66801664102731095, -18.57583492944399950 ) ) ;
#10051=ORIENTED_EDGE ( 'NONE', *, *, #16110, .F. ) ;
#10059=ORIENTED_EDGE ( 'NONE', *, *, #3486, .F. ) ;
#10060=CARTESIAN_POINT ( 'NONE',  ( 8.000000000000000000, 0.000000000000000000, 0.000000000000000000 ) ) ;
#10062=ORIENTED_EDGE ( 'NONE', *, *, #6095, .T. ) ;
#10072=VERTEX_POINT ( 'NONE', #8645 ) ;
#10085=DIRECTION ( 'NONE',  ( -1.000000000000000000, -0.000000000000000000, -0.000000000000000000 ) ) ;
#10088=ORIENTED_EDGE ( 'NONE', *, *, #1272, .F. ) ;
#10089=CARTESIAN_POINT ( 'NONE',  ( 0.02436607992776498519, -21.30679549418621832, -12.59161484032935618 ) ) ;
#10094=DIRECTION ( 'NONE',  ( 0.000000000000000000, 0.000000000000000000, 1.000000000000000000 ) ) ;
#10099=CARTESIAN_POINT ( 'NONE',  ( 2.765633920072235963, 21.30679549418649543, -12.59161484032888723 ) ) ;
#10105=FACE_OUTER_BOUND ( 'NONE', #9394, .T. ) ;
#10108=CARTESIAN_POINT ( 'NONE',  ( 0.7589665089996491254, -24.80232951178369660, -12.05173163741749320 ) ) ;
#10111=EDGE_LOOP ( 'NONE', ( #12299, #6828, #12877, #19269 ) ) ;
#10112=CARTESIAN_POINT ( 'NONE',  ( 2.789999999999999147, 9.324097380959765147, -22.25075486061728824 ) ) ;
#10115=CARTESIAN_POINT ( 'NONE',  ( 1.749999999999998002, 4.633866840648922292, 27.68468304288260384 ) ) ;
#10117=CARTESIAN_POINT ( 'NONE',  ( 0.000000000000000000, 2.680914349914567470E-13, -25.59481291497571220 ) ) ;
#10120=DIRECTION ( 'NONE',  ( -1.000000000000000000, -0.000000000000000000, -0.000000000000000000 ) ) ;
#10122=CARTESIAN_POINT ( 'NONE',  ( 0.000000000000000000, -7.909232158574988958, 24.34211360614297348 ) ) ;
#10123=ORIENTED_EDGE ( 'NONE', *, *, #14313, .T. ) ;
#10125=AXIS2_PLACEMENT_3D ( 'NONE', #5083, #5181, #18892 ) ;
#10126=VERTEX_POINT ( 'NONE', #9774 ) ;
#10131=ADVANCED_FACE ( 'NONE', ( #8461 ), #14565, .T. ) ;
#10137=CIRCLE ( 'NONE', #2150, 2.524999999999997247 ) ;
#10138=AXIS2_PLACEMENT_3D ( 'NONE', #14539, #2217, #8526 ) ;
#10142=LINE ( 'NONE', #553, #14559 ) ;
#10146=ORIENTED_EDGE ( 'NONE', *, *, #17983, .F. ) ;
#10147=CARTESIAN_POINT ( 'NONE',  ( 2.789999999999999147, -14.55412442567631537, 19.64056340710869719 ) ) ;
#10148=FACE_OUTER_BOUND ( 'NONE', #5659, .T. ) ;
#10151=CARTESIAN_POINT ( 'NONE',  ( 2.789999999999999147, 25.59481291497571220, 0.000000000000000000 ) ) ;
#10157=CARTESIAN_POINT ( 'NONE',  ( 0.02436607992776064838, 18.55949924794892780, 16.37294372382865504 ) ) ;
#10167=CARTESIAN_POINT ( 'NONE',  ( 2.789999999999999147, -22.25075486061731667, -9.324097380959683434 ) ) ;
#10168=VERTEX_POINT ( 'NONE', #17848 ) ;
#10172=CARTESIAN_POINT ( 'NONE',  ( 0.8958345380406140812, -24.59696699259434993, 12.96989951879399250 ) ) ;
#10173=ORIENTED_EDGE ( 'NONE', *, *, #14341, .T. ) ;
#10174=ORIENTED_EDGE ( 'NONE', *, *, #7821, .F. ) ;
#10175=LINE ( 'NONE', #16370, #6641 ) ;
#10187=DIRECTION ( 'NONE',  ( -1.000000000000000000, 0.000000000000000000, -0.000000000000000000 ) ) ;
#10193=CARTESIAN_POINT ( 'NONE',  ( 1.394999999999998685, -27.68468304288255410, -4.633866840649221608 ) ) ;
#10204=VERTEX_POINT ( 'NONE', #8942 ) ;
#10208=AXIS2_PLACEMENT_3D ( 'NONE', #6327, #18546, #1746 ) ;
#10217=CARTESIAN_POINT ( 'NONE',  ( 1.039999999999997593, 0.000000000000000000, 0.000000000000000000 ) ) ;
#10219=CARTESIAN_POINT ( 'NONE',  ( 2.718184757033982102, -18.89296398180179537, -16.91181672897754495 ) ) ;
#10221=ORIENTED_EDGE ( 'NONE', *, *, #12803, .F. ) ;
#10223=EDGE_LOOP ( 'NONE', ( #15818, #5941, #17066, #19284, #1916, #8397 ) ) ;
#10224=UNCERTAINTY_MEASURE_WITH_UNIT (LENGTH_MEASURE( 1.000000000000000082E-05 ), #13882, 'distance_accuracy_value', 'NONE');
#10226=CARTESIAN_POINT ( 'NONE',  ( 2.765633920072242180, 22.71065055754465689, -9.836394144775473691 ) ) ;
#10227=ADVANCED_FACE ( 'NONE', ( #5025 ), #11135, .F. ) ;
#10235=ORIENTED_EDGE ( 'NONE', *, *, #12144, .T. ) ;
#10244=AXIS2_PLACEMENT_3D ( 'NONE', #2818, #14840, #1134 ) ;
#10246=ORIENTED_EDGE ( 'NONE', *, *, #3830, .F. ) ;
#10253=FACE_OUTER_BOUND ( 'NONE', #2336, .T. ) ;
#10260=EDGE_CURVE ( 'NONE', #16376, #9486, #10735, .T. ) ;
#10262=EDGE_LOOP ( 'NONE', ( #10367, #11341, #16962, #1432, #14463, #5217, #14391 ) ) ;
#10263=DIRECTION ( 'NONE',  ( -1.000000000000000000, -0.000000000000000000, -0.000000000000000000 ) ) ;
#10264=DIRECTION ( 'NONE',  ( -1.000000000000000000, 0.000000000000000000, 0.000000000000000000 ) ) ;
#10265=CARTESIAN_POINT ( 'NONE',  ( 5.566640002541124371E-16, 15.96500990068152426, -18.34424029220094354 ) ) ;
#10266=CARTESIAN_POINT ( 'NONE',  ( 2.262072637928883800, -23.73240184472485836, -12.96450951081243375 ) ) ;
#10267=ORIENTED_EDGE ( 'NONE', *, *, #13340, .T. ) ;
#10274=ADVANCED_FACE ( 'NONE', ( #8017 ), #7835, .T. ) ;
#10276=CARTESIAN_POINT ( 'NONE',  ( 2.459751808031945922E-16, 12.51294990530016271, 20.85230829256858343 ) ) ;
#10278=ORIENTED_EDGE ( 'NONE', *, *, #7251, .F. ) ;
#10282=ADVANCED_FACE ( 'NONE', ( #4931 ), #5604, .T. ) ;
#10285=AXIS2_PLACEMENT_3D ( 'NONE', #3115, #7504, #6203 ) ;
#10289=DIRECTION ( 'NONE',  ( 1.000000000000000000, 0.000000000000000000, 0.000000000000000000 ) ) ;
#10291=CARTESIAN_POINT ( 'NONE',  ( 1.749999999999998002, -27.68468304288262516, 4.633866840648810381 ) ) ;
#10292=LINE ( 'NONE', #14889, #9497 ) ;
#10293=CYLINDRICAL_SURFACE ( 'NONE', #18604, 13.20000000000000284 ) ;
#10294=VERTEX_POINT ( 'NONE', #6121 ) ;
#10303=ORIENTED_EDGE ( 'NONE', *, *, #4073, .T. ) ;
#10305=DIRECTION ( 'NONE',  ( 1.000000000000000000, 0.000000000000000000, -0.000000000000000000 ) ) ;
#10307=ADVANCED_FACE ( 'NONE', ( #6216 ), #1829, .F. ) ;
#10309=ORIENTED_EDGE ( 'NONE', *, *, #12794, .F. ) ;
#10316=CARTESIAN_POINT ( 'NONE',  ( 2.789999999999999147, 15.04425356660790136, -20.70663861606255196 ) ) ;
#10318=VERTEX_POINT ( 'NONE', #13754 ) ;
#10331=TOROIDAL_SURFACE ( 'NONE', #11901, 24.12539914357697768, 8.000000000000000000 ) ;
#10340=CARTESIAN_POINT ( 'NONE',  ( 1.039999999999996927, 20.02152543075374069, -19.67366047555508501 ) ) ;
#10347=CARTESIAN_POINT ( 'NONE',  ( 2.789999999999999147, -8.936381166381891568E-14, 25.59481291497571220 ) ) ;
#10351=DIRECTION ( 'NONE',  ( 1.000000000000000000, 0.000000000000000000, -0.000000000000000000 ) ) ;
#10357=ORIENTED_EDGE ( 'NONE', *, *, #2835, .T. ) ;
#10359=CARTESIAN_POINT ( 'NONE',  ( 1.749999999999998002, -19.67366047555515252, -20.02152543075368030 ) ) ;
#10367=ORIENTED_EDGE ( 'NONE', *, *, #9192, .F. ) ;
#10368=CARTESIAN_POINT ( 'NONE',  ( 0.02436607992776585255, -5.391175441198789109, 24.15498966839961170 ) ) ;
#10373=ADVANCED_FACE ( 'NONE', ( #11956 ), #16813, .T. ) ;
#10378=TOROIDAL_SURFACE ( 'NONE', #1742, 24.12539914357697413, 8.000000000000000000 ) ;
#10380=CARTESIAN_POINT ( 'NONE',  ( 0.7589665349472695111, -27.14933624560910630, 4.828387785247921116 ) ) ;
#10382=CARTESIAN_POINT ( 'NONE',  ( -10.00000000000000000, 0.000000000000000000, 0.000000000000000000 ) ) ;
#10395=VERTEX_POINT ( 'NONE', #9156 ) ;
#10396=DIRECTION ( 'NONE',  ( -1.000000000000000000, 0.000000000000000000, 0.000000000000000000 ) ) ;
#10398=DIRECTION ( 'NONE',  ( -1.000000000000000000, 0.000000000000000000, -0.000000000000000000 ) ) ;
#10400=CYLINDRICAL_SURFACE ( 'NONE', #3851, 2.524999999999995914 ) ;
#10401=DIRECTION ( 'NONE',  ( -1.000000000000000000, -0.000000000000000000, -0.000000000000000000 ) ) ;
#10403=ORIENTED_EDGE ( 'NONE', *, *, #1023, .T. ) ;
#10410=CARTESIAN_POINT ( 'NONE',  ( 2.031033471609898111, -27.31260702007178409, 3.797536611356223890 ) ) ;
#10411=DIRECTION ( 'NONE',  ( -1.000000000000000000, -0.000000000000000000, -0.000000000000000000 ) ) ;
#10412=ADVANCED_FACE ( 'NONE', ( #1452 ), #8173, .T. ) ;
#10418=CARTESIAN_POINT ( 'NONE',  ( 0.000000000000000000, -15.04425356660744839, -20.70663861606288236 ) ) ;
#10420=B_SPLINE_CURVE_WITH_KNOTS ( 'NONE', 3,
 ( #12850, #5338, #7113, #13142, #17553, #751 ),
 .UNSPECIFIED., .F., .F.,
 ( 4, 2, 4 ),
 ( 2.321268216996885854E-07, 0.001878622960950492504, 0.003757013795079285415 ),
 .UNSPECIFIED. ) ;
#10430=EDGE_LOOP ( 'NONE', ( #16342, #7004, #1672, #9657 ) ) ;
#10434=CARTESIAN_POINT ( 'NONE',  ( 2.262072661820536013, 26.82026385750178932, -3.461047254864356049 ) ) ;
#10435=ORIENTED_EDGE ( 'NONE', *, *, #10749, .F. ) ;
#10439=DIRECTION ( 'NONE',  ( -1.000000000000000000, -0.000000000000000000, 0.000000000000000000 ) ) ;
#10442=ORIENTED_EDGE ( 'NONE', *, *, #3994, .F. ) ;
#10444=ORIENTED_EDGE ( 'NONE', *, *, #12443, .F. ) ;
#10448=DIRECTION ( 'NONE',  ( 1.000000000000000000, 0.000000000000000000, -0.000000000000000000 ) ) ;
#10450=ORIENTED_EDGE ( 'NONE', *, *, #5797, .T. ) ;
#10452=CARTESIAN_POINT ( 'NONE',  ( 1.039999999999999147, 12.52377138324259676, -25.12109765559640095 ) ) ;
#10454=CARTESIAN_POINT ( 'NONE',  ( 0.000000000000000000, 24.04302995059966719, 1.991882183130389228 ) ) ;
#10459=VERTEX_POINT ( 'NONE', #3346 ) ;
#10461=DIRECTION ( 'NONE',  ( 0.000000000000000000, 0.000000000000000000, 1.000000000000000000 ) ) ;
#10462=DIRECTION ( 'NONE',  ( 0.000000000000000000, 0.000000000000000000, 1.000000000000000000 ) ) ;
#10463=ORIENTED_EDGE ( 'NONE', *, *, #13868, .F. ) ;
#10469=AXIS2_PLACEMENT_3D ( 'NONE', #3949, #14851, #3849 ) ;
#10481=VECTOR ( 'NONE', #627, 1000.000000000000000 ) ;
#10484=AXIS2_PLACEMENT_3D ( 'NONE', #4908, #18904, #1901 ) ;
#10486=CARTESIAN_POINT ( 'NONE',  ( 2.789999999999999147, 2.336989772644613161, -24.63872515616080250 ) ) ;
#10491=SURFACE_SIDE_STYLE ('',( #4380 ) ) ;
#10494=CIRCLE ( 'NONE', #2808, 24.12539914357697413 ) ;
#10495=CARTESIAN_POINT ( 'NONE',  ( 2.789999999999999147, 20.70663861606293210, -12.51925356660738053 ) ) ;
#10515=DIRECTION ( 'NONE',  ( 1.000000000000000000, 0.000000000000000000, 0.000000000000000000 ) ) ;
#10517=CARTESIAN_POINT ( 'NONE',  ( -10.00000000000000000, 0.000000000000000000, 0.000000000000000000 ) ) ;
#10520=CARTESIAN_POINT ( 'NONE',  ( 2.789999999999999147, -9.324097380959603498, 22.25075486061734864 ) ) ;
#10523=ORIENTED_EDGE ( 'NONE', *, *, #423, .F. ) ;
#10525=CARTESIAN_POINT ( 'NONE',  ( 2.601776096565022289, 22.54313264455032240, -12.84621645676820201 ) ) ;
#10531=LINE ( 'NONE', #3292, #1092 ) ;
#10534=ORIENTED_EDGE ( 'NONE', *, *, #10676, .T. ) ;
#10536=ORIENTED_EDGE ( 'NONE', *, *, #12150, .T. ) ;
#10541=CARTESIAN_POINT ( 'NONE',  ( 2.358581579527286198, -23.43037373958380343, 12.94152279942367656 ) ) ;
#10544=CARTESIAN_POINT ( 'NONE',  ( 0.07186813532171169860, -2.577209017047189299, 25.22589920183361301 ) ) ;
#10546=CYLINDRICAL_SURFACE ( 'NONE', #15705, 2.524999999999995914 ) ;
#10550=CIRCLE ( 'NONE', #9269, 2.524999999999996358 ) ;
#10551=VERTEX_POINT ( 'NONE', #18137 ) ;
#10552=B_SPLINE_CURVE_WITH_KNOTS ( 'NONE', 3,
 ( #15004, #10600, #16706, #13299 ),
 .UNSPECIFIED., .F., .F.,
 ( 4, 4 ),
 ( 2.034713381942769504E-07, 0.0006887909409525124101 ),
 .UNSPECIFIED. ) ;
#10554=DIRECTION ( 'NONE',  ( -1.000000000000000000, -0.000000000000000000, -0.000000000000000000 ) ) ;
#10556=VERTEX_POINT ( 'NONE', #5914 ) ;
#10560=ORIENTED_EDGE ( 'NONE', *, *, #11443, .T. ) ;
#10563=EDGE_LOOP ( 'NONE', ( #1566, #13296, #6893, #8627 ) ) ;
#10566=DIRECTION ( 'NONE',  ( 0.000000000000000000, 0.000000000000000000, 1.000000000000000000 ) ) ;
#10568=ORIENTED_EDGE ( 'NONE', *, *, #14385, .F. ) ;
#10574=ORIENTED_EDGE ( 'NONE', *, *, #6032, .F. ) ;
#10578=ORIENTED_EDGE ( 'NONE', *, *, #378, .F. ) ;
#10591=CARTESIAN_POINT ( 'NONE',  ( 2.789999999999999147, -7.909232158574647009, -24.34211360614308006 ) ) ;
#10596=DIRECTION ( 'NONE',  ( -1.000000000000000000, -0.000000000000000000, 0.000000000000000000 ) ) ;
#10597=CARTESIAN_POINT ( 'NONE',  ( 2.765633920072239516, -24.63872515616084513, 2.336989772644183283 ) ) ;
#10600=CARTESIAN_POINT ( 'NONE',  ( 0.006974663525959075641, 12.53640742967783694, -21.08118142846890208 ) ) ;
#10601=B_SPLINE_CURVE_WITH_KNOTS ( 'NONE', 3,
 ( #8832, #11829, #7507, #2814 ),
 .UNSPECIFIED., .F., .F.,
 ( 4, 4 ),
 ( 2.135345996175579449E-07, 0.0006888010880210803950 ),
 .UNSPECIFIED. ) ;
#10605=CIRCLE ( 'NONE', #5478, 24.12539914357697413 ) ;
#10611=ORIENTED_EDGE ( 'NONE', *, *, #14160, .T. ) ;
#10612=DIRECTION ( 'NONE',  ( -1.000000000000000000, -0.000000000000000000, -0.000000000000000000 ) ) ;
#10613=DIRECTION ( 'NONE',  ( 0.000000000000000000, 0.000000000000000000, 1.000000000000000000 ) ) ;
#10614=CARTESIAN_POINT ( 'NONE',  ( 2.789895169984651702, -20.67846228565646172, -12.51925356660783528 ) ) ;
#10616=CIRCLE ( 'NONE', #13170, 2.524999999999995914 ) ;
#10618=FACE_OUTER_BOUND ( 'NONE', #16280, .T. ) ;
#10621=CARTESIAN_POINT ( 'NONE',  ( 2.765633920072238627, 5.391175441198956086, -24.15498966839956907 ) ) ;
#10624=VERTEX_POINT ( 'NONE', #7205 ) ;
#10634=ORIENTED_EDGE ( 'NONE', *, *, #6981, .T. ) ;
#10639=CARTESIAN_POINT ( 'NONE',  ( 2.783025325906567371, 2.249040938978837278, -24.42374957165203142 ) ) ;
#10651=CARTESIAN_POINT ( 'NONE',  ( 1.039999999999995817, 4.633866840648921404, 27.68468304288260029 ) ) ;
#10660=CIRCLE ( 'NONE', #4583, 28.06981291497571362 ) ;
#10663=EDGE_CURVE ( 'NONE', #5291, #15288, #13422, .T. ) ;
#10664=CARTESIAN_POINT ( 'NONE',  ( 0.000000000000000000, 23.48180575137739368, -5.535312321042471062 ) ) ;
#10666=ORIENTED_EDGE ( 'NONE', *, *, #3708, .T. ) ;
#10668=EDGE_CURVE ( 'NONE', #1940, #4236, #71, .T. ) ;
#10669=CARTESIAN_POINT ( 'NONE',  ( 0.02436607992776151574, 24.15498966839970052, -5.391175441198366336 ) ) ;
#10676=EDGE_CURVE ( 'NONE', #16730, #2850, #121, .T. ) ;
#10677=ORIENTED_EDGE ( 'NONE', *, *, #14586, .F. ) ;
#10678=AXIS2_PLACEMENT_3D ( 'NONE', #3835, #18944, #2520 ) ;
#10683=EDGE_LOOP ( 'NONE', ( #14526, #19512, #2615, #12202, #19237, #12752, #1227, #14328 ) ) ;
#10685=CARTESIAN_POINT ( 'NONE',  ( 0.000000000000000000, -22.25075486061732732, -9.324097380959701198 ) ) ;
#10689=CARTESIAN_POINT ( 'NONE',  ( 2.789999999999999147, -19.64056340710864745, -14.55412442567638287 ) ) ;
#10695=ORIENTED_EDGE ( 'NONE', *, *, #16003, .T. ) ;
#10696=DIRECTION ( 'NONE',  ( -1.000000000000000000, -0.000000000000000000, 0.000000000000000000 ) ) ;
#10697=EDGE_CURVE ( 'NONE', #619, #10459, #13896, .T. ) ;
#10699=ORIENTED_EDGE ( 'NONE', *, *, #16372, .T. ) ;
#10708=( NAMED_UNIT ( * ) PLANE_ANGLE_UNIT ( ) SI_UNIT ( $, .RADIAN. ) );
#10709=LINE ( 'NONE', #7689, #5568 ) ;
#10710=CARTESIAN_POINT ( 'NONE',  ( 1.749999999999998002, 12.96210679857822257, -24.89775460606818669 ) ) ;
#10713=CARTESIAN_POINT ( 'NONE',  ( 2.765633920072234631, -21.30679549418640306, 12.59161484032904887 ) ) ;
#10722=CARTESIAN_POINT ( 'NONE',  ( 0.02436607992775978102, 24.63872515616082737, 2.336989772644355146 ) ) ;
#10724=ORIENTED_EDGE ( 'NONE', *, *, #15596, .F. ) ;
#10725=EDGE_CURVE ( 'NONE', #5656, #19204, #7203, .T. ) ;
#10727=CARTESIAN_POINT ( 'NONE',  ( 1.039999999999997593, -12.52377138324241557, 25.12109765559648977 ) ) ;
#10732=FACE_OUTER_BOUND ( 'NONE', #18182, .T. ) ;
#10734=CARTESIAN_POINT ( 'NONE',  ( -7.755480735455585059E-14, 24.22524813288762502, -2.133839912090887303 ) ) ;
#10735=CIRCLE ( 'NONE', #17121, 24.12539914357697413 ) ;
#10739=AXIS2_PLACEMENT_3D ( 'NONE', #12645, #6815, #11343 ) ;
#10740=CARTESIAN_POINT ( 'NONE',  ( 2.765633920072234631, -21.30679549418640306, 12.59161484032904887 ) ) ;
#10742=CARTESIAN_POINT ( 'NONE',  ( 2.789999999999999147, -15.04425356660744839, -20.70663861606288236 ) ) ;
#10743=LINE ( 'NONE', #3131, #15269 ) ;
#10744=VERTEX_POINT ( 'NONE', #1817 ) ;
#10749=EDGE_CURVE ( 'NONE', #881, #18268, #14264, .T. ) ;
#10750=VECTOR ( 'NONE', #7006, 1000.000000000000000 ) ;
#10751=DIRECTION ( 'NONE',  ( 0.000000000000000000, 0.000000000000000000, -1.000000000000000000 ) ) ;
#10754=CARTESIAN_POINT ( 'NONE',  ( 2.718184743034448569, 24.78695292654929005, -5.344212458769106888 ) ) ;
#10756=ORIENTED_EDGE ( 'NONE', *, *, #5982, .F. ) ;
#10758=ORIENTED_EDGE ( 'NONE', *, *, #1048, .T. ) ;
#10760=CARTESIAN_POINT ( 'NONE',  ( 0.02436607992775544421, -22.71065055754445439, -9.836394144775947979 ) ) ;
#10762=VERTEX_POINT ( 'NONE', #2014 ) ;
#10765=CARTESIAN_POINT ( 'NONE',  ( 2.604434325169353581, -2.851997810081467577, -25.77772010606609498 ) ) ;
#10774=DIRECTION ( 'NONE',  ( 1.000000000000000000, 0.000000000000000000, 0.000000000000000000 ) ) ;
#10780=CARTESIAN_POINT ( 'NONE',  ( 1.749999999999998002, 0.000000000000000000, 0.000000000000000000 ) ) ;
#10782=AXIS2_PLACEMENT_3D ( 'NONE', #15129, #522, #18914 ) ;
#10783=VERTEX_POINT ( 'NONE', #1912 ) ;
#10786=DIRECTION ( 'NONE',  ( 0.000000000000000000, 0.000000000000000000, 1.000000000000000000 ) ) ;
#10797=DIRECTION ( 'NONE',  ( 0.000000000000000000, 0.000000000000000000, 1.000000000000000000 ) ) ;
#10799=CARTESIAN_POINT ( 'NONE',  ( 0.000000000000000000, -24.04302995059965653, -1.991882183130557094 ) ) ;
#10801=CIRCLE ( 'NONE', #15602, 24.12539914357697768 ) ;
#10803=( LENGTH_UNIT ( ) NAMED_UNIT ( * ) SI_UNIT ( .MILLI., .METRE. ) );
#10806=EDGE_CURVE ( 'NONE', #19214, #9684, #7083, .T. ) ;
#10807=FACE_OUTER_BOUND ( 'NONE', #8655, .T. ) ;
#10809=FACE_OUTER_BOUND ( 'NONE', #15863, .T. ) ;
#10810=DIRECTION ( 'NONE',  ( -1.000000000000000000, -0.000000000000000000, -0.000000000000000000 ) ) ;
#10812=CARTESIAN_POINT ( 'NONE',  ( 0.0003207540509378258692, 20.70663861606293921, -12.51925356660738053 ) ) ;
#10814=CARTESIAN_POINT ( 'NONE',  ( 0.1855654851361735469, 10.67816411292198175, -23.63475234378971379 ) ) ;
#10817=EDGE_CURVE ( 'NONE', #19442, #12550, #19679, .T. ) ;
#10819=CARTESIAN_POINT ( 'NONE',  ( 2.789999999999999147, -20.62201879784921843, 12.52067188844344336 ) ) ;
#10821=VERTEX_POINT ( 'NONE', #8314 ) ;
#10823=CARTESIAN_POINT ( 'NONE',  ( 1.039999999999998925, -4.147968289691484678, 27.76164181293050248 ) ) ;
#10824=CARTESIAN_POINT ( 'NONE',  ( 0.02436607992776498519, 9.836394144775706394, 22.71065055754456097 ) ) ;
#10831=ORIENTED_EDGE ( 'NONE', *, *, #4899, .T. ) ;
#10834=ORIENTED_EDGE ( 'NONE', *, *, #5982, .T. ) ;
#10838=EDGE_CURVE ( 'NONE', #16718, #19487, #11611, .T. ) ;
#10843=CARTESIAN_POINT ( 'NONE',  ( 2.790000000000076419, -20.85287692521938752, 12.51293083811791718 ) ) ;
#10855=CARTESIAN_POINT ( 'NONE',  ( 2.789999999999999147, 20.62201879784912606, 12.52067188844359080 ) ) ;
#10860=EDGE_LOOP ( 'NONE', ( #16527, #3349, #10062, #16876, #11226, #2055, #13016, #12381 ) ) ;
#10862=CARTESIAN_POINT ( 'NONE',  ( 0.07181524296601660140, -16.91181672897718968, -18.89296398180210446 ) ) ;
#10863=CARTESIAN_POINT ( 'NONE',  ( 2.765633920072239516, -2.336989772644097574, -24.63872515616085224 ) ) ;
#10866=TOROIDAL_SURFACE ( 'NONE', #13410, 24.12539914357697768, 8.000000000000000000 ) ;
#10873=CARTESIAN_POINT ( 'NONE',  ( 2.262072637928882468, -12.96450951081233605, 23.73240184472491876 ) ) ;
#10875=AXIS2_PLACEMENT_3D ( 'NONE', #181, #16801, #10786 ) ;
#10877=CARTESIAN_POINT ( 'NONE',  ( 1.749999999999998002, -20.02152543075360214, 19.67366047555523068 ) ) ;
#10880=DIRECTION ( 'NONE',  ( -1.000000000000000000, -0.000000000000000000, -0.000000000000000000 ) ) ;
#10882=ORIENTED_EDGE ( 'NONE', *, *, #18987, .T. ) ;
#10887=CARTESIAN_POINT ( 'NONE',  ( 2.724374482943360487, 21.84204283372364230, 12.72258903105646688 ) ) ;
#10889=VERTEX_POINT ( 'NONE', #16019 ) ;
#10898=ADVANCED_FACE ( 'NONE', ( #16130 ), #16185, .T. ) ;
#10901=CARTESIAN_POINT ( 'NONE',  ( 0.1882238782932344201, 17.47009390565490605, 19.18368891937496556 ) ) ;
#10902=CARTESIAN_POINT ( 'NONE',  ( -10.00000000000000000, 0.000000000000000000, 0.000000000000000000 ) ) ;
#10903=ORIENTED_EDGE ( 'NONE', *, *, #13821, .F. ) ;
#10917=CARTESIAN_POINT ( 'NONE',  ( 0.5321745087963422050, -11.58891744060090367, -24.44564404695856297 ) ) ;
#10925=CARTESIAN_POINT ( 'NONE',  ( 0.006974771092478231072, 9.686319561460942751, 22.53337530003406997 ) ) ;
#10929=ORIENTED_EDGE ( 'NONE', *, *, #13205, .F. ) ;
#10932=CARTESIAN_POINT ( 'NONE',  ( 2.765633920072242624, -22.71065055754459650, 9.836394144775621129 ) ) ;
#10943=CARTESIAN_POINT ( 'NONE',  ( 0.02436607992776151574, -16.37294372382871188, 18.55949924794887096 ) ) ;
#10944=VECTOR ( 'NONE', #8497, 1000.000000000000000 ) ;
#10945=EDGE_LOOP ( 'NONE', ( #7223, #9307, #17575, #6089 ) ) ;
#10962=VERTEX_POINT ( 'NONE', #2691 ) ;
#10964=CARTESIAN_POINT ( 'NONE',  ( 1.039999999999998259, 12.52377138324223615, 25.12109765559657859 ) ) ;
#10969=ORIENTED_EDGE ( 'NONE', *, *, #840, .F. ) ;
#10974=CARTESIAN_POINT ( 'NONE',  ( 0.006974771092478813939, -22.53337530003410905, 9.686319561460866367 ) ) ;
#10976=ORIENTED_EDGE ( 'NONE', *, *, #456, .F. ) ;
#10981=CARTESIAN_POINT ( 'NONE',  ( 0.000000000000000000, -20.62201879784923264, 12.52067188844344336 ) ) ;
#10987=CARTESIAN_POINT ( 'NONE',  ( 0.000000000000000000, 18.28042085475300382, -15.74360496233363804 ) ) ;
#10988=EDGE_CURVE ( 'NONE', #13429, #10783, #8808, .T. ) ;
#10996=CYLINDRICAL_SURFACE ( 'NONE', #116, 2.524999999999995914 ) ;
#11007=VERTEX_POINT ( 'NONE', #13217 ) ;
#11008=CARTESIAN_POINT ( 'NONE',  ( 2.765633920072233742, -24.15498966839966855, 5.391175441198523544 ) ) ;
#11014=CARTESIAN_POINT ( 'NONE',  ( 1.039999999999997149, -4.633866840648735774, -27.68468304288263226 ) ) ;
#11018=EDGE_CURVE ( 'NONE', #12265, #9627, #4839, .T. ) ;
#11020=CARTESIAN_POINT ( 'NONE',  ( 1.749999999999998002, 19.67366047555530528, 20.02152543075352753 ) ) ;
#11024=ORIENTED_EDGE ( 'NONE', *, *, #15251, .F. ) ;
#11025=CARTESIAN_POINT ( 'NONE',  ( 1.749999999999998002, -27.76164181293049182, -4.147968289691579713 ) ) ;
#11026=DIRECTION ( 'NONE',  ( -1.000000000000000000, -0.000000000000000000, -0.000000000000000000 ) ) ;
#11038=EDGE_LOOP ( 'NONE', ( #11705, #1070, #6857, #9973, #18463, #15519 ) ) ;
#11039=DIRECTION ( 'NONE',  ( 0.000000000000000000, 0.000000000000000000, 1.000000000000000000 ) ) ;
#11040=CARTESIAN_POINT ( 'NONE',  ( 2.783068888626318405, 9.685942809247050533, 22.53293026234507579 ) ) ;
#11042=EDGE_CURVE ( 'NONE', #4945, #1219, #3732, .T. ) ;
#11050=ORIENTED_EDGE ( 'NONE', *, *, #13494, .F. ) ;
#11055=FACE_OUTER_BOUND ( 'NONE', #11460, .T. ) ;
#11057=ORIENTED_EDGE ( 'NONE', *, *, #9093, .T. ) ;
#11060=CARTESIAN_POINT ( 'NONE',  ( 1.039999999999997593, 0.000000000000000000, 0.000000000000000000 ) ) ;
#11063=AXIS2_PLACEMENT_3D ( 'NONE', #13113, #6894, #5104 ) ;
#11065=AXIS2_PLACEMENT_3D ( 'NONE', #18229, #114, #12125 ) ;
#11073=DIRECTION ( 'NONE',  ( 0.000000000000000000, 0.000000000000000000, 1.000000000000000000 ) ) ;
#11078=EDGE_LOOP ( 'NONE', ( #18572, #10123, #18677, #10634 ) ) ;
#11079=ORIENTED_EDGE ( 'NONE', *, *, #7818, .T. ) ;
#11080=CARTESIAN_POINT ( 'NONE',  ( 0.000000000000000000, 15.04425356660790136, -20.70663861606255196 ) ) ;
#11090=CIRCLE ( 'NONE', #10138, 28.06981291497571362 ) ;
#11094=CARTESIAN_POINT ( 'NONE',  ( 0.02436607992776325046, -24.15498966839958683, -5.391175441198872598 ) ) ;
#11102=AXIS2_PLACEMENT_3D ( 'NONE', #16941, #6309, #1729 ) ;
#11113=VERTEX_POINT ( 'NONE', #12205 ) ;
#11123=DIRECTION ( 'NONE',  ( -1.000000000000000000, 0.000000000000000000, 0.000000000000000000 ) ) ;
#11125=EDGE_CURVE ( 'NONE', #2276, #10395, #12000, .T. ) ;
#11127=ADVANCED_FACE ( 'NONE', ( #18693 ), #9303, .T. ) ;
#11128=LINE ( 'NONE', #5018, #16944 ) ;
#11130=ADVANCED_FACE ( 'NONE', ( #6470 ), #7219, .T. ) ;
#11135=CYLINDRICAL_SURFACE ( 'NONE', #12002, 2.524999999999995914 ) ;
#11140=ORIENTED_EDGE ( 'NONE', *, *, #16536, .F. ) ;
#11143=ORIENTED_EDGE ( 'NONE', *, *, #162, .F. ) ;
#11147=CARTESIAN_POINT ( 'NONE',  ( 2.790000000000000036, 22.37986894186685660, -9.514945144208509120 ) ) ;
#11157=CARTESIAN_POINT ( 'NONE',  ( 6.560148031203755073E-16, 23.69843731927177544, -5.456805104200854295 ) ) ;
#11160=ORIENTED_EDGE ( 'NONE', *, *, #13395, .F. ) ;
#11162=CARTESIAN_POINT ( 'NONE',  ( -10.00000000000000000, 0.000000000000000000, 0.000000000000000000 ) ) ;
#11165=ADVANCED_FACE ( 'NONE', ( #11588 ), #12699, .T. ) ;
#11170=EDGE_CURVE ( 'NONE', #1219, #16193, #8188, .T. ) ;
#11177=DIRECTION ( 'NONE',  ( -1.000000000000000000, 0.000000000000000000, 0.000000000000000000 ) ) ;
#11191=VECTOR ( 'NONE', #11402, 1000.000000000000000 ) ;
#11192=AXIS2_PLACEMENT_3D ( 'NONE', #7616, #9133, #13633 ) ;
#11194=CARTESIAN_POINT ( 'NONE',  ( 0.02436607992775891365, -24.63872515616080960, -2.336989772644527008 ) ) ;
#11200=CARTESIAN_POINT ( 'NONE',  ( 2.789999999999999147, -23.48180575137726223, -5.535312321042966666 ) ) ;
#11203=LINE ( 'NONE', #14303, #14394 ) ;
#11207=CARTESIAN_POINT ( 'NONE',  ( 0.02436607992776585255, -5.391175441198789109, 24.15498966839961170 ) ) ;
#11208=TOROIDAL_SURFACE ( 'NONE', #17603, 24.12539914357697768, 8.000000000000000000 ) ;
#11212=LINE ( 'NONE', #3701, #11876 ) ;
#11213=CARTESIAN_POINT ( 'NONE',  ( 0.02436607992775674525, 9.836394144776026138, -22.71065055754441531 ) ) ;
#11217=B_SPLINE_CURVE_WITH_KNOTS ( 'NONE', 3,
 ( #3084, #6364, #13996, #15304 ),
 .UNSPECIFIED., .F., .F.,
 ( 4, 4 ),
 ( 2.135345996173299606E-07, 0.0006888010880210790939 ),
 .UNSPECIFIED. ) ;
#11218=ORIENTED_EDGE ( 'NONE', *, *, #19377, .F. ) ;
#11223=EDGE_CURVE ( 'NONE', #18420, #14758, #18736, .T. ) ;
#11226=ORIENTED_EDGE ( 'NONE', *, *, #14377, .T. ) ;
#11231=CARTESIAN_POINT ( 'NONE',  ( 2.789999999999999147, -20.70663861606260170, -15.04425356660783031 ) ) ;
#11232=CARTESIAN_POINT ( 'NONE',  ( 0.02436607992776064838, 18.55949924794892780, 16.37294372382865504 ) ) ;
#11233=ORIENTED_EDGE ( 'NONE', *, *, #15175, .T. ) ;
#11235=DIRECTION ( 'NONE',  ( -1.000000000000000000, -0.000000000000000000, 0.000000000000000000 ) ) ;
#11241=CARTESIAN_POINT ( 'NONE',  ( 50.00050000000000239, 0.000000000000000000, 0.000000000000000000 ) ) ;
#11252=AXIS2_PLACEMENT_3D ( 'NONE', #1661, #7759, #16975 ) ;
#11254=CARTESIAN_POINT ( 'NONE',  ( 2.789999999999999147, 14.55412442567617681, 19.64056340710880022 ) ) ;
#11256=EDGE_LOOP ( 'NONE', ( #12849, #4411, #17182, #14228, #16930, #3841 ) ) ;
#11261=MECHANICAL_DESIGN_GEOMETRIC_PRESENTATION_REPRESENTATION('',(#18280),#12214);
#11266=AXIS2_PLACEMENT_3D ( 'NONE', #1369, #969, #11576 ) ;
#11267=VECTOR ( 'NONE', #4480, 1000.000000000000000 ) ;
#11270=VECTOR ( 'NONE', #16666, 1000.000000000000000 ) ;
#11275=CARTESIAN_POINT ( 'NONE',  ( 5.139549990269394683E-16, -2.133490293297187979, 24.22479935914660132 ) ) ;
#11281=CIRCLE ( 'NONE', #16707, 2.524999999999998135 ) ;
#11284=CIRCLE ( 'NONE', #18308, 2.524999999999995914 ) ;
#11291=CARTESIAN_POINT ( 'NONE',  ( 8.000000000000000000, 0.000000000000000000, 0.000000000000000000 ) ) ;
#11299=ADVANCED_FACE ( 'NONE', ( #9907 ), #18191, .T. ) ;
#11312=CARTESIAN_POINT ( 'NONE',  ( 2.789999999999999147, 20.70663861606293210, -15.04425356660737556 ) ) ;
#11315=ORIENTED_EDGE ( 'NONE', *, *, #423, .T. ) ;
#11317=CARTESIAN_POINT ( 'NONE',  ( 0.02436607992776368414, -9.836394144775550075, -22.71065055754462492 ) ) ;
#11322=B_SPLINE_CURVE_WITH_KNOTS ( 'NONE', 3,
 ( #3739, #5334, #9760, #14347, #6720, #12846 ),
 .UNSPECIFIED., .F., .F.,
 ( 4, 2, 4 ),
 ( 2.032124546189838441E-07, 0.001878594002992310316, 0.003756984793530001362 ),
 .UNSPECIFIED. ) ;
#11323=CARTESIAN_POINT ( 'NONE',  ( 0.07181525696555157712, 5.344212458769712626, -24.78695292654915860 ) ) ;
#11329=CARTESIAN_POINT ( 'NONE',  ( -5.209999999999999964, 0.000000000000000000, 0.000000000000000000 ) ) ;
#11338=CARTESIAN_POINT ( 'NONE',  ( 1.039999999999997149, -4.633866840648735774, -27.68468304288263226 ) ) ;
#11341=ORIENTED_EDGE ( 'NONE', *, *, #1859, .F. ) ;
#11342=CARTESIAN_POINT ( 'NONE',  ( 2.765633920072237295, 12.59161484032912171, 21.30679549418635688 ) ) ;
#11343=DIRECTION ( 'NONE',  ( 0.000000000000000000, 0.000000000000000000, 1.000000000000000000 ) ) ;
#11345=B_SPLINE_CURVE_WITH_KNOTS ( 'NONE', 3,
 ( #13535, #2724, #19639, #5922, #18144, #7516 ),
 .UNSPECIFIED., .F., .F.,
 ( 4, 2, 4 ),
 ( 4.462636882273700183E-07, 0.001879885203074810199, 0.003759324142461393028 ),
 .UNSPECIFIED. ) ;
#11346=ADVANCED_FACE ( 'NONE', ( #7356 ), #7545, .T. ) ;
#11349=DIRECTION ( 'NONE',  ( 0.000000000000000000, 0.000000000000000000, 1.000000000000000000 ) ) ;
#11353=EDGE_CURVE ( 'NONE', #758, #16305, #15565, .T. ) ;
#11363=VERTEX_POINT ( 'NONE', #16389 ) ;
#11364=CARTESIAN_POINT ( 'NONE',  ( 0.06562551705663710599, -21.84204283372370625, 12.72258903105631234 ) ) ;
#11367=VERTEX_POINT ( 'NONE', #13580 ) ;
#11372=CARTESIAN_POINT ( 'NONE',  ( -10.00000000000000000, 0.000000000000000000, 0.000000000000000000 ) ) ;
#11374=DIRECTION ( 'NONE',  ( 0.000000000000000000, 6.870191984066572599E-15, -1.000000000000000000 ) ) ;
#11376=CARTESIAN_POINT ( 'NONE',  ( 0.000000000000000000, 0.000000000000000000, 0.000000000000000000 ) ) ;
#11378=EDGE_CURVE ( 'NONE', #19481, #10551, #5637, .T. ) ;
#11384=CARTESIAN_POINT ( 'NONE',  ( 2.563317066925346527E-16, -12.51294990530000817, -20.85230829256867935 ) ) ;
#11385=VERTEX_POINT ( 'NONE', #4379 ) ;
#11388=ORIENTED_EDGE ( 'NONE', *, *, #13649, .F. ) ;
#11389=CARTESIAN_POINT ( 'NONE',  ( 1.394999999999999574, 12.52377138324259676, -25.12109765559640451 ) ) ;
#11392=AXIS2_PLACEMENT_3D ( 'NONE', #4098, #19293, #5585 ) ;
#11397=CARTESIAN_POINT ( 'NONE',  ( 2.780897501012522977, 21.10878525316979903, -12.54316204260869760 ) ) ;
#11398=ORIENTED_EDGE ( 'NONE', *, *, #12307, .T. ) ;
#11399=FACE_OUTER_BOUND ( 'NONE', #2945, .T. ) ;
#11402=DIRECTION ( 'NONE',  ( -1.000000000000000000, 0.000000000000000000, 0.000000000000000000 ) ) ;
#11412=ADVANCED_FACE ( 'NONE', ( #19478 ), #16532, .T. ) ;
#11413=CARTESIAN_POINT ( 'NONE',  ( 0.07181525068722525995, 25.22524549359950541, -2.576941577947494011 ) ) ;
#11414=ORIENTED_EDGE ( 'NONE', *, *, #2767, .T. ) ;
#11416=CARTESIAN_POINT ( 'NONE',  ( 1.039999999999995595, 4.147968289691676524, -27.76164181293047051 ) ) ;
#11417=EDGE_CURVE ( 'NONE', #12785, #2600, #2472, .T. ) ;
#11419=CARTESIAN_POINT ( 'NONE',  ( 2.789999999999999147, -5.391175441198789109, 24.15498966839961170 ) ) ;
#11424=CARTESIAN_POINT ( 'NONE',  ( 2.257825477245765988, -19.66801664102690239, -18.57583492944443293 ) ) ;
#11432=CARTESIAN_POINT ( 'NONE',  ( 1.039999999999997593, -12.52377138324241557, 25.12109765559648977 ) ) ;
#11443=EDGE_CURVE ( 'NONE', #10821, #8477, #13192, .T. ) ;
#11444=FACE_OUTER_BOUND ( 'NONE', #4046, .T. ) ;
#11450=ORIENTED_EDGE ( 'NONE', *, *, #3360, .T. ) ;
#11456=AXIS2_PLACEMENT_3D ( 'NONE', #2294, #5581, #6977 ) ;
#11458=DIRECTION ( 'NONE',  ( -1.000000000000000000, -0.000000000000000000, 0.000000000000000000 ) ) ;
#11460=EDGE_LOOP ( 'NONE', ( #7746, #5880, #9096, #9085 ) ) ;
#11464=ORIENTED_EDGE ( 'NONE', *, *, #11417, .F. ) ;
#11467=EDGE_CURVE ( 'NONE', #19481, #9137, #10292, .T. ) ;
#11474=EDGE_CURVE ( 'NONE', #16477, #14603, #309, .T. ) ;
#11483=VERTEX_POINT ( 'NONE', #1771 ) ;
#11484=DIRECTION ( 'NONE',  ( -1.000000000000000000, -0.000000000000000000, -0.000000000000000000 ) ) ;
#11490=DIRECTION ( 'NONE',  ( 0.000000000000000000, 0.000000000000000000, 1.000000000000000000 ) ) ;
#11491=TOROIDAL_SURFACE ( 'NONE', #2856, 24.12539914357697768, 8.000000000000000000 ) ;
#11496=ORIENTED_EDGE ( 'NONE', *, *, #13132, .F. ) ;
#11498=DIRECTION ( 'NONE',  ( 1.000000000000000000, -0.000000000000000000, 0.000000000000000000 ) ) ;
#11504=CARTESIAN_POINT ( 'NONE',  ( 2.765633920072239071, -12.59161484032927092, 21.30679549418627161 ) ) ;
#11505=B_SPLINE_CURVE_WITH_KNOTS ( 'NONE', 3,
 ( #13489, #1096, #7070, #16403, #10108, #5881 ),
 .UNSPECIFIED., .F., .F.,
 ( 4, 2, 4 ),
 ( 2.586195665722962057E-07, 0.001878649493629687504, 0.003757040367692802973 ),
 .UNSPECIFIED. ) ;
#11511=CARTESIAN_POINT ( 'NONE',  ( 0.000000000000000000, 1.991882183130641248, -24.04302995059964942 ) ) ;
#11513=CARTESIAN_POINT ( 'NONE',  ( 2.783025306068355853, -16.17543236988001354, 18.43727551351025795 ) ) ;
#11515=DIRECTION ( 'NONE',  ( -1.000000000000000000, -0.000000000000000000, -0.000000000000000000 ) ) ;
#11516=CARTESIAN_POINT ( 'NONE',  ( 1.749999999999998002, 0.000000000000000000, 0.000000000000000000 ) ) ;
#11519=EDGE_CURVE ( 'NONE', #17056, #8643, #12231, .T. ) ;
#11524=CARTESIAN_POINT ( 'NONE',  ( 2.262072769566603636, 24.43806413951692136, -11.57956866523193185 ) ) ;
#11533=AXIS2_PLACEMENT_3D ( 'NONE', #1102, #998, #5588 ) ;
#11534=EDGE_CURVE ( 'NONE', #9486, #2268, #10137, .T. ) ;
#11538=CARTESIAN_POINT ( 'NONE',  ( 0.006931111373680289185, 9.685942809247373830, -22.53293026234493723 ) ) ;
#11543=ORIENTED_EDGE ( 'NONE', *, *, #4801, .F. ) ;
#11546=FACE_OUTER_BOUND ( 'NONE', #2191, .T. ) ;
#11548=ORIENTED_EDGE ( 'NONE', *, *, #3825, .F. ) ;
#11554=DIRECTION ( 'NONE',  ( -1.000000000000000000, -0.000000000000000000, -0.000000000000000000 ) ) ;
#11555=ORIENTED_EDGE ( 'NONE', *, *, #1863, .F. ) ;
#11562=VECTOR ( 'NONE', #4018, 1000.000000000000000 ) ;
#11564=ORIENTED_EDGE ( 'NONE', *, *, #263, .T. ) ;
#11576=DIRECTION ( 'NONE',  ( 0.000000000000000000, 1.374038396813314756E-15, -1.000000000000000000 ) ) ;
#11580=DIRECTION ( 'NONE',  ( 0.000000000000000000, 0.000000000000000000, 1.000000000000000000 ) ) ;
#11588=FACE_OUTER_BOUND ( 'NONE', #14409, .T. ) ;
#11589=CARTESIAN_POINT ( 'NONE',  ( 2.783025336474041378, -12.53640742967737332, -21.08118142846917209 ) ) ;
#11592=DIRECTION ( 'NONE',  ( -1.000000000000000000, 0.000000000000000000, 0.000000000000000000 ) ) ;
#11593=FACE_OUTER_BOUND ( 'NONE', #11894, .T. ) ;
#11605=CARTESIAN_POINT ( 'NONE',  ( 0.02436607992776064838, 5.391175441198615914, 24.15498966839965078 ) ) ;
#11607=AXIS2_PLACEMENT_3D ( 'NONE', #4608, #5994, #1707 ) ;
#11609=DIRECTION ( 'NONE',  ( 0.000000000000000000, 0.000000000000000000, 1.000000000000000000 ) ) ;
#11611=LINE ( 'NONE', #9736, #13616 ) ;
#11614=VERTEX_POINT ( 'NONE', #10877 ) ;
#11615=DIRECTION ( 'NONE',  ( -1.000000000000000000, -0.000000000000000000, -0.000000000000000000 ) ) ;
#11620=DIRECTION ( 'NONE',  ( 0.000000000000000000, 0.000000000000000000, 1.000000000000000000 ) ) ;
#11621=EDGE_CURVE ( 'NONE', #13895, #4324, #4060, .T. ) ;
#11626=EDGE_CURVE ( 'NONE', #9660, #2276, #17167, .T. ) ;
#11630=CIRCLE ( 'NONE', #17746, 24.12539914357697768 ) ;
#11631=CYLINDRICAL_SURFACE ( 'NONE', #12203, 13.19999999999999929 ) ;
#11637=TOROIDAL_SURFACE ( 'NONE', #7787, 24.12539914357697413, 8.000000000000000000 ) ;
#11638=VERTEX_POINT ( 'NONE', #15384 ) ;
#11641=EDGE_LOOP ( 'NONE', ( #3051, #1233, #15649, #16333 ) ) ;
#11642=FACE_OUTER_BOUND ( 'NONE', #1086, .T. ) ;
#11645=CARTESIAN_POINT ( 'NONE',  ( 1.749999999999998002, -19.67366047555544739, 20.02152543075338897 ) ) ;
#11647=CIRCLE ( 'NONE', #6515, 24.12539914357697413 ) ;
#11650=ORIENTED_EDGE ( 'NONE', *, *, #19364, .F. ) ;
#11659=ORIENTED_EDGE ( 'NONE', *, *, #2355, .T. ) ;
#11662=DIRECTION ( 'NONE',  ( -1.000000000000000000, 0.000000000000000000, 0.000000000000000000 ) ) ;
#11669=ORIENTED_EDGE ( 'NONE', *, *, #5159, .F. ) ;
#11676=VERTEX_POINT ( 'NONE', #1964 ) ;
#11681=DIRECTION ( 'NONE',  ( -1.000000000000000000, -0.000000000000000000, -0.000000000000000000 ) ) ;
#11684=CYLINDRICAL_SURFACE ( 'NONE', #8386, 13.19999999999999929 ) ;
#11687=B_SPLINE_CURVE_WITH_KNOTS ( 'NONE', 3,
 ( #7092, #19124, #8713, #13031, #19312, #11338 ),
 .UNSPECIFIED., .F., .F.,
 ( 4, 2, 4 ),
 ( 1.979325885420528755E-07, 0.001878588715165608204, 0.003756979497742674035 ),
 .UNSPECIFIED. ) ;
#11689=EDGE_CURVE ( 'NONE', #16591, #4589, #1282, .T. ) ;
#11691=FACE_OUTER_BOUND ( 'NONE', #10223, .T. ) ;
#11701=TOROIDAL_SURFACE ( 'NONE', #5619, 24.12539914357697413, 8.000000000000000000 ) ;
#11703=DIRECTION ( 'NONE',  ( 0.000000000000000000, -1.000000000000000000, -4.122115190439943875E-15 ) ) ;
#11704=DIRECTION ( 'NONE',  ( -1.000000000000000000, -0.000000000000000000, -0.000000000000000000 ) ) ;
#11705=ORIENTED_EDGE ( 'NONE', *, *, #4899, .F. ) ;
#11706=CARTESIAN_POINT ( 'NONE',  ( 2.765633920072235075, 24.63872515616082737, -2.336989772644355590 ) ) ;
#11710=VERTEX_POINT ( 'NONE', #2062 ) ;
#11712=DIRECTION ( 'NONE',  ( 0.000000000000000000, 0.000000000000000000, 1.000000000000000000 ) ) ;
#11715=CARTESIAN_POINT ( 'NONE',  ( 0.1855654851361731306, -10.67816411292181655, 23.63475234378979195 ) ) ;
#11716=ADVANCED_FACE ( 'NONE', ( #10148 ), #14745, .T. ) ;
#11721=ORIENTED_EDGE ( 'NONE', *, *, #1055, .F. ) ;
#11724=EDGE_LOOP ( 'NONE', ( #4416, #7452, #2697, #12988, #520, #1551, #19504 ) ) ;
#11726=EDGE_CURVE ( 'NONE', #11007, #8766, #3099, .T. ) ;
#11741=DIRECTION ( 'NONE',  ( -1.000000000000000000, 0.000000000000000000, 0.000000000000000000 ) ) ;
#11743=EDGE_CURVE ( 'NONE', #10395, #6118, #3562, .T. ) ;
#11744=CYLINDRICAL_SURFACE ( 'NONE', #1318, 13.19999999999999929 ) ;
#11749=VECTOR ( 'NONE', #17364, 1000.000000000000000 ) ;
#11753=B_SPLINE_CURVE_WITH_KNOTS ( 'NONE', 3,
 ( #3140, #239, #15259, #15357 ),
 .UNSPECIFIED., .F., .F.,
 ( 4, 4 ),
 ( 0.005258139959819225183, 0.005948405594583413246 ),
 .UNSPECIFIED. ) ;
#11755=DIRECTION ( 'NONE',  ( 0.000000000000000000, 0.000000000000000000, 1.000000000000000000 ) ) ;
#11757=AXIS2_PLACEMENT_3D ( 'NONE', #15045, #18149, #4732 ) ;
#11759=ORIENTED_EDGE ( 'NONE', *, *, #18562, .T. ) ;
#11760=FACE_OUTER_BOUND ( 'NONE', #9606, .T. ) ;
#11763=EDGE_CURVE ( 'NONE', #10072, #8830, #7929, .T. ) ;
#11781=CARTESIAN_POINT ( 'NONE',  ( -10.00000000000000000, 0.000000000000000000, 0.000000000000000000 ) ) ;
#11782=CARTESIAN_POINT ( 'NONE',  ( 2.789999999999999147, 5.535312321043049266, -23.48180575137724446 ) ) ;
#11788=EDGE_LOOP ( 'NONE', ( #12961, #2474, #11398, #6901 ) ) ;
#11790=CARTESIAN_POINT ( 'NONE',  ( -10.00000000000000000, 0.000000000000000000, 0.000000000000000000 ) ) ;
#11795=CARTESIAN_POINT ( 'NONE',  ( 0.02436607992776151574, 24.15498966839970052, -5.391175441198366336 ) ) ;
#11797=LINE ( 'NONE', #4097, #17951 ) ;
#11803=B_SPLINE_CURVE_WITH_KNOTS ( 'NONE', 3,
 ( #10291, #16387, #17591, #3879, #8581, #19379 ),
 .UNSPECIFIED., .F., .F.,
 ( 4, 2, 4 ),
 ( 4.462636678113234028E-07, 0.001879885020955180275, 0.003759323778242549142 ),
 .UNSPECIFIED. ) ;
#11813=VERTEX_POINT ( 'NONE', #6117 ) ;
#11823=B_SPLINE_CURVE_WITH_KNOTS ( 'NONE', 3,
 ( #19329, #14935, #1226, #2618 ),
 .UNSPECIFIED., .F., .F.,
 ( 4, 4 ),
 ( 2.034713381942770033E-07, 0.0006045424356928436873 ),
 .UNSPECIFIED. ) ;
#11829=CARTESIAN_POINT ( 'NONE',  ( 0.006974674093433583938, -24.42374957165207405, 2.249040938978413173 ) ) ;
#11834=FACE_OUTER_BOUND ( 'NONE', #18037, .T. ) ;
#11836=CARTESIAN_POINT ( 'NONE',  ( 0.02436607992775891365, -24.63872515616080960, -2.336989772644527008 ) ) ;
#11860=DIRECTION ( 'NONE',  ( 0.000000000000000000, 0.000000000000000000, 1.000000000000000000 ) ) ;
#11867=EDGE_CURVE ( 'NONE', #14187, #13278, #15356, .T. ) ;
#11871=FACE_OUTER_BOUND ( 'NONE', #17973, .T. ) ;
#11875=DIRECTION ( 'NONE',  ( -1.000000000000000000, -0.000000000000000000, -0.000000000000000000 ) ) ;
#11876=VECTOR ( 'NONE', #810, 1000.000000000000000 ) ;
#11877=EDGE_CURVE ( 'NONE', #59, #16209, #5560, .T. ) ;
#11878=CARTESIAN_POINT ( 'NONE',  ( 2.789999999999999147, -18.28042085475289369, 15.74360496233375173 ) ) ;
#11884=EDGE_CURVE ( 'NONE', #15571, #6035, #326, .T. ) ;
#11886=TOROIDAL_SURFACE ( 'NONE', #77, 24.12539914357697413, 8.000000000000000000 ) ;
#11888=AXIS2_PLACEMENT_3D ( 'NONE', #4758, #12372, #3362 ) ;
#11891=CARTESIAN_POINT ( 'NONE',  ( 2.790000000000077307, -9.515416771311352662, 22.38018801136472646 ) ) ;
#11894=EDGE_LOOP ( 'NONE', ( #6540, #3665, #6754, #13455 ) ) ;
#11896=CARTESIAN_POINT ( 'NONE',  ( 2.765633920072239071, -12.59161484032927092, 21.30679549418627161 ) ) ;
#11898=ORIENTED_EDGE ( 'NONE', *, *, #14663, .F. ) ;
#11901=AXIS2_PLACEMENT_3D ( 'NONE', #14168, #15478, #6544 ) ;
#11903=CARTESIAN_POINT ( 'NONE',  ( 1.039999999999995595, 4.147968289691676524, -27.76164181293047051 ) ) ;
#11906=AXIS2_PLACEMENT_3D ( 'NONE', #2230, #2035, #338 ) ;
#11908=CARTESIAN_POINT ( 'NONE',  ( 2.789999999999999147, 9.836394144776026138, -22.71065055754441531 ) ) ;
#11909=EDGE_CURVE ( 'NONE', #19366, #1940, #17812, .T. ) ;
#11913=ORIENTED_EDGE ( 'NONE', *, *, #12709, .T. ) ;
#11915=ORIENTED_EDGE ( 'NONE', *, *, #16085, .T. ) ;
#11921=ORIENTED_EDGE ( 'NONE', *, *, #6148, .F. ) ;
#11934=LINE ( 'NONE', #1431, #18863 ) ;
#11936=CARTESIAN_POINT ( 'NONE',  ( 2.601776121706763423, 19.18368891937490517, 17.47009390565497711 ) ) ;
#11944=EDGE_CURVE ( 'NONE', #6719, #9660, #16069, .T. ) ;
#11946=CARTESIAN_POINT ( 'NONE',  ( 2.031033479673587827, -19.12621924769852555, -19.86422722021333342 ) ) ;
#11948=CARTESIAN_POINT ( 'NONE',  ( 2.601776105308176046, -2.857713464478872201, 25.78859396478526733 ) ) ;
#11956=FACE_OUTER_BOUND ( 'NONE', #18903, .T. ) ;
#11969=EDGE_CURVE ( 'NONE', #540, #17188, #18827, .T. ) ;
#11970=CIRCLE ( 'NONE', #8135, 28.06981291497571007 ) ;
#11971=ORIENTED_EDGE ( 'NONE', *, *, #453, .F. ) ;
#11976=B_SPLINE_CURVE_WITH_KNOTS ( 'NONE', 3,
 ( #3974, #12784, #5367, #19268, #9795, #18980 ),
 .UNSPECIFIED., .F., .F.,
 ( 4, 2, 4 ),
 ( 4.462636695653741059E-07, 0.001879885036799761782, 0.003759323809929957915 ),
 .UNSPECIFIED. ) ;
#11984=CARTESIAN_POINT ( 'NONE',  ( 1.394999999999999574, 27.68468304288259318, 4.633866840649019103 ) ) ;
#11988=AXIS2_PLACEMENT_3D ( 'NONE', #11291, #11484, #11580 ) ;
#11989=DIRECTION ( 'NONE',  ( -1.000000000000000000, 0.000000000000000000, -0.000000000000000000 ) ) ;
#11999=VERTEX_POINT ( 'NONE', #227 ) ;
#12000=B_SPLINE_CURVE_WITH_KNOTS ( 'NONE', 3,
 ( #9506, #7985, #15508, #3493 ),
 .UNSPECIFIED., .F., .F.,
 ( 4, 4 ),
 ( 4.462636695580848051E-07, 0.0004963285629697519611 ),
 .UNSPECIFIED. ) ;
#12002=AXIS2_PLACEMENT_3D ( 'NONE', #18437, #7624, #4730 ) ;
#12003=B_SPLINE_CURVE_WITH_KNOTS ( 'NONE', 3,
 ( #5792, #8911, #2599, #2696, #16418, #15014 ),
 .UNSPECIFIED., .F., .F.,
 ( 4, 2, 4 ),
 ( 2.032124546190077199E-07, 0.001878594002992309232, 0.003756984793529999193 ),
 .UNSPECIFIED. ) ;
#12005=CARTESIAN_POINT ( 'NONE',  ( 0.02436607992776455150, 21.30679549418631780, 12.59161484032919986 ) ) ;
#12006=LINE ( 'NONE', #4201, #18647 ) ;
#12012=EDGE_LOOP ( 'NONE', ( #9637, #16152, #17733, #6195 ) ) ;
#12014=ORIENTED_EDGE ( 'NONE', *, *, #1520, .T. ) ;
#12020=LINE ( 'NONE', #7093, #11562 ) ;
#12023=CIRCLE ( 'NONE', #15226, 28.06981291497571362 ) ;
#12035=EDGE_CURVE ( 'NONE', #19497, #6719, #6756, .T. ) ;
#12043=CARTESIAN_POINT ( 'NONE',  ( 2.789999999999999147, 1.991882183130632589, -24.04302995059963877 ) ) ;
#12051=VECTOR ( 'NONE', #4804, 1000.000000000000000 ) ;
#12053=EDGE_CURVE ( 'NONE', #15383, #3340, #14623, .T. ) ;
#12056=CARTESIAN_POINT ( 'NONE',  ( -5.209999999999999964, 0.000000000000000000, 0.000000000000000000 ) ) ;
#12063=AXIS2_PLACEMENT_3D ( 'NONE', #10418, #2895, #15116 ) ;
#12066=CARTESIAN_POINT ( 'NONE',  ( 1.394999999999999574, -24.89775460606823287, -12.96210679857813908 ) ) ;
#12069=ORIENTED_EDGE ( 'NONE', *, *, #1341, .F. ) ;
#12074=CARTESIAN_POINT ( 'NONE',  ( 0.07186815222488067423, -24.78765742476142719, 5.344160105508607650 ) ) ;
#12075=ORIENTED_EDGE ( 'NONE', *, *, #3034, .F. ) ;
#12078=EDGE_CURVE ( 'NONE', #6035, #4236, #14630, .T. ) ;
#12080=ORIENTED_EDGE ( 'NONE', *, *, #1128, .T. ) ;
#12084=LINE ( 'NONE', #10486, #16762 ) ;
#12085=CARTESIAN_POINT ( 'NONE',  ( 0.02436607992775717893, -9.836394144775869819, 22.71065055754449347 ) ) ;
#12087=CARTESIAN_POINT ( 'NONE',  ( 1.749999999999998002, 0.000000000000000000, 0.000000000000000000 ) ) ;
#12089=ORIENTED_EDGE ( 'NONE', *, *, #503, .F. ) ;
#12098=DIRECTION ( 'NONE',  ( -1.000000000000000000, 0.000000000000000000, 0.000000000000000000 ) ) ;
#12107=DIRECTION ( 'NONE',  ( -1.000000000000000000, -0.000000000000000000, 0.000000000000000000 ) ) ;
#12113=ORIENTED_EDGE ( 'NONE', *, *, #8123, .F. ) ;
#12119=AXIS2_PLACEMENT_3D ( 'NONE', #11162, #14361, #3548 ) ;
#12120=B_SPLINE_CURVE_WITH_KNOTS ( 'NONE', 3,
 ( #13084, #19178, #5471, #975, #3681, #16097 ),
 .UNSPECIFIED., .F., .F.,
 ( 4, 2, 4 ),
 ( 2.586195665736120714E-07, 0.001878649493629690539, 0.003757040367692807744 ),
 .UNSPECIFIED. ) ;
#12125=DIRECTION ( 'NONE',  ( 0.000000000000000000, 0.000000000000000000, 1.000000000000000000 ) ) ;
#12127=EDGE_CURVE ( 'NONE', #19487, #1162, #19721, .T. ) ;
#12136=ORIENTED_EDGE ( 'NONE', *, *, #17837, .F. ) ;
#12138=ORIENTED_EDGE ( 'NONE', *, *, #2486, .F. ) ;
#12143=CARTESIAN_POINT ( 'NONE',  ( 1.960886852992497653, -24.44424927289185590, 12.96989951879399072 ) ) ;
#12144=EDGE_CURVE ( 'NONE', #9713, #13429, #2238, .T. ) ;
#12150=EDGE_CURVE ( 'NONE', #19072, #253, #1029, .T. ) ;
#12156=ORIENTED_EDGE ( 'NONE', *, *, #6435, .T. ) ;
#12157=FACE_OUTER_BOUND ( 'NONE', #7139, .T. ) ;
#12160=ORIENTED_EDGE ( 'NONE', *, *, #10260, .T. ) ;
#12168=CARTESIAN_POINT ( 'NONE',  ( 0.7592463834391185440, 12.05220173035438513, 24.80264696524887214 ) ) ;
#12171=ORIENTED_EDGE ( 'NONE', *, *, #10817, .T. ) ;
#12173=VERTEX_POINT ( 'NONE', #3817 ) ;
#12185=CARTESIAN_POINT ( 'NONE',  ( 0.000000000000000000, 0.000000000000000000, 0.000000000000000000 ) ) ;
#12186=CARTESIAN_POINT ( 'NONE',  ( 0.1882238946918228795, -25.78859396478530641, 2.857713464478602194 ) ) ;
#12200=CARTESIAN_POINT ( 'NONE',  ( 0.07186813532171051899, 2.577209017047360717, -25.22589920183358814 ) ) ;
#12202=ORIENTED_EDGE ( 'NONE', *, *, #16901, .T. ) ;
#12203=AXIS2_PLACEMENT_3D ( 'NONE', #17734, #4027, #5331 ) ;
#12205=CARTESIAN_POINT ( 'NONE',  ( 2.765633920072238183, 2.336989772644269436, 24.63872515616083447 ) ) ;
#12206=FILL_AREA_STYLE ('',( #16714 ) ) ;
#12208=CIRCLE ( 'NONE', #3574, 24.12539914357697768 ) ;
#12210=ORIENTED_EDGE ( 'NONE', *, *, #9972, .F. ) ;
#12211=DIRECTION ( 'NONE',  ( 0.000000000000000000, -0.9510565162951523099, -0.3090169943749515591 ) ) ;
#12212=CARTESIAN_POINT ( 'NONE',  ( 2.765633920072242624, 9.836394144775706394, 22.71065055754456097 ) ) ;
#12213=CARTESIAN_POINT ( 'NONE',  ( 2.789999999999999147, 0.000000000000000000, 0.000000000000000000 ) ) ;
#12214=( GEOMETRIC_REPRESENTATION_CONTEXT ( 3 ) GLOBAL_UNCERTAINTY_ASSIGNED_CONTEXT ( ( #10224 ) ) GLOBAL_UNIT_ASSIGNED_CONTEXT ( ( #13882, #363, #5064 ) ) REPRESENTATION_CONTEXT ( 'NONE', 'WORKASPACE' ) );
#12218=B_SPLINE_CURVE_WITH_KNOTS ( 'NONE', 3,
 ( #2368, #874, #16555, #13077, #11946, #19171 ),
 .UNSPECIFIED., .F., .F.,
 ( 4, 2, 4 ),
 ( 2.321268216997094965E-07, 0.001878622960950495756, 0.003757013795079291486 ),
 .UNSPECIFIED. ) ;
#12227=CIRCLE ( 'NONE', #19241, 28.06981291497571007 ) ;
#12231=B_SPLINE_CURVE_WITH_KNOTS ( 'NONE', 3,
 ( #1477, #18671, #7663, #7769, #16688, #15289 ),
 .UNSPECIFIED., .F., .F.,
 ( 4, 2, 4 ),
 ( 2.321268216997199256E-07, 0.001878622960950494455, 0.003757013795079288884 ),
 .UNSPECIFIED. ) ;
#12234=B_SPLINE_CURVE_WITH_KNOTS ( 'NONE', 3,
 ( #18289, #272, #18577, #6449, #9583, #17183 ),
 .UNSPECIFIED., .F., .F.,
 ( 4, 2, 4 ),
 ( 4.462636695616422376E-07, 0.001879885036799763083, 0.003759323809929964420 ),
 .UNSPECIFIED. ) ;
#12237=CYLINDRICAL_SURFACE ( 'NONE', #10244, 28.06981291497571362 ) ;
#12238=ORIENTED_EDGE ( 'NONE', *, *, #465, .T. ) ;
#12239=CARTESIAN_POINT ( 'NONE',  ( 0.006974674093433516284, 24.42374957165205629, -2.249040938978583259 ) ) ;
#12241=ORIENTED_EDGE ( 'NONE', *, *, #1674, .F. ) ;
#12242=CARTESIAN_POINT ( 'NONE',  ( 2.765633920072236407, 2.336989772644613161, -24.63872515616080250 ) ) ;
#12245=DIRECTION ( 'NONE',  ( 0.000000000000000000, 0.000000000000000000, 1.000000000000000000 ) ) ;
#12247=AXIS2_PLACEMENT_3D ( 'NONE', #12056, #39, #1546 ) ;
#12248=LINE ( 'NONE', #9242, #8878 ) ;
#12249=ORIENTED_EDGE ( 'NONE', *, *, #2710, .F. ) ;
#12250=CARTESIAN_POINT ( 'NONE',  ( 2.765633920072238183, -5.391175441198789109, 24.15498966839961170 ) ) ;
#12255=DIRECTION ( 'NONE',  ( -1.000000000000000000, -0.000000000000000000, 0.000000000000000000 ) ) ;
#12256=VERTEX_POINT ( 'NONE', #18024 ) ;
#12261=ORIENTED_EDGE ( 'NONE', *, *, #9329, .T. ) ;
#12265=VERTEX_POINT ( 'NONE', #13405 ) ;
#12266=CARTESIAN_POINT ( 'NONE',  ( 0.5321745087963408727, 11.58891744060107065, 24.44564404695848836 ) ) ;
#12270=EDGE_CURVE ( 'NONE', #14758, #6823, #570, .T. ) ;
#12271=EDGE_CURVE ( 'NONE', #7096, #17509, #2462, .T. ) ;
#12274=B_SPLINE_CURVE_WITH_KNOTS ( 'NONE', 3,
 ( #15651, #242, #3238, #7738, #10754, #1842 ),
 .UNSPECIFIED., .F., .F.,
 ( 4, 2, 4 ),
 ( 4.462636677693390501E-07, 0.001879885020955137558, 0.003759323778242505774 ),
 .UNSPECIFIED. ) ;
#12275=ORIENTED_EDGE ( 'NONE', *, *, #3006, .F. ) ;
#12281=ADVANCED_FACE ( 'NONE', ( #8710 ), #17916, .T. ) ;
#12283=VERTEX_POINT ( 'NONE', #8812 ) ;
#12291=LINE ( 'NONE', #18094, #2344 ) ;
#12293=CARTESIAN_POINT ( 'NONE',  ( 2.171938186095908829, 23.93436800624300886, 12.96259772325185544 ) ) ;
#12297=CARTESIAN_POINT ( 'NONE',  ( 2.789999999999999147, 2.680914349914567470E-13, -25.59481291497571220 ) ) ;
#12299=ORIENTED_EDGE ( 'NONE', *, *, #11743, .F. ) ;
#12303=LINE ( 'NONE', #8080, #12808 ) ;
#12305=CARTESIAN_POINT ( 'NONE',  ( 2.789999999999999147, -23.48180575137726223, -5.535312321042966666 ) ) ;
#12307=EDGE_CURVE ( 'NONE', #9684, #4759, #12003, .T. ) ;
#12308=AXIS2_PLACEMENT_3D ( 'NONE', #18539, #12914, #9448 ) ;
#12314=ORIENTED_EDGE ( 'NONE', *, *, #16337, .F. ) ;
#12319=CARTESIAN_POINT ( 'NONE',  ( 1.394999999999999574, -12.52377138324206740, -25.12109765559666741 ) ) ;
#12321=CARTESIAN_POINT ( 'NONE',  ( 2.783025306068356297, 16.17543236988015209, -18.43727551351014071 ) ) ;
#12323=CARTESIAN_POINT ( 'NONE',  ( 1.394999999999999574, -27.76164181293054511, 4.147968289691193355 ) ) ;
#12327=VECTOR ( 'NONE', #2078, 1000.000000000000000 ) ;
#12328=EDGE_LOOP ( 'NONE', ( #10882, #3884, #6957, #13551 ) ) ;
#12334=DIRECTION ( 'NONE',  ( 0.000000000000000000, 0.000000000000000000, 1.000000000000000000 ) ) ;
#12337=CYLINDRICAL_SURFACE ( 'NONE', #4790, 2.524999999999995914 ) ;
#12340=VERTEX_POINT ( 'NONE', #14914 ) ;
#12341=CARTESIAN_POINT ( 'NONE',  ( 8.000000000000000000, 0.000000000000000000, 0.000000000000000000 ) ) ;
#12344=DIRECTION ( 'NONE',  ( 0.000000000000000000, 0.000000000000000000, 1.000000000000000000 ) ) ;
#12346=VERTEX_POINT ( 'NONE', #1208 ) ;
#12347=CARTESIAN_POINT ( 'NONE',  ( 0.4314184204727332661, 23.43037373958377501, 12.94152279942384709 ) ) ;
#12348=DIRECTION ( 'NONE',  ( -1.000000000000000000, -0.000000000000000000, -0.000000000000000000 ) ) ;
#12362=CARTESIAN_POINT ( 'NONE',  ( 0.0001048950922011769414, -20.67847077765692632, -12.51925356660783351 ) ) ;
#12363=EDGE_LOOP ( 'NONE', ( #19339, #17659, #6026, #5066 ) ) ;
#12367=ORIENTED_EDGE ( 'NONE', *, *, #13201, .F. ) ;
#12368=CARTESIAN_POINT ( 'NONE',  ( 0.000000000000000000, 24.04302995059966364, -1.991882183130399664 ) ) ;
#12372=DIRECTION ( 'NONE',  ( 1.000000000000000000, 0.000000000000000000, 0.000000000000000000 ) ) ;
#12377=CARTESIAN_POINT ( 'NONE',  ( -5.209999999999999964, 0.000000000000000000, 0.000000000000000000 ) ) ;
#12379=CARTESIAN_POINT ( 'NONE',  ( 2.718131853594929037, -12.74240566898999383, 21.92302674874958868 ) ) ;
#12381=ORIENTED_EDGE ( 'NONE', *, *, #985, .F. ) ;
#12387=CYLINDRICAL_SURFACE ( 'NONE', #17841, 13.19999999999999929 ) ;
#12390=EDGE_CURVE ( 'NONE', #15288, #10168, #2918, .T. ) ;
#12400=ADVANCED_FACE ( 'NONE', ( #10809 ), #15906, .T. ) ;
#12409=VECTOR ( 'NONE', #515, 1000.000000000000000 ) ;
#12417=DIRECTION ( 'NONE',  ( -1.000000000000000000, -0.000000000000000000, -0.000000000000000000 ) ) ;
#12419=ORIENTED_EDGE ( 'NONE', *, *, #3552, .F. ) ;
#12427=ORIENTED_EDGE ( 'NONE', *, *, #3622, .T. ) ;
#12439=CARTESIAN_POINT ( 'NONE',  ( 0.02436607992776541887, 12.59161484032942901, -21.30679549418617924 ) ) ;
#12442=CARTESIAN_POINT ( 'NONE',  ( 2.789999999999999147, -7.334849878007672963, 23.31896751603329676 ) ) ;
#12443=EDGE_CURVE ( 'NONE', #18676, #16730, #14002, .T. ) ;
#12445=AXIS2_PLACEMENT_3D ( 'NONE', #11372, #9976, #955 ) ;
#12446=ORIENTED_EDGE ( 'NONE', *, *, #3486, .T. ) ;
#12447=CARTESIAN_POINT ( 'NONE',  ( 2.257825467309741541, 3.467596033028661928, -26.83036154824990760 ) ) ;
#12451=CARTESIAN_POINT ( 'NONE',  ( 2.030753616560877717, 12.05220173035473863, -24.80264696524870516 ) ) ;
#12454=DIRECTION ( 'NONE',  ( 0.000000000000000000, 0.000000000000000000, 1.000000000000000000 ) ) ;
#12460=EDGE_CURVE ( 'NONE', #19497, #5656, #10494, .T. ) ;
#12469=EDGE_LOOP ( 'NONE', ( #12977, #1000, #8545, #2958 ) ) ;
#12474=AXIS2_PLACEMENT_3D ( 'NONE', #2640, #18062, #11755 ) ;
#12478=VERTEX_POINT ( 'NONE', #13908 ) ;
#12479=EDGE_CURVE ( 'NONE', #14825, #2982, #10801, .T. ) ;
#12483=CARTESIAN_POINT ( 'NONE',  ( 0.000000000000000000, 15.74360496233383522, 18.28042085475283329 ) ) ;
#12489=CYLINDRICAL_SURFACE ( 'NONE', #1972, 2.524999999999996358 ) ;
#12493=ORIENTED_EDGE ( 'NONE', *, *, #6847, .T. ) ;
#12497=CARTESIAN_POINT ( 'NONE',  ( -7.723595606797438030E-14, -23.69897269326674305, -5.456611084822102775 ) ) ;
#12499=CARTESIAN_POINT ( 'NONE',  ( 0.006930995026450773554, -23.92277630352799278, 5.408431875071351591 ) ) ;
#12504=ORIENTED_EDGE ( 'NONE', *, *, #16475, .T. ) ;
#12511=AXIS2_PLACEMENT_3D ( 'NONE', #9964, #2433, #8349 ) ;
#12514=CARTESIAN_POINT ( 'NONE',  ( 2.790000000000078639, 15.96555658743789152, -18.34439787333489136 ) ) ;
#12517=ORIENTED_EDGE ( 'NONE', *, *, #8685, .T. ) ;
#12520=ORIENTED_EDGE ( 'NONE', *, *, #14817, .F. ) ;
#12522=AXIS2_PLACEMENT_3D ( 'NONE', #9618, #3412, #4811 ) ;
#12525=CARTESIAN_POINT ( 'NONE',  ( 1.749999999999998002, -20.02152543075360214, 19.67366047555523068 ) ) ;
#12530=ORIENTED_EDGE ( 'NONE', *, *, #12572, .F. ) ;
#12532=ORIENTED_EDGE ( 'NONE', *, *, #2734, .F. ) ;
#12537=DIRECTION ( 'NONE',  ( -1.000000000000000000, -0.000000000000000000, -0.000000000000000000 ) ) ;
#12539=CARTESIAN_POINT ( 'NONE',  ( 2.789999999999999147, 0.000000000000000000, 0.000000000000000000 ) ) ;
#12546=CARTESIAN_POINT ( 'NONE',  ( 2.765633920072242624, 9.836394144775706394, 22.71065055754456097 ) ) ;
#12550=VERTEX_POINT ( 'NONE', #11200 ) ;
#12561=VERTEX_POINT ( 'NONE', #13195 ) ;
#12568=ORIENTED_EDGE ( 'NONE', *, *, #18519, .T. ) ;
#12569=CARTESIAN_POINT ( 'NONE',  ( 0.5279273746168616777, 26.57710921259767645, -4.996265754456091557 ) ) ;
#12570=CARTESIAN_POINT ( 'NONE',  ( 2.789999999999999147, -9.836394144775550075, -22.71065055754462492 ) ) ;
#12572=EDGE_CURVE ( 'NONE', #13180, #5891, #549, .T. ) ;
#12573=CARTESIAN_POINT ( 'NONE',  ( 2.030753616560879493, 24.80264696524883306, 12.05220173035447750 ) ) ;
#12578=DIRECTION ( 'NONE',  ( -1.000000000000000000, -0.000000000000000000, -0.000000000000000000 ) ) ;
#12585=CARTESIAN_POINT ( 'NONE',  ( 2.765633920072238627, 5.391175441198956086, -24.15498966839956907 ) ) ;
#12589=ORIENTED_EDGE ( 'NONE', *, *, #16372, .F. ) ;
#12591=DIRECTION ( 'NONE',  ( -1.000000000000000000, -0.000000000000000000, -0.000000000000000000 ) ) ;
#12596=ADVANCED_FACE ( 'NONE', ( #11399 ), #2090, .T. ) ;
#12602=CARTESIAN_POINT ( 'NONE',  ( -1.906188514513426096E-16, -24.22479935914659066, -2.133490293297270579 ) ) ;
#12616=CARTESIAN_POINT ( 'NONE',  ( 0.006974657972265005043, 23.92335783895637746, 5.408388659524176134 ) ) ;
#12620=FACE_OUTER_BOUND ( 'NONE', #16662, .T. ) ;
#12623=AXIS2_PLACEMENT_3D ( 'NONE', #6320, #12348, #15352 ) ;
#12627=DIRECTION ( 'NONE',  ( -1.000000000000000000, -0.000000000000000000, -0.000000000000000000 ) ) ;
#12628=CARTESIAN_POINT ( 'NONE',  ( 1.039999999999999369, -12.52377138324206918, -25.12109765559666741 ) ) ;
#12636=CARTESIAN_POINT ( 'NONE',  ( 2.765633920072238183, 2.336989772644269436, 24.63872515616083447 ) ) ;
#12637=DIRECTION ( 'NONE',  ( -1.000000000000000000, 0.000000000000000000, -0.000000000000000000 ) ) ;
#12642=ORIENTED_EDGE ( 'NONE', *, *, #3261, .T. ) ;
#12643=CARTESIAN_POINT ( 'NONE',  ( 0.6102186610125081012, 23.94322454545469370, 12.96989951879415770 ) ) ;
#12644=ADVANCED_FACE ( 'NONE', ( #14988 ), #1385, .F. ) ;
#12645=CARTESIAN_POINT ( 'NONE',  ( 2.790000000000000924, 0.000000000000000000, 0.000000000000000000 ) ) ;
#12650=CARTESIAN_POINT ( 'NONE',  ( 2.789999999999999147, 22.25075486061751207, -9.324097380959219805 ) ) ;
#12655=VECTOR ( 'NONE', #11235, 1000.000000000000000 ) ;
#12656=ORIENTED_EDGE ( 'NONE', *, *, #2168, .F. ) ;
#12660=CARTESIAN_POINT ( 'NONE',  ( -5.209999999999999964, 0.000000000000000000, 0.000000000000000000 ) ) ;
#12662=EDGE_LOOP ( 'NONE', ( #3427, #10442, #2914, #11140, #12113, #3029, #4835 ) ) ;
#12666=ORIENTED_EDGE ( 'NONE', *, *, #2486, .T. ) ;
#12669=VECTOR ( 'NONE', #721, 1000.000000000000000 ) ;
#12677=B_SPLINE_CURVE_WITH_KNOTS ( 'NONE', 3,
 ( #14574, #10265, #1054, #7133 ),
 .UNSPECIFIED., .F., .F.,
 ( 4, 4 ),
 ( 0.005258110598983630792, 0.005948376585272738271 ),
 .UNSPECIFIED. ) ;
#12679=CARTESIAN_POINT ( 'NONE',  ( 2.789999999999999147, 0.000000000000000000, 0.000000000000000000 ) ) ;
#12682=ORIENTED_EDGE ( 'NONE', *, *, #11125, .F. ) ;
#12686=VERTEX_POINT ( 'NONE', #15187 ) ;
#12688=DIRECTION ( 'NONE',  ( 0.000000000000000000, 0.000000000000000000, 1.000000000000000000 ) ) ;
#12699=CYLINDRICAL_SURFACE ( 'NONE', #10125, 28.06981291497571362 ) ;
#12700=CARTESIAN_POINT ( 'NONE',  ( 1.039999999999997593, 0.000000000000000000, 0.000000000000000000 ) ) ;
#12701=DIRECTION ( 'NONE',  ( -1.000000000000000000, -0.000000000000000000, 0.000000000000000000 ) ) ;
#12709=EDGE_CURVE ( 'NONE', #8648, #1328, #16233, .T. ) ;
#12712=CARTESIAN_POINT ( 'NONE',  ( 2.780931166827226519, -21.10834851580694504, -12.54305517365643929 ) ) ;
#12715=B_SPLINE_CURVE_WITH_KNOTS ( 'NONE', 3,
 ( #3924, #6909, #8621, #14638, #16034, #11342 ),
 .UNSPECIFIED., .F., .F.,
 ( 4, 2, 4 ),
 ( 4.462636695652347161E-07, 0.001879885036799764601, 0.003759323809929963987 ),
 .UNSPECIFIED. ) ;
#12717=ORIENTED_EDGE ( 'NONE', *, *, #8490, .T. ) ;
#12724=CARTESIAN_POINT ( 'NONE',  ( 0.02436607992776498519, 9.836394144775706394, 22.71065055754456097 ) ) ;
#12729=ORIENTED_EDGE ( 'NONE', *, *, #18615, .F. ) ;
#12730=CARTESIAN_POINT ( 'NONE',  ( 2.765633920072242624, -22.71065055754459650, 9.836394144775621129 ) ) ;
#12731=ORIENTED_EDGE ( 'NONE', *, *, #1951, .T. ) ;
#12733=DIRECTION ( 'NONE',  ( 0.000000000000000000, 0.000000000000000000, 1.000000000000000000 ) ) ;
#12736=CARTESIAN_POINT ( 'NONE',  ( 2.257825477245773982, 18.57583492944447556, -19.66801664102683489 ) ) ;
#12738=CARTESIAN_POINT ( 'NONE',  ( 0.7589665203264061022, 19.86422722021312026, 19.12621924769873161 ) ) ;
#12742=EDGE_CURVE ( 'NONE', #9816, #15555, #4382, .T. ) ;
#12750=DIRECTION ( 'NONE',  ( -1.000000000000000000, -0.000000000000000000, -0.000000000000000000 ) ) ;
#12752=ORIENTED_EDGE ( 'NONE', *, *, #19364, .T. ) ;
#12759=VERTEX_POINT ( 'NONE', #7258 ) ;
#12761=DIRECTION ( 'NONE',  ( -1.000000000000000000, -0.000000000000000000, -0.000000000000000000 ) ) ;
#12764=EDGE_CURVE ( 'NONE', #10294, #17165, #1218, .T. ) ;
#12769=EDGE_CURVE ( 'NONE', #13000, #9369, #17516, .T. ) ;
#12784=CARTESIAN_POINT ( 'NONE',  ( 0.7592463965288823724, -12.98165646470099155, 24.32906614999610895 ) ) ;
#12785=VERTEX_POINT ( 'NONE', #5768 ) ;
#12788=B_SPLINE_CURVE_WITH_KNOTS ( 'NONE', 3,
 ( #11094, #16909, #12497, #14000 ),
 .UNSPECIFIED., .F., .F.,
 ( 4, 4 ),
 ( 1.981826382900849143E-07, 0.0006887856082032019125 ),
 .UNSPECIFIED. ) ;
#12793=AXIS2_PLACEMENT_3D ( 'NONE', #6210, #4924, #14027 ) ;
#12794=EDGE_CURVE ( 'NONE', #8320, #13895, #8436, .T. ) ;
#12803=EDGE_CURVE ( 'NONE', #16376, #10624, #17724, .T. ) ;
#12807=FACE_OUTER_BOUND ( 'NONE', #4989, .T. ) ;
#12808=VECTOR ( 'NONE', #9593, 1000.000000000000000 ) ;
#12810=CIRCLE ( 'NONE', #3852, 2.524999999999996803 ) ;
#12813=CARTESIAN_POINT ( 'NONE',  ( 0.000000000000000000, 2.680914349914567470E-13, -23.06981291497571362 ) ) ;
#12816=EDGE_CURVE ( 'NONE', #15252, #9066, #3129, .T. ) ;
#12817=CYLINDRICAL_SURFACE ( 'NONE', #11533, 13.19999999999999929 ) ;
#12823=FACE_OUTER_BOUND ( 'NONE', #13448, .T. ) ;
#12824=ORIENTED_EDGE ( 'NONE', *, *, #16644, .T. ) ;
#12829=CARTESIAN_POINT ( 'NONE',  ( 0.1882238946918232125, -2.857713464478510268, -25.78859396478530996 ) ) ;
#12834=ORIENTED_EDGE ( 'NONE', *, *, #17955, .T. ) ;
#12836=DIRECTION ( 'NONE',  ( 1.000000000000000000, 0.000000000000000000, 0.000000000000000000 ) ) ;
#12842=EDGE_CURVE ( 'NONE', #1726, #18935, #12234, .T. ) ;
#12846=CARTESIAN_POINT ( 'NONE',  ( 1.039999999999996261, 24.89775460606850999, -12.96210679857759018 ) ) ;
#12849=ORIENTED_EDGE ( 'NONE', *, *, #1846, .F. ) ;
#12850=CARTESIAN_POINT ( 'NONE',  ( 0.02436607992775978102, 16.37294372382885044, -18.55949924794875017 ) ) ;
#12857=AXIS2_PLACEMENT_3D ( 'NONE', #15516, #9118, #4708 ) ;
#12862=ORIENTED_EDGE ( 'NONE', *, *, #11726, .T. ) ;
#12866=AXIS2_PLACEMENT_3D ( 'NONE', #7853, #9271, #7448 ) ;
#12869=AXIS2_PLACEMENT_3D ( 'NONE', #13071, #11662, #14580 ) ;
#12872=ORIENTED_EDGE ( 'NONE', *, *, #1272, .T. ) ;
#12877=ORIENTED_EDGE ( 'NONE', *, *, #15473, .T. ) ;
#12882=CARTESIAN_POINT ( 'NONE',  ( 2.789999999999999147, -15.04425356660744839, -20.70663861606288236 ) ) ;
#12885=ADVANCED_FACE ( 'NONE', ( #8065 ), #12387, .T. ) ;
#12892=EDGE_CURVE ( 'NONE', #5362, #15740, #16523, .T. ) ;
#12893=CARTESIAN_POINT ( 'NONE',  ( 0.7589665203264086557, -19.86422722021297815, -19.12621924769889148 ) ) ;
#12908=CARTESIAN_POINT ( 'NONE',  ( 2.718184767880469810, -10.24584646439555691, 23.19431517146929878 ) ) ;
#12914=DIRECTION ( 'NONE',  ( -1.000000000000000000, -0.000000000000000000, -0.000000000000000000 ) ) ;
#12917=CARTESIAN_POINT ( 'NONE',  ( 2.789999999999999147, -18.28042085475289369, 15.74360496233375173 ) ) ;
#12924=ORIENTED_EDGE ( 'NONE', *, *, #3409, .F. ) ;
#12929=B_SPLINE_CURVE_WITH_KNOTS ( 'NONE', 3,
 ( #12917, #13019, #4103, #2586 ),
 .UNSPECIFIED., .F., .F.,
 ( 4, 4 ),
 ( 0.005258110598983608240, 0.005948376585272733934 ),
 .UNSPECIFIED. ) ;
#12940=DIRECTION ( 'NONE',  ( -1.000000000000000000, 0.000000000000000000, 0.000000000000000000 ) ) ;
#12943=DIRECTION ( 'NONE',  ( 0.000000000000000000, 0.000000000000000000, 1.000000000000000000 ) ) ;
#12945=AXIS2_PLACEMENT_3D ( 'NONE', #4796, #3397, #200 ) ;
#12947=CARTESIAN_POINT ( 'NONE',  ( 2.783068888626321513, 22.53293026234517171, -9.685942809246819607 ) ) ;
#12948=ORIENTED_EDGE ( 'NONE', *, *, #8652, .T. ) ;
#12953=CARTESIAN_POINT ( 'NONE',  ( 1.039999999999996705, -27.68468304288255410, -4.633866840649218055 ) ) ;
#12958=CARTESIAN_POINT ( 'NONE',  ( -5.209999999999999964, 0.000000000000000000, 0.000000000000000000 ) ) ;
#12961=ORIENTED_EDGE ( 'NONE', *, *, #8157, .T. ) ;
#12972=CARTESIAN_POINT ( 'NONE',  ( 2.789999999999999147, -22.25075486061744812, 9.324097380959361914 ) ) ;
#12977=ORIENTED_EDGE ( 'NONE', *, *, #18387, .T. ) ;
#12980=AXIS2_PLACEMENT_3D ( 'NONE', #8002, #15915, #3607 ) ;
#12983=PRODUCT_DEFINITION ( 'UNKNOWN', '', #7626, #5968 ) ;
#12988=ORIENTED_EDGE ( 'NONE', *, *, #19319, .F. ) ;
#12990=EDGE_CURVE ( 'NONE', #11367, #12173, #16047, .T. ) ;
#12992=AXIS2_PLACEMENT_3D ( 'NONE', #1586, #9099, #14900 ) ;
#12994=CARTESIAN_POINT ( 'NONE',  ( 2.789999999999999147, 24.44424927289184879, 0.2301004812061933913 ) ) ;
#12999=CARTESIAN_POINT ( 'NONE',  ( 2.765633920072238627, -21.30679549418621832, -12.59161484032935618 ) ) ;
#13000=VERTEX_POINT ( 'NONE', #15978 ) ;
#13007=CYLINDRICAL_SURFACE ( 'NONE', #737, 28.06981291497571362 ) ;
#13009=CARTESIAN_POINT ( 'NONE',  ( 2.765633920072235519, -9.836394144775869819, 22.71065055754449347 ) ) ;
#13013=DIRECTION ( 'NONE',  ( 0.000000000000000000, 0.000000000000000000, 1.000000000000000000 ) ) ;
#13014=TOROIDAL_SURFACE ( 'NONE', #10782, 24.12539914357697413, 8.000000000000000000 ) ;
#13016=ORIENTED_EDGE ( 'NONE', *, *, #1052, .T. ) ;
#13019=CARTESIAN_POINT ( 'NONE',  ( 2.790000000000000480, -18.34424029220122776, 15.96500990068118497 ) ) ;
#13022=AXIS2_PLACEMENT_3D ( 'NONE', #6805, #13222, #4110 ) ;
#13024=CARTESIAN_POINT ( 'NONE',  ( 2.030753610301984313, -19.86438386685646762, -19.12676442129367516 ) ) ;
#13025=ORIENTED_EDGE ( 'NONE', *, *, #14735, .T. ) ;
#13031=CARTESIAN_POINT ( 'NONE',  ( 0.5279273746168626769, -4.996265754456183927, -26.57710921259766224 ) ) ;
#13032=DIRECTION ( 'NONE',  ( -1.000000000000000000, 0.000000000000000000, -0.000000000000000000 ) ) ;
#13033=CARTESIAN_POINT ( 'NONE',  ( 0.02436607992775934733, -2.336989772644440855, 24.63872515616082026 ) ) ;
#13039=AXIS2_PLACEMENT_3D ( 'NONE', #14211, #405, #2003 ) ;
#13047=CARTESIAN_POINT ( 'NONE',  ( 2.789999999999999147, 23.48180575137737947, -5.535312321042476391 ) ) ;
#13055=ORIENTED_EDGE ( 'NONE', *, *, #15258, .F. ) ;
#13056=CARTESIAN_POINT ( 'NONE',  ( 0.7188676524878460095, -24.19190980169966210, 12.96989951879399428 ) ) ;
#13061=CARTESIAN_POINT ( 'NONE',  ( 2.765633920072234631, 16.37294372382885044, -18.55949924794875017 ) ) ;
#13071=CARTESIAN_POINT ( 'NONE',  ( 2.789999999999999147, 14.18181402625742749, 19.91106274590519121 ) ) ;
#13075=CIRCLE ( 'NONE', #18494, 24.12539914357697768 ) ;
#13077=CARTESIAN_POINT ( 'NONE',  ( 2.262072706628476926, -18.56460150496924655, -19.66369668717053898 ) ) ;
#13084=CARTESIAN_POINT ( 'NONE',  ( 2.765633920072241736, -9.836394144775550075, -22.71065055754462492 ) ) ;
#13092=CARTESIAN_POINT ( 'NONE',  ( 2.788130827028544534, 20.90869469097885158, -12.51925356660739297 ) ) ;
#13093=ORIENTED_EDGE ( 'NONE', *, *, #2521, .F. ) ;
#13098=EDGE_CURVE ( 'NONE', #569, #3340, #10175, .T. ) ;
#13099=CARTESIAN_POINT ( 'NONE',  ( 2.783025228907522131, -9.686319561461109728, 22.53337530003400246 ) ) ;
#13107=AXIS2_PLACEMENT_3D ( 'NONE', #8611, #14628, #2312 ) ;
#13112=ORIENTED_EDGE ( 'NONE', *, *, #3006, .T. ) ;
#13113=CARTESIAN_POINT ( 'NONE',  ( 2.789999999999999147, -24.34211360614294506, -7.909232158575071558 ) ) ;
#13117=CARTESIAN_POINT ( 'NONE',  ( 2.789999999999999147, 2.680914349914567470E-13, -23.06981291497571362 ) ) ;
#13119=CARTESIAN_POINT ( 'NONE',  ( 2.783068945535915883, -2.248820353272798389, -24.42321038836784908 ) ) ;
#13132=EDGE_CURVE ( 'NONE', #9713, #303, #8261, .T. ) ;
#13133=DIRECTION ( 'NONE',  ( 0.000000000000000000, 0.000000000000000000, 1.000000000000000000 ) ) ;
#13142=CARTESIAN_POINT ( 'NONE',  ( 0.5279272933715190019, 18.56460150496967287, -19.66369668717012331 ) ) ;
#13170=AXIS2_PLACEMENT_3D ( 'NONE', #10002, #19381, #3787 ) ;
#13176=ORIENTED_EDGE ( 'NONE', *, *, #5252, .F. ) ;
#13178=CARTESIAN_POINT ( 'NONE',  ( 0.02436607992775978102, -12.59161484032896361, -21.30679549418645280 ) ) ;
#13180=VERTEX_POINT ( 'NONE', #19360 ) ;
#13183=ORIENTED_EDGE ( 'NONE', *, *, #17932, .T. ) ;
#13188=DIRECTION ( 'NONE',  ( 1.000000000000000000, -0.000000000000000000, 0.000000000000000000 ) ) ;
#13191=AXIS2_PLACEMENT_3D ( 'NONE', #15179, #10289, #19574 ) ;
#13192=LINE ( 'NONE', #10193, #866 ) ;
#13193=CARTESIAN_POINT ( 'NONE',  ( 2.789999999999999147, -22.71065055754445439, -9.836394144775947979 ) ) ;
#13195=CARTESIAN_POINT ( 'NONE',  ( 1.039999999999997593, -24.89775460606841051, 12.96210679857778025 ) ) ;
#13199=CYLINDRICAL_SURFACE ( 'NONE', #14135, 2.524999999999995914 ) ;
#13201=EDGE_CURVE ( 'NONE', #5854, #9684, #9138, .T. ) ;
#13204=EDGE_CURVE ( 'NONE', #12478, #17826, #7662, .T. ) ;
#13205=EDGE_CURVE ( 'NONE', #1162, #11385, #6147, .T. ) ;
#13207=VECTOR ( 'NONE', #15157, 1000.000000000000000 ) ;
#13213=VECTOR ( 'NONE', #95, 1000.000000000000000 ) ;
#13214=CARTESIAN_POINT ( 'NONE',  ( 2.789999999999999147, -8.936381166381891568E-14, 25.59481291497571220 ) ) ;
#13216=ORIENTED_EDGE ( 'NONE', *, *, #13403, .F. ) ;
#13217=CARTESIAN_POINT ( 'NONE',  ( 0.000000000000000000, -24.04302995059967429, 1.991882183130232242 ) ) ;
#13219=CARTESIAN_POINT ( 'NONE',  ( 0.02436607992776108206, -24.15498966839966855, 5.391175441198523544 ) ) ;
#13221=ORIENTED_EDGE ( 'NONE', *, *, #17895, .T. ) ;
#13222=DIRECTION ( 'NONE',  ( -1.000000000000000000, -0.000000000000000000, -0.000000000000000000 ) ) ;
#13229=ORIENTED_EDGE ( 'NONE', *, *, #5059, .F. ) ;
#13237=CARTESIAN_POINT ( 'NONE',  ( 0.1882238782932344479, 19.18368891937516452, -17.47009390565470000 ) ) ;
#13244=ORIENTED_EDGE ( 'NONE', *, *, #7127, .T. ) ;
#13245=CARTESIAN_POINT ( 'NONE',  ( 2.789999999999999147, 5.391175441198615914, 24.15498966839965078 ) ) ;
#13247=CARTESIAN_POINT ( 'NONE',  ( 0.000000000000000000, -1.991882183130475603, 24.04302995059966719 ) ) ;
#13250=FACE_OUTER_BOUND ( 'NONE', #7865, .T. ) ;
#13251=VERTEX_POINT ( 'NONE', #4557 ) ;
#13264=EDGE_LOOP ( 'NONE', ( #15130, #10695, #12156, #16420 ) ) ;
#13268=ORIENTED_EDGE ( 'NONE', *, *, #17983, .T. ) ;
#13271=DIRECTION ( 'NONE',  ( 1.000000000000000000, -0.000000000000000000, -0.000000000000000000 ) ) ;
#13278=VERTEX_POINT ( 'NONE', #12368 ) ;
#13288=CYLINDRICAL_SURFACE ( 'NONE', #5534, 28.06981291497571362 ) ;
#13290=DIRECTION ( 'NONE',  ( -1.000000000000000000, 0.000000000000000000, -0.000000000000000000 ) ) ;
#13296=ORIENTED_EDGE ( 'NONE', *, *, #17579, .F. ) ;
#13299=CARTESIAN_POINT ( 'NONE',  ( 0.000000000000000000, 12.52067188844379864, -20.62201879784900882 ) ) ;
#13301=CARTESIAN_POINT ( 'NONE',  ( -10.00000000000000000, 0.000000000000000000, 0.000000000000000000 ) ) ;
#13309=VECTOR ( 'NONE', #18793, 1000.000000000000000 ) ;
#13316=EDGE_CURVE ( 'NONE', #14880, #619, #4594, .T. ) ;
#13317=ORIENTED_EDGE ( 'NONE', *, *, #3087, .F. ) ;
#13325=DIRECTION ( 'NONE',  ( 0.000000000000000000, 0.000000000000000000, 1.000000000000000000 ) ) ;
#13330=VERTEX_POINT ( 'NONE', #349 ) ;
#13331=ADVANCED_FACE ( 'NONE', ( #6433 ), #4443, .T. ) ;
#13340=EDGE_CURVE ( 'NONE', #5005, #1162, #15345, .T. ) ;
#13349=ADVANCED_FACE ( 'NONE', ( #1559 ), #5701, .T. ) ;
#13350=CARTESIAN_POINT ( 'NONE',  ( 8.000000000000000000, 0.000000000000000000, 0.000000000000000000 ) ) ;
#13352=AXIS2_PLACEMENT_3D ( 'NONE', #18536, #18833, #17336 ) ;
#13353=FACE_OUTER_BOUND ( 'NONE', #18606, .T. ) ;
#13369=CARTESIAN_POINT ( 'NONE',  ( 2.789999999999999147, -20.70663861606260170, -15.04425356660783031 ) ) ;
#13370=ORIENTED_EDGE ( 'NONE', *, *, #14224, .F. ) ;
#13371=CARTESIAN_POINT ( 'NONE',  ( 2.789999999999999147, 23.48180575137730131, 5.535312321042802353 ) ) ;
#13372=EDGE_CURVE ( 'NONE', #15740, #6118, #16761, .T. ) ;
#13373=FACE_OUTER_BOUND ( 'NONE', #7169, .T. ) ;
#13375=DIRECTION ( 'NONE',  ( 0.000000000000000000, 0.000000000000000000, 1.000000000000000000 ) ) ;
#13379=DIRECTION ( 'NONE',  ( -1.000000000000000000, -0.000000000000000000, -0.000000000000000000 ) ) ;
#13381=DIRECTION ( 'NONE',  ( -1.000000000000000000, -0.000000000000000000, -0.000000000000000000 ) ) ;
#13386=DIRECTION ( 'NONE',  ( 0.000000000000000000, 0.000000000000000000, 1.000000000000000000 ) ) ;
#13387=B_SPLINE_CURVE_WITH_KNOTS ( 'NONE', 3,
 ( #12212, #16720, #2999, #14405, #3692, #17110 ),
 .UNSPECIFIED., .F., .F.,
 ( 4, 2, 4 ),
 ( 2.586195665699493951E-07, 0.001878649493629688805, 0.003757040367692807744 ),
 .UNSPECIFIED. ) ;
#13391=CARTESIAN_POINT ( 'NONE',  ( 1.039999999999996705, -27.68468304288255410, -4.633866840649218055 ) ) ;
#13393=ORIENTED_EDGE ( 'NONE', *, *, #11170, .T. ) ;
#13395=EDGE_CURVE ( 'NONE', #18268, #17360, #17959, .T. ) ;
#13403=EDGE_CURVE ( 'NONE', #196, #14221, #15949, .T. ) ;
#13404=VERTEX_POINT ( 'NONE', #15962 ) ;
#13405=CARTESIAN_POINT ( 'NONE',  ( 2.789999999999999147, 24.04302995059966364, -1.991882183130384121 ) ) ;
#13407=CARTESIAN_POINT ( 'NONE',  ( 2.789999999999999147, -20.62201879784904079, -12.52067188844374179 ) ) ;
#13410=AXIS2_PLACEMENT_3D ( 'NONE', #12341, #12537, #16945 ) ;
#13422=B_SPLINE_CURVE_WITH_KNOTS ( 'NONE', 3,
 ( #11025, #3513, #9630, #15627, #15723, #3321 ),
 .UNSPECIFIED., .F., .F.,
 ( 4, 2, 4 ),
 ( 4.462636732861209103E-07, 0.001879885066975070214, 0.003759323870276854232 ),
 .UNSPECIFIED. ) ;
#13426=ADVANCED_FACE ( 'NONE', ( #6634 ), #2249, .T. ) ;
#13429=VERTEX_POINT ( 'NONE', #9667 ) ;
#13430=CARTESIAN_POINT ( 'NONE',  ( 2.030753610301991419, 19.86438386685660618, 19.12676442129351173 ) ) ;
#13432=DIRECTION ( 'NONE',  ( 0.000000000000000000, 0.000000000000000000, 1.000000000000000000 ) ) ;
#13433=CARTESIAN_POINT ( 'NONE',  ( 2.765633920072242624, 9.836394144775706394, 22.71065055754456097 ) ) ;
#13434=DIRECTION ( 'NONE',  ( 0.000000000000000000, 0.000000000000000000, 1.000000000000000000 ) ) ;
#13441=EDGE_CURVE ( 'NONE', #18420, #15528, #1562, .T. ) ;
#13445=FACE_BOUND ( 'NONE', #5017, .T. ) ;
#13447=CARTESIAN_POINT ( 'NONE',  ( 2.718131853594931258, -21.92302674874953539, -12.74240566899008442 ) ) ;
#13448=EDGE_LOOP ( 'NONE', ( #6491, #19058, #19049, #2694 ) ) ;
#13455=ORIENTED_EDGE ( 'NONE', *, *, #11626, .T. ) ;
#13456=ORIENTED_EDGE ( 'NONE', *, *, #7489, .F. ) ;
#13457=DIRECTION ( 'NONE',  ( 1.000000000000000000, -0.000000000000000000, -0.000000000000000000 ) ) ;
#13461=ORIENTED_EDGE ( 'NONE', *, *, #607, .F. ) ;
#13467=ORIENTED_EDGE ( 'NONE', *, *, #13201, .T. ) ;
#13469=AXIS2_PLACEMENT_3D ( 'NONE', #2124, #13032, #11620 ) ;
#13471=DIRECTION ( 'NONE',  ( -1.000000000000000000, -0.000000000000000000, -0.000000000000000000 ) ) ;
#13475=ORIENTED_EDGE ( 'NONE', *, *, #3139, .F. ) ;
#13482=AXIS2_PLACEMENT_3D ( 'NONE', #15474, #9174, #5956 ) ;
#13486=DIRECTION ( 'NONE',  ( -1.000000000000000000, 0.000000000000000000, 0.000000000000000000 ) ) ;
#13488=ORIENTED_EDGE ( 'NONE', *, *, #8486, .F. ) ;
#13489=CARTESIAN_POINT ( 'NONE',  ( 0.02436607992775544421, -22.71065055754445439, -9.836394144775947979 ) ) ;
#13494=EDGE_CURVE ( 'NONE', #540, #18318, #19761, .T. ) ;
#13498=AXIS2_PLACEMENT_3D ( 'NONE', #2030, #3135, #11039 ) ;
#13499=CARTESIAN_POINT ( 'NONE',  ( 2.262072661820534236, -26.82026385750180353, 3.461047254864169975 ) ) ;
#13500=DIRECTION ( 'NONE',  ( 0.000000000000000000, 0.000000000000000000, 1.000000000000000000 ) ) ;
#13501=ORIENTED_EDGE ( 'NONE', *, *, #6423, .T. ) ;
#13509=EDGE_LOOP ( 'NONE', ( #15334, #17926, #13758, #5106 ) ) ;
#13512=EDGE_CURVE ( 'NONE', #11113, #298, #16549, .T. ) ;
#13513=CARTESIAN_POINT ( 'NONE',  ( 2.718131847775118182, 24.78765742476139522, 5.344160105508784397 ) ) ;
#13518=CARTESIAN_POINT ( 'NONE',  ( 0.07186813532171011654, 25.22589920183360945, 2.577209017047096484 ) ) ;
#13520=ORIENTED_EDGE ( 'NONE', *, *, #1740, .T. ) ;
#13521=CIRCLE ( 'NONE', #2977, 24.12539914357697413 ) ;
#13531=CYLINDRICAL_SURFACE ( 'NONE', #7980, 2.524999999999995914 ) ;
#13535=CARTESIAN_POINT ( 'NONE',  ( 1.039999999999995373, 25.12109765559670649, -12.52377138324197681 ) ) ;
#13550=FACE_OUTER_BOUND ( 'NONE', #15635, .T. ) ;
#13551=ORIENTED_EDGE ( 'NONE', *, *, #4165, .F. ) ;
#13558=ORIENTED_EDGE ( 'NONE', *, *, #16355, .T. ) ;
#13567=TOROIDAL_SURFACE ( 'NONE', #6841, 24.12539914357697413, 8.000000000000000000 ) ;
#13576=CARTESIAN_POINT ( 'NONE',  ( 2.789999999999999147, 9.324097380959765147, -22.25075486061728824 ) ) ;
#13579=ORIENTED_EDGE ( 'NONE', *, *, #1520, .F. ) ;
#13580=CARTESIAN_POINT ( 'NONE',  ( 2.789999999999999147, -9.324097380959294412, -22.25075486061747654 ) ) ;
#13582=VERTEX_POINT ( 'NONE', #11645 ) ;
#13585=CIRCLE ( 'NONE', #4962, 24.12539914357697413 ) ;
#13598=DIRECTION ( 'NONE',  ( -1.000000000000000000, -0.000000000000000000, -0.000000000000000000 ) ) ;
#13600=VECTOR ( 'NONE', #8378, 1000.000000000000000 ) ;
#13604=B_SPLINE_CURVE_WITH_KNOTS ( 'NONE', 3,
 ( #921, #7000, #19615, #4212 ),
 .UNSPECIFIED., .F., .F.,
 ( 4, 4 ),
 ( 1.981826382900849143E-07, 0.0006887856082032012620 ),
 .UNSPECIFIED. ) ;
#13607=DIRECTION ( 'NONE',  ( 0.000000000000000000, 0.000000000000000000, 1.000000000000000000 ) ) ;
#13608=CARTESIAN_POINT ( 'NONE',  ( 0.02436607992775934733, -21.30679549418640306, 12.59161484032904887 ) ) ;
#13616=VECTOR ( 'NONE', #2403, 1000.000000000000000 ) ;
#13631=CIRCLE ( 'NONE', #11392, 2.524999999999995914 ) ;
#13633=DIRECTION ( 'NONE',  ( 0.000000000000000000, 0.000000000000000000, 1.000000000000000000 ) ) ;
#13641=B_SPLINE_CURVE_WITH_KNOTS ( 'NONE', 3,
 ( #7045, #11384, #6856, #13178 ),
 .UNSPECIFIED., .F., .F.,
 ( 4, 4 ),
 ( 0.005258139959819249469, 0.005948405594583416715 ),
 .UNSPECIFIED. ) ;
#13642=CARTESIAN_POINT ( 'NONE',  ( 1.749999999999998002, 4.147968289691672084, -27.76164181293047406 ) ) ;
#13649=EDGE_CURVE ( 'NONE', #479, #2446, #13075, .T. ) ;
#13650=CARTESIAN_POINT ( 'NONE',  ( 0.000000000000000000, 0.000000000000000000, 0.000000000000000000 ) ) ;
#13651=CARTESIAN_POINT ( 'NONE',  ( 0.02436607992775978102, 16.37294372382885044, -18.55949924794875017 ) ) ;
#13652=ORIENTED_EDGE ( 'NONE', *, *, #858, .F. ) ;
#13653=LINE ( 'NONE', #7225, #8965 ) ;
#13655=CARTESIAN_POINT ( 'NONE',  ( 2.604434283110813819, -22.53097606932974983, -12.84444904262050002 ) ) ;
#13657=CARTESIAN_POINT ( 'NONE',  ( -7.688810570594222860E-14, -5.456611084822025504, 23.69897269326675016 ) ) ;
#13658=AXIS2_PLACEMENT_3D ( 'NONE', #14818, #10515, #12211 ) ;
#13659=VERTEX_POINT ( 'NONE', #9039 ) ;
#13661=CARTESIAN_POINT ( 'NONE',  ( 2.601776091974071115, -5.251266773802197640, -25.40949241676359094 ) ) ;
#13663=AXIS2_PLACEMENT_3D ( 'NONE', #11060, #17168, #2251 ) ;
#13667=CARTESIAN_POINT ( 'NONE',  ( 0.02436607992776064838, 12.59161484032912171, 21.30679549418635688 ) ) ;
#13681=CARTESIAN_POINT ( 'NONE',  ( 0.006974771092476448643, 22.53337530003417655, -9.686319561460717154 ) ) ;
#13683=CARTESIAN_POINT ( 'NONE',  ( 2.789999999999999147, 15.74360496233381390, 18.28042085475283685 ) ) ;
#13684=EDGE_CURVE ( 'NONE', #2446, #2766, #15305, .T. ) ;
#13689=CARTESIAN_POINT ( 'NONE',  ( 2.789999999999999147, -23.48180575137734039, 5.535312321042630934 ) ) ;
#13692=EDGE_LOOP ( 'NONE', ( #6497, #5037, #3373, #8787, #18256, #18843, #9937 ) ) ;
#13694=CARTESIAN_POINT ( 'NONE',  ( 2.789999999999999591, -24.22479935914660487, 2.133490293296927742 ) ) ;
#13700=CARTESIAN_POINT ( 'NONE',  ( 2.765633920072233742, -24.15498966839966855, 5.391175441198523544 ) ) ;
#13703=DIRECTION ( 'NONE',  ( 0.000000000000000000, 0.000000000000000000, 1.000000000000000000 ) ) ;
#13711=FACE_OUTER_BOUND ( 'NONE', #17526, .T. ) ;
#13715=CARTESIAN_POINT ( 'NONE',  ( 2.789999999999999147, 20.70663861606272249, 15.04425356660767932 ) ) ;
#13725=EDGE_LOOP ( 'NONE', ( #9886, #7027, #10834, #17567 ) ) ;
#13727=DIRECTION ( 'NONE',  ( 0.000000000000000000, 0.000000000000000000, 1.000000000000000000 ) ) ;
#13733=CARTESIAN_POINT ( 'NONE',  ( 0.02436607992776628623, 24.63872515616082737, -2.336989772644355590 ) ) ;
#13736=LINE ( 'NONE', #3126, #17886 ) ;
#13739=DIRECTION ( 'NONE',  ( -1.000000000000000000, -0.000000000000000000, -0.000000000000000000 ) ) ;
#13742=ORIENTED_EDGE ( 'NONE', *, *, #8652, .F. ) ;
#13744=B_SPLINE_CURVE_WITH_KNOTS ( 'NONE', 3,
 ( #17493, #8580, #5375, #5178 ),
 .UNSPECIFIED., .F., .F.,
 ( 4, 4 ),
 ( 0.005342776758202955750, 0.005948405594583417583 ),
 .UNSPECIFIED. ) ;
#13747=ORIENTED_EDGE ( 'NONE', *, *, #3087, .T. ) ;
#13754=CARTESIAN_POINT ( 'NONE',  ( 1.749999999999998002, 12.52377138324259143, -25.12109765559640451 ) ) ;
#13755=CARTESIAN_POINT ( 'NONE',  ( 2.765633920072235963, 24.63872515616082737, 2.336989772644355146 ) ) ;
#13758=ORIENTED_EDGE ( 'NONE', *, *, #3631, .T. ) ;
#13760=CARTESIAN_POINT ( 'NONE',  ( 1.749999999999998002, 24.89775460606851354, -12.96210679857759729 ) ) ;
#13761=ORIENTED_EDGE ( 'NONE', *, *, #4345, .T. ) ;
#13775=CARTESIAN_POINT ( 'NONE',  ( 0.000000000000000000, 18.28042085475300382, -15.74360496233363804 ) ) ;
#13777=ORIENTED_EDGE ( 'NONE', *, *, #7489, .T. ) ;
#13784=DIRECTION ( 'NONE',  ( 0.000000000000000000, 0.000000000000000000, 1.000000000000000000 ) ) ;
#13796=CARTESIAN_POINT ( 'NONE',  ( 0.000000000000000000, 0.000000000000000000, 0.000000000000000000 ) ) ;
#13802=LINE ( 'NONE', #11908, #7144 ) ;
#13803=AXIS2_PLACEMENT_3D ( 'NONE', #13715, #15322, #18413 ) ;
#13806=DIRECTION ( 'NONE',  ( -1.000000000000000000, -0.000000000000000000, -0.000000000000000000 ) ) ;
#13809=AXIS2_PLACEMENT_3D ( 'NONE', #13980, #17082, #1965 ) ;
#13813=CARTESIAN_POINT ( 'NONE',  ( 0.000000000000000000, 0.000000000000000000, 0.000000000000000000 ) ) ;
#13817=DIRECTION ( 'NONE',  ( 0.000000000000000000, 0.000000000000000000, 1.000000000000000000 ) ) ;
#13821=EDGE_CURVE ( 'NONE', #5932, #18318, #13972, .T. ) ;
#13830=CARTESIAN_POINT ( 'NONE',  ( 0.02436607992775761261, 22.71065055754452544, 9.836394144775786330 ) ) ;
#13836=ORIENTED_EDGE ( 'NONE', *, *, #4028, .T. ) ;
#13843=ORIENTED_EDGE ( 'NONE', *, *, #7299, .T. ) ;
#13850=CARTESIAN_POINT ( 'NONE',  ( 0.02436607992776455150, -22.71065055754459650, 9.836394144775621129 ) ) ;
#13863=ORIENTED_EDGE ( 'NONE', *, *, #11884, .F. ) ;
#13865=DIRECTION ( 'NONE',  ( 0.000000000000000000, 0.000000000000000000, 1.000000000000000000 ) ) ;
#13868=EDGE_CURVE ( 'NONE', #18023, #5005, #8162, .T. ) ;
#13870=ORIENTED_EDGE ( 'NONE', *, *, #5358, .T. ) ;
#13871=B_SPLINE_CURVE_WITH_KNOTS ( 'NONE', 3,
 ( #2812, #19627, #16836, #10434, #5912, #16733 ),
 .UNSPECIFIED., .F., .F.,
 ( 4, 2, 4 ),
 ( 2.132675795048140432E-07, 0.001878604073277005205, 0.003756994878974505639 ),
 .UNSPECIFIED. ) ;
#13873=CARTESIAN_POINT ( 'NONE',  ( 2.789999999999999147, -18.28042085475266276, -15.74360496233401996 ) ) ;
#13879=ORIENTED_EDGE ( 'NONE', *, *, #5980, .F. ) ;
#13881=CARTESIAN_POINT ( 'NONE',  ( 0.000000000000000000, 22.25075486061751207, -9.324097380959241121 ) ) ;
#13882=( LENGTH_UNIT ( ) NAMED_UNIT ( * ) SI_UNIT ( .MILLI., .METRE. ) );
#13883=CIRCLE ( 'NONE', #14538, 24.12539914357697413 ) ;
#13895=VERTEX_POINT ( 'NONE', #4864 ) ;
#13896=B_SPLINE_CURVE_WITH_KNOTS ( 'NONE', 3,
 ( #12724, #10925, #15432, #18717 ),
 .UNSPECIFIED., .F., .F.,
 ( 4, 4 ),
 ( 3.059063720795842371E-07, 0.0006888942284914355242 ),
 .UNSPECIFIED. ) ;
#13899=CARTESIAN_POINT ( 'NONE',  ( 2.765633920072236407, -2.336989772644440855, 24.63872515616082026 ) ) ;
#13901=CARTESIAN_POINT ( 'NONE',  ( 0.07181525068722517668, 2.576941577947404305, 25.22524549359951251 ) ) ;
#13908=CARTESIAN_POINT ( 'NONE',  ( 1.039999999999996705, -19.67366047555515252, -20.02152543075367319 ) ) ;
#13909=DIRECTION ( 'NONE',  ( 1.000000000000000000, 0.000000000000000000, 0.000000000000000000 ) ) ;
#13914=CARTESIAN_POINT ( 'NONE',  ( 1.039999999999999147, 12.52377138324259676, -25.12109765559640095 ) ) ;
#13917=ORIENTED_EDGE ( 'NONE', *, *, #4420, .F. ) ;
#13922=CIRCLE ( 'NONE', #10739, 4.000000000000000000 ) ;
#13925=CARTESIAN_POINT ( 'NONE',  ( 1.749999999999998002, 24.89775460606832524, 12.96210679857795256 ) ) ;
#13926=ORIENTED_EDGE ( 'NONE', *, *, #5127, .F. ) ;
#13930=DIRECTION ( 'NONE',  ( 0.000000000000000000, 1.374038396813314756E-15, -1.000000000000000000 ) ) ;
#13934=ORIENTED_EDGE ( 'NONE', *, *, #15171, .T. ) ;
#13939=DIRECTION ( 'NONE',  ( -1.000000000000000000, -0.000000000000000000, -0.000000000000000000 ) ) ;
#13941=ORIENTED_EDGE ( 'NONE', *, *, #4170, .T. ) ;
#13949=DIRECTION ( 'NONE',  ( 0.000000000000000000, 0.000000000000000000, -1.000000000000000000 ) ) ;
#13951=CARTESIAN_POINT ( 'NONE',  ( 2.601776144743014108, 10.68696068830440815, -23.64332819722370260 ) ) ;
#13953=ORIENTED_EDGE ( 'NONE', *, *, #6711, .F. ) ;
#13960=ORIENTED_EDGE ( 'NONE', *, *, #2245, .T. ) ;
#13962=EDGE_CURVE ( 'NONE', #1328, #283, #12677, .T. ) ;
#13965=VECTOR ( 'NONE', #12637, 1000.000000000000000 ) ;
#13971=ADVANCED_FACE ( 'NONE', ( #6845 ), #16359, .T. ) ;
#13972=LINE ( 'NONE', #6742, #626 ) ;
#13973=AXIS2_PLACEMENT_3D ( 'NONE', #6242, #7650, #2954 ) ;
#13980=CARTESIAN_POINT ( 'NONE',  ( 2.789999999999999147, -24.44424927289185590, -0.2301004812060095106 ) ) ;
#13983=CARTESIAN_POINT ( 'NONE',  ( 2.031033465052724196, 4.828387785248403397, -27.14933624560903525 ) ) ;
#13991=ADVANCED_FACE ( 'NONE', ( #17470 ), #16074, .F. ) ;
#13992=CARTESIAN_POINT ( 'NONE',  ( 2.031033465052725084, -27.14933624560904946, -4.828387785248313691 ) ) ;
#13996=CARTESIAN_POINT ( 'NONE',  ( -7.728448779411724935E-14, -2.133839912090635949, -24.22524813288764989 ) ) ;
#14000=CARTESIAN_POINT ( 'NONE',  ( 0.000000000000000000, -23.48180575137727288, -5.535312321042949790 ) ) ;
#14001=ORIENTED_EDGE ( 'NONE', *, *, #7731, .T. ) ;
#14002=CIRCLE ( 'NONE', #583, 28.06981291497571007 ) ;
#14004=DIRECTION ( 'NONE',  ( -1.000000000000000000, -0.000000000000000000, -0.000000000000000000 ) ) ;
#14008=CARTESIAN_POINT ( 'NONE',  ( 2.783025342027735327, -5.408388659523925668, -23.92335783895643075 ) ) ;
#14011=ORIENTED_EDGE ( 'NONE', *, *, #18969, .T. ) ;
#14020=EDGE_CURVE ( 'NONE', #2162, #3518, #17, .T. ) ;
#14024=DIRECTION ( 'NONE',  ( 0.000000000000000000, 0.000000000000000000, 1.000000000000000000 ) ) ;
#14027=DIRECTION ( 'NONE',  ( 0.000000000000000000, -0.8090169943749488946, 0.5877852522924711387 ) ) ;
#14033=CARTESIAN_POINT ( 'NONE',  ( 2.789999999999999147, 15.04425356660790136, -18.18163861606255338 ) ) ;
#14040=ORIENTED_EDGE ( 'NONE', *, *, #4328, .T. ) ;
#14044=ORIENTED_EDGE ( 'NONE', *, *, #16013, .T. ) ;
#14049=EDGE_LOOP ( 'NONE', ( #3125, #2514, #18141, #8193, #18439, #919 ) ) ;
#14051=CARTESIAN_POINT ( 'NONE',  ( 2.031033467310408014, 12.98167595241057626, -24.32849926382737138 ) ) ;
#14053=ORIENTED_EDGE ( 'NONE', *, *, #13098, .T. ) ;
#14064=DIRECTION ( 'NONE',  ( -1.000000000000000000, 0.000000000000000000, -0.000000000000000000 ) ) ;
#14072=FACE_OUTER_BOUND ( 'NONE', #15827, .T. ) ;
#14085=EDGE_CURVE ( 'NONE', #15252, #13330, #16274, .T. ) ;
#14089=CARTESIAN_POINT ( 'NONE',  ( 1.039999999999996483, 4.147968289691283950, 27.76164181293052735 ) ) ;
#14105=ORIENTED_EDGE ( 'NONE', *, *, #14369, .T. ) ;
#14112=ORIENTED_EDGE ( 'NONE', *, *, #9080, .T. ) ;
#14113=AXIS2_PLACEMENT_3D ( 'NONE', #13214, #2204, #11703 ) ;
#14115=CIRCLE ( 'NONE', #3248, 24.12539914357697768 ) ;
#14120=DIRECTION ( 'NONE',  ( 0.000000000000000000, 0.000000000000000000, 1.000000000000000000 ) ) ;
#14122=EDGE_CURVE ( 'NONE', #10318, #8201, #581, .T. ) ;
#14126=B_SPLINE_CURVE_WITH_KNOTS ( 'NONE', 3,
 ( #19130, #5515, #18837, #9947 ),
 .UNSPECIFIED., .F., .F.,
 ( 4, 4 ),
 ( 0.005258120783916789796, 0.005948386350302922905 ),
 .UNSPECIFIED. ) ;
#14130=LINE ( 'NONE', #15734, #3734 ) ;
#14133=DIRECTION ( 'NONE',  ( 0.000000000000000000, 0.000000000000000000, 1.000000000000000000 ) ) ;
#14135=AXIS2_PLACEMENT_3D ( 'NONE', #2675, #13290, #1090 ) ;
#14138=B_SPLINE_CURVE_WITH_KNOTS ( 'NONE', 3,
 ( #10722, #13518, #4506, #16833, #19623, #2903 ),
 .UNSPECIFIED., .F., .F.,
 ( 4, 2, 4 ),
 ( 2.132675795046084789E-07, 0.001878604073277003903, 0.003756994878974503470 ),
 .UNSPECIFIED. ) ;
#14144=ORIENTED_EDGE ( 'NONE', *, *, #9426, .F. ) ;
#14158=CARTESIAN_POINT ( 'NONE',  ( 0.02436607992776064838, 5.391175441198615914, 24.15498966839965078 ) ) ;
#14160=EDGE_CURVE ( 'NONE', #11385, #18023, #12274, .T. ) ;
#14164=ORIENTED_EDGE ( 'NONE', *, *, #5365, .T. ) ;
#14165=AXIS2_PLACEMENT_3D ( 'NONE', #18329, #7300, #9127 ) ;
#14166=CIRCLE ( 'NONE', #4569, 2.524999999999995470 ) ;
#14168=CARTESIAN_POINT ( 'NONE',  ( 8.000000000000000000, 0.000000000000000000, 0.000000000000000000 ) ) ;
#14170=CARTESIAN_POINT ( 'NONE',  ( 0.02436607992776758727, 24.15498966839963302, 5.391175441198700291 ) ) ;
#14174=CARTESIAN_POINT ( 'NONE',  ( 2.789999999999999147, 24.44424927289185945, -0.2301004812058395077 ) ) ;
#14175=ORIENTED_EDGE ( 'NONE', *, *, #12709, .F. ) ;
#14180=B_SPLINE_CURVE_WITH_KNOTS ( 'NONE', 3,
 ( #14372, #4766, #3559, #6545, #8265, #14272 ),
 .UNSPECIFIED., .F., .F.,
 ( 4, 2, 4 ),
 ( 4.462636808903086370E-07, 0.001879885123572231417, 0.003759323983463572477 ),
 .UNSPECIFIED. ) ;
#14181=CARTESIAN_POINT ( 'NONE',  ( 2.789999999999999147, 2.680914349914567470E-13, -25.59481291497571220 ) ) ;
#14183=VERTEX_POINT ( 'NONE', #4742 ) ;
#14187=VERTEX_POINT ( 'NONE', #447 ) ;
#14188=DIRECTION ( 'NONE',  ( 1.000000000000000000, -0.000000000000000000, -0.000000000000000000 ) ) ;
#14190=AXIS2_PLACEMENT_3D ( 'NONE', #12994, #10187, #9998 ) ;
#14191=FACE_OUTER_BOUND ( 'NONE', #17155, .T. ) ;
#14197=CARTESIAN_POINT ( 'NONE',  ( 0.07181524296601451973, 16.91181672897733534, 18.89296398180198011 ) ) ;
#14203=CARTESIAN_POINT ( 'NONE',  ( 2.790000000000077307, -5.456611084821691549, -23.69897269326682832 ) ) ;
#14211=CARTESIAN_POINT ( 'NONE',  ( 2.789999999999999147, -7.909232158574647009, -24.34211360614308006 ) ) ;
#14212=ORIENTED_EDGE ( 'NONE', *, *, #13441, .T. ) ;
#14219=CARTESIAN_POINT ( 'NONE',  ( 2.718131885465892683, -18.89333555428565603, 16.91241718341992240 ) ) ;
#14221=VERTEX_POINT ( 'NONE', #16153 ) ;
#14224=EDGE_CURVE ( 'NONE', #4306, #12283, #5552, .T. ) ;
#14228=ORIENTED_EDGE ( 'NONE', *, *, #7818, .F. ) ;
#14229=CARTESIAN_POINT ( 'NONE',  ( 2.604434514863827488, -23.63475234378990208, 10.67816411292155543 ) ) ;
#14233=DIRECTION ( 'NONE',  ( 0.000000000000000000, 0.000000000000000000, 1.000000000000000000 ) ) ;
#14234=AXIS2_PLACEMENT_3D ( 'NONE', #17880, #11875, #17987 ) ;
#14236=CARTESIAN_POINT ( 'NONE',  ( 2.789999999999999147, 1.991882183130294637, 24.04302995059966364 ) ) ;
#14240=LINE ( 'NONE', #739, #19671 ) ;
#14243=B_SPLINE_CURVE_WITH_KNOTS ( 'NONE', 3,
 ( #12305, #18402, #3189, #15403 ),
 .UNSPECIFIED., .F., .F.,
 ( 4, 4 ),
 ( 0.005258214619651960589, 0.005948481662034167325 ),
 .UNSPECIFIED. ) ;
#14254=CARTESIAN_POINT ( 'NONE',  ( 2.789999999999999147, -20.70663861606282197, 15.04425356660753188 ) ) ;
#14258=LINE ( 'NONE', #9769, #19463 ) ;
#14259=ORIENTED_EDGE ( 'NONE', *, *, #503, .T. ) ;
#14264=CIRCLE ( 'NONE', #9149, 24.12539914357697768 ) ;
#14270=EDGE_CURVE ( 'NONE', #13330, #5965, #836, .T. ) ;
#14272=CARTESIAN_POINT ( 'NONE',  ( 2.765633920072235963, -16.37294372382871188, 18.55949924794887096 ) ) ;
#14273=AXIS2_PLACEMENT_3D ( 'NONE', #6868, #3985, #17400 ) ;
#14282=DIRECTION ( 'NONE',  ( 1.000000000000000000, -0.000000000000000000, -0.000000000000000000 ) ) ;
#14287=AXIS2_PLACEMENT_3D ( 'NONE', #14842, #5156, #11073 ) ;
#14288=EDGE_LOOP ( 'NONE', ( #11555, #7957, #14987, #4755 ) ) ;
#14294=CARTESIAN_POINT ( 'NONE',  ( 0.02436607992776281678, 2.336989772644269436, 24.63872515616083447 ) ) ;
#14301=AXIS2_PLACEMENT_3D ( 'NONE', #7990, #3497, #6575 ) ;
#14303=CARTESIAN_POINT ( 'NONE',  ( 2.789999999999999147, 12.59161484032942901, -21.30679549418617924 ) ) ;
#14304=VECTOR ( 'NONE', #13271, 1000.000000000000000 ) ;
#14305=CARTESIAN_POINT ( 'NONE',  ( 2.789999999999999147, -20.70663861606260170, -15.04425356660783031 ) ) ;
#14308=CARTESIAN_POINT ( 'NONE',  ( 8.000000000000000000, 0.000000000000000000, 0.000000000000000000 ) ) ;
#14309=CARTESIAN_POINT ( 'NONE',  ( 1.394999999999999574, -12.96210679857767900, -24.89775460606846380 ) ) ;
#14313=EDGE_CURVE ( 'NONE', #6761, #17056, #10142, .T. ) ;
#14318=AXIS2_PLACEMENT_3D ( 'NONE', #11080, #1578, #7667 ) ;
#14324=CARTESIAN_POINT ( 'NONE',  ( 1.394999999999999574, -4.633866840649122132, 27.68468304288257542 ) ) ;
#14328=ORIENTED_EDGE ( 'NONE', *, *, #15473, .F. ) ;
#14338=CARTESIAN_POINT ( 'NONE',  ( 2.765633920072239516, 21.30679549418631780, 12.59161484032919986 ) ) ;
#14341=EDGE_CURVE ( 'NONE', #2962, #16730, #11322, .T. ) ;
#14347=CARTESIAN_POINT ( 'NONE',  ( 0.5279273620711150139, 23.73240184472514613, -12.96450951081191150 ) ) ;
#14349=CARTESIAN_POINT ( 'NONE',  ( 1.749999999999998002, -24.89775460606821866, -12.96210679857815684 ) ) ;
#14361=DIRECTION ( 'NONE',  ( -1.000000000000000000, -0.000000000000000000, -0.000000000000000000 ) ) ;
#14369=EDGE_CURVE ( 'NONE', #3518, #17740, #5640, .T. ) ;
#14370=DIRECTION ( 'NONE',  ( 1.000000000000000000, 0.000000000000000000, -0.000000000000000000 ) ) ;
#14372=CARTESIAN_POINT ( 'NONE',  ( 1.749999999999998002, -19.67366047555544739, 20.02152543075338897 ) ) ;
#14376=DIRECTION ( 'NONE',  ( -1.000000000000000000, -0.000000000000000000, -0.000000000000000000 ) ) ;
#14377=EDGE_CURVE ( 'NONE', #3153, #11007, #10601, .T. ) ;
#14383=AXIS2_PLACEMENT_3D ( 'NONE', #19431, #7406, #7209 ) ;
#14384=FACE_OUTER_BOUND ( 'NONE', #10022, .T. ) ;
#14385=EDGE_CURVE ( 'NONE', #3518, #7686, #10531, .T. ) ;
#14388=ORIENTED_EDGE ( 'NONE', *, *, #18360, .F. ) ;
#14391=ORIENTED_EDGE ( 'NONE', *, *, #861, .F. ) ;
#14394=VECTOR ( 'NONE', #14407, 1000.000000000000000 ) ;
#14396=AXIS2_PLACEMENT_3D ( 'NONE', #10902, #4797, #3398 ) ;
#14405=CARTESIAN_POINT ( 'NONE',  ( 2.262072769566602304, 11.57956866523218586, 24.43806413951680767 ) ) ;
#14407=DIRECTION ( 'NONE',  ( -1.000000000000000000, 0.000000000000000000, -0.000000000000000000 ) ) ;
#14409=EDGE_LOOP ( 'NONE', ( #18374, #1267, #4269, #8601 ) ) ;
#14415=CYLINDRICAL_SURFACE ( 'NONE', #374, 13.19999999999999929 ) ;
#14416=CARTESIAN_POINT ( 'NONE',  ( 2.789999999999999147, 12.52067188844351442, 20.62201879784917935 ) ) ;
#14417=ORIENTED_EDGE ( 'NONE', *, *, #7227, .F. ) ;
#14420=CARTESIAN_POINT ( 'NONE',  ( 0.000000000000000000, 15.74360496233383522, 18.28042085475283329 ) ) ;
#14421=CARTESIAN_POINT ( 'NONE',  ( 2.789679245949058917, 20.70663861606308487, -12.51925356660738053 ) ) ;
#14425=DIRECTION ( 'NONE',  ( -1.000000000000000000, -0.000000000000000000, -0.000000000000000000 ) ) ;
#14431=CARTESIAN_POINT ( 'NONE',  ( 1.039999999999997593, 0.000000000000000000, 0.000000000000000000 ) ) ;
#14432=ORIENTED_EDGE ( 'NONE', *, *, #17370, .T. ) ;
#14435=CARTESIAN_POINT ( 'NONE',  ( 2.789999999999999147, 21.30679549418649543, -12.59161484032888723 ) ) ;
#14437=EDGE_CURVE ( 'NONE', #8766, #1773, #7966, .T. ) ;
#14443=AXIS2_PLACEMENT_3D ( 'NONE', #8694, #18007, #7170 ) ;
#14445=CARTESIAN_POINT ( 'NONE',  ( 0.02436607992775891365, -24.63872515616080960, -2.336989772644527008 ) ) ;
#14454=CARTESIAN_POINT ( 'NONE',  ( 0.006931069955678950678, -18.43696893154746164, -16.17493693894899209 ) ) ;
#14463=ORIENTED_EDGE ( 'NONE', *, *, #17955, .F. ) ;
#14469=AXIS2_PLACEMENT_3D ( 'NONE', #12679, #10880, #4870 ) ;
#14475=AXIS2_PLACEMENT_3D ( 'NONE', #11312, #17412, #6976 ) ;
#14483=EDGE_CURVE ( 'NONE', #11614, #13582, #8113, .T. ) ;
#14504=CYLINDRICAL_SURFACE ( 'NONE', #14190, 13.19999999999999929 ) ;
#14516=CARTESIAN_POINT ( 'NONE',  ( 2.765633920072235963, 21.30679549418649543, -12.59161484032888723 ) ) ;
#14517=CARTESIAN_POINT ( 'NONE',  ( 2.257825491203655055, -11.58891744060124473, 24.44564404695840665 ) ) ;
#14521=ORIENTED_EDGE ( 'NONE', *, *, #2254, .F. ) ;
#14524=CARTESIAN_POINT ( 'NONE',  ( 2.257825459230520693, 4.993157874727810253, 26.58873630738054317 ) ) ;
#14526=ORIENTED_EDGE ( 'NONE', *, *, #8145, .T. ) ;
#14537=CARTESIAN_POINT ( 'NONE',  ( -7.810937420967753123E-14, 20.85287692521929159, 12.51293083811806461 ) ) ;
#14538=AXIS2_PLACEMENT_3D ( 'NONE', #16221, #10120, #8706 ) ;
#14539=CARTESIAN_POINT ( 'NONE',  ( 1.749999999999998002, 0.000000000000000000, 0.000000000000000000 ) ) ;
#14545=VECTOR ( 'NONE', #3705, 1000.000000000000000 ) ;
#14547=ADVANCED_FACE ( 'NONE', ( #2566 ), #2470, .T. ) ;
#14554=EDGE_CURVE ( 'NONE', #16193, #18731, #11803, .T. ) ;
#14557=EDGE_LOOP ( 'NONE', ( #16679, #8373, #16189, #16791 ) ) ;
#14559=VECTOR ( 'NONE', #8241, 1000.000000000000000 ) ;
#14565=CYLINDRICAL_SURFACE ( 'NONE', #15522, 13.19999999999999929 ) ;
#14568=CARTESIAN_POINT ( 'NONE',  ( 0.1855657389739082119, 5.253342437939721776, 25.39738473785002881 ) ) ;
#14569=EDGE_CURVE ( 'NONE', #1120, #7944, #19613, .T. ) ;
#14570=ADVANCED_FACE ( 'NONE', ( #6866 ), #7253, .F. ) ;
#14574=CARTESIAN_POINT ( 'NONE',  ( 0.000000000000000000, 15.74360496233409634, -18.28042085475261302 ) ) ;
#14580=DIRECTION ( 'NONE',  ( 0.000000000000000000, 0.000000000000000000, 1.000000000000000000 ) ) ;
#14581=ORIENTED_EDGE ( 'NONE', *, *, #873, .F. ) ;
#14582=ORIENTED_EDGE ( 'NONE', *, *, #8932, .T. ) ;
#14583=CARTESIAN_POINT ( 'NONE',  ( 2.789999999999999147, -9.324097380959294412, -22.25075486061747654 ) ) ;
#14586=EDGE_CURVE ( 'NONE', #3731, #13404, #11630, .T. ) ;
#14592=ORIENTED_EDGE ( 'NONE', *, *, #7299, .F. ) ;
#14593=DIRECTION ( 'NONE',  ( 1.000000000000000000, -0.000000000000000000, 0.000000000000000000 ) ) ;
#14596=AXIS2_PLACEMENT_3D ( 'NONE', #5765, #13379, #1382 ) ;
#14599=CARTESIAN_POINT ( 'NONE',  ( 1.039999999999997149, -27.68468304288261805, 4.633866840648821039 ) ) ;
#14603=VERTEX_POINT ( 'NONE', #6060 ) ;
#14610=AXIS2_PLACEMENT_3D ( 'NONE', #16199, #8784, #5572 ) ;
#14619=CARTESIAN_POINT ( 'NONE',  ( 0.1882239080259273667, 5.251266773802727883, -25.40949241676348080 ) ) ;
#14623=CIRCLE ( 'NONE', #13022, 28.06981291497571362 ) ;
#14627=CIRCLE ( 'NONE', #13663, 28.06981291497571007 ) ;
#14628=DIRECTION ( 'NONE',  ( -1.000000000000000000, -0.000000000000000000, -0.000000000000000000 ) ) ;
#14630=LINE ( 'NONE', #3913, #10481 ) ;
#14632=CARTESIAN_POINT ( 'NONE',  ( 2.031033471609898111, 3.797536611356316705, 27.31260702007176988 ) ) ;
#14638=CARTESIAN_POINT ( 'NONE',  ( 2.601776096565022289, 12.84621645676845070, 22.54313264455018384 ) ) ;
#14640=VECTOR ( 'NONE', #10396, 1000.000000000000000 ) ;
#14644=CARTESIAN_POINT ( 'NONE',  ( 2.789999999999999147, 23.31896751603342821, -7.334849878007252855 ) ) ;
#14646=ORIENTED_EDGE ( 'NONE', *, *, #12816, .F. ) ;
#14651=VERTEX_POINT ( 'NONE', #12085 ) ;
#14663=EDGE_CURVE ( 'NONE', #16676, #8648, #3445, .T. ) ;
#14664=FACE_OUTER_BOUND ( 'NONE', #1748, .T. ) ;
#14666=AXIS2_PLACEMENT_3D ( 'NONE', #7215, #14848, #13434 ) ;
#14668=CARTESIAN_POINT ( 'NONE',  ( 2.718184749312774873, 25.22524549359950541, 2.576941577947493567 ) ) ;
#14670=CARTESIAN_POINT ( 'NONE',  ( 1.039999999999996705, 27.76164181293051669, -4.147968289691385202 ) ) ;
#14684=EDGE_CURVE ( 'NONE', #17509, #19081, #15190, .T. ) ;
#14688=ORIENTED_EDGE ( 'NONE', *, *, #13868, .T. ) ;
#14689=CARTESIAN_POINT ( 'NONE',  ( 0.02436607992775978102, 2.336989772644613161, -24.63872515616080250 ) ) ;
#14690=CARTESIAN_POINT ( 'NONE',  ( 1.394999999999998685, 19.67366047555559661, -20.02152543075324331 ) ) ;
#14692=DIRECTION ( 'NONE',  ( -1.000000000000000000, 0.000000000000000000, 0.000000000000000000 ) ) ;
#14698=CARTESIAN_POINT ( 'NONE',  ( 1.039999999999997593, 0.000000000000000000, 0.000000000000000000 ) ) ;
#14702=ORIENTED_EDGE ( 'NONE', *, *, #14569, .T. ) ;
#14703=EDGE_CURVE ( 'NONE', #2600, #993, #18711, .T. ) ;
#14704=CARTESIAN_POINT ( 'NONE',  ( 2.783068961317271217, -12.53626894672843051, 21.08061549536610713 ) ) ;
#14706=EDGE_CURVE ( 'NONE', #13582, #6761, #14180, .T. ) ;
#14707=CARTESIAN_POINT ( 'NONE',  ( 2.789999999999999147, -1.991882183130462503, 24.04302995059964942 ) ) ;
#14709=ORIENTED_EDGE ( 'NONE', *, *, #16725, .F. ) ;
#14711=VECTOR ( 'NONE', #7512, 1000.000000000000000 ) ;
#14712=CARTESIAN_POINT ( 'NONE',  ( -5.209999999999999964, 0.000000000000000000, 0.000000000000000000 ) ) ;
#14724=EDGE_CURVE ( 'NONE', #8429, #19636, #17760, .T. ) ;
#14727=CARTESIAN_POINT ( 'NONE',  ( 8.000000000000000000, 0.000000000000000000, 0.000000000000000000 ) ) ;
#14735=EDGE_CURVE ( 'NONE', #13251, #15913, #11647, .T. ) ;
#14736=CARTESIAN_POINT ( 'NONE',  ( 2.789999999999999147, 0.000000000000000000, 0.000000000000000000 ) ) ;
#14737=CARTESIAN_POINT ( 'NONE',  ( 2.765633920072242180, 22.71065055754465689, -9.836394144775473691 ) ) ;
#14739=DIRECTION ( 'NONE',  ( -1.000000000000000000, 0.000000000000000000, 0.000000000000000000 ) ) ;
#14744=ORIENTED_EDGE ( 'NONE', *, *, #16802, .F. ) ;
#14745=CYLINDRICAL_SURFACE ( 'NONE', #9176, 13.19999999999999929 ) ;
#14750=ORIENTED_EDGE ( 'NONE', *, *, #12990, .F. ) ;
#14758=VERTEX_POINT ( 'NONE', #3466 ) ;
#14760=AXIS2_PLACEMENT_3D ( 'NONE', #18585, #17093, #6176 ) ;
#14761=CARTESIAN_POINT ( 'NONE',  ( 2.765633920072235963, 24.63872515616082737, 2.336989772644355146 ) ) ;
#14762=CIRCLE ( 'NONE', #19536, 24.12539914357697413 ) ;
#14766=DIRECTION ( 'NONE',  ( 0.000000000000000000, 0.000000000000000000, 1.000000000000000000 ) ) ;
#14777=ORIENTED_EDGE ( 'NONE', *, *, #4351, .T. ) ;
#14787=DIRECTION ( 'NONE',  ( -1.000000000000000000, 0.000000000000000000, -0.000000000000000000 ) ) ;
#14789=DIRECTION ( 'NONE',  ( 0.000000000000000000, 0.000000000000000000, 1.000000000000000000 ) ) ;
#14791=CARTESIAN_POINT ( 'NONE',  ( -7.664413047240269201E-14, 2.133839912090805147, 24.22524813288763568 ) ) ;
#14793=ORIENTED_EDGE ( 'NONE', *, *, #4939, .F. ) ;
#14794=DIRECTION ( 'NONE',  ( 0.000000000000000000, 0.000000000000000000, 1.000000000000000000 ) ) ;
#14799=CIRCLE ( 'NONE', #16398, 28.06981291497571007 ) ;
#14802=B_SPLINE_CURVE_WITH_KNOTS ( 'NONE', 3,
 ( #12650, #11147, #12947, #14737 ),
 .UNSPECIFIED., .F., .F.,
 ( 4, 4 ),
 ( 0.005258105385878691744, 0.005948373736081389272 ),
 .UNSPECIFIED. ) ;
#14804=CARTESIAN_POINT ( 'NONE',  ( 2.790000000000079527, -18.34439787333494820, -15.96555658743782580 ) ) ;
#14805=CARTESIAN_POINT ( 'NONE',  ( 2.765633920072235519, 18.55949924794892780, 16.37294372382865504 ) ) ;
#14809=CARTESIAN_POINT ( 'NONE',  ( 2.601776091974069338, 5.251266773802368171, 25.40949241676355541 ) ) ;
#14817=EDGE_CURVE ( 'NONE', #10168, #10294, #18664, .T. ) ;
#14818=CARTESIAN_POINT ( 'NONE',  ( 2.789999999999999147, -7.909232158574988958, 24.34211360614297348 ) ) ;
#14823=DIRECTION ( 'NONE',  ( 0.000000000000000000, 0.000000000000000000, 1.000000000000000000 ) ) ;
#14825=VERTEX_POINT ( 'NONE', #5647 ) ;
#14827=ADVANCED_FACE ( 'NONE', ( #11760 ), #17864, .T. ) ;
#14833=CARTESIAN_POINT ( 'NONE',  ( 2.789999999999999147, 0.000000000000000000, 0.000000000000000000 ) ) ;
#14835=ORIENTED_EDGE ( 'NONE', *, *, #8490, .F. ) ;
#14840=DIRECTION ( 'NONE',  ( -1.000000000000000000, -0.000000000000000000, -0.000000000000000000 ) ) ;
#14842=CARTESIAN_POINT ( 'NONE',  ( 0.000000000000000000, 0.000000000000000000, 0.000000000000000000 ) ) ;
#14848=DIRECTION ( 'NONE',  ( -1.000000000000000000, -0.000000000000000000, -0.000000000000000000 ) ) ;
#14851=DIRECTION ( 'NONE',  ( -1.000000000000000000, -0.000000000000000000, -0.000000000000000000 ) ) ;
#14860=PLANE ( 'NONE',  #19505 ) ;
#14867=LINE ( 'NONE', #19455, #3533 ) ;
#14872=ORIENTED_EDGE ( 'NONE', *, *, #11467, .T. ) ;
#14874=CARTESIAN_POINT ( 'NONE',  ( 0.000000000000000000, -5.535312321042921369, 23.48180575137728354 ) ) ;
#14877=DIRECTION ( 'NONE',  ( 0.000000000000000000, 0.000000000000000000, 1.000000000000000000 ) ) ;
#14879=CARTESIAN_POINT ( 'NONE',  ( 0.7589665326895889130, -12.98167595241004335, -24.32849926382764849 ) ) ;
#14880=VERTEX_POINT ( 'NONE', #18262 ) ;
#14883=B_SPLINE_CURVE_WITH_KNOTS ( 'NONE', 3,
 ( #1439, #6124, #1336, #5927, #16750, #7521 ),
 .UNSPECIFIED., .F., .F.,
 ( 4, 2, 4 ),
 ( 2.321268216997094965E-07, 0.001878622960950499009, 0.003757013795079297992 ),
 .UNSPECIFIED. ) ;
#14889=CARTESIAN_POINT ( 'NONE',  ( 1.394999999999998685, 20.02152543075374425, -19.67366047555508857 ) ) ;
#14891=DIRECTION ( 'NONE',  ( -1.000000000000000000, 0.000000000000000000, 0.000000000000000000 ) ) ;
#14898=ORIENTED_EDGE ( 'NONE', *, *, #10838, .F. ) ;
#14899=CARTESIAN_POINT ( 'NONE',  ( 2.790000000000000480, -12.51294990530030837, 20.85230829256849105 ) ) ;
#14900=DIRECTION ( 'NONE',  ( 0.000000000000000000, 0.000000000000000000, 1.000000000000000000 ) ) ;
#14901=AXIS2_PLACEMENT_3D ( 'NONE', #11329, #11515, #3908 ) ;
#14904=EDGE_CURVE ( 'NONE', #4439, #11113, #8256, .T. ) ;
#14906=CARTESIAN_POINT ( 'NONE',  ( 8.000000000000000000, 0.000000000000000000, 0.000000000000000000 ) ) ;
#14907=CARTESIAN_POINT ( 'NONE',  ( 2.765633920072239516, -24.63872515616084513, 2.336989772644183283 ) ) ;
#14908=DIRECTION ( 'NONE',  ( -1.000000000000000000, 0.000000000000000000, 0.000000000000000000 ) ) ;
#14914=CARTESIAN_POINT ( 'NONE',  ( 1.039999999999996927, -25.12109765559644714, -12.52377138324250438 ) ) ;
#14920=EDGE_CURVE ( 'NONE', #312, #5246, #5155, .T. ) ;
#14930=DIRECTION ( 'NONE',  ( -1.000000000000000000, -0.000000000000000000, -0.000000000000000000 ) ) ;
#14935=CARTESIAN_POINT ( 'NONE',  ( 0.009102498987474663336, -21.10878525316950771, -12.54316204260915768 ) ) ;
#14937=CARTESIAN_POINT ( 'NONE',  ( 0.07181525696555274285, -24.78695292654917637, -5.344212458769628249 ) ) ;
#14938=ORIENTED_EDGE ( 'NONE', *, *, #15321, .F. ) ;
#14939=CARTESIAN_POINT ( 'NONE',  ( 0.7589665283900980386, -27.31260702007172725, -3.797536611356600034 ) ) ;
#14956=DIRECTION ( 'NONE',  ( -1.000000000000000000, 0.000000000000000000, -0.000000000000000000 ) ) ;
#14958=CIRCLE ( 'NONE', #13039, 2.524999999999995470 ) ;
#14978=DIRECTION ( 'NONE',  ( 0.000000000000000000, 0.000000000000000000, 1.000000000000000000 ) ) ;
#14981=CARTESIAN_POINT ( 'NONE',  ( 2.789999999999999147, -7.909232158574988958, 24.34211360614297348 ) ) ;
#14986=CARTESIAN_POINT ( 'NONE',  ( 2.789999999999999147, 7.334849878007507762, 23.31896751603335005 ) ) ;
#14987=ORIENTED_EDGE ( 'NONE', *, *, #408, .F. ) ;
#14988=FACE_OUTER_BOUND ( 'NONE', #7283, .T. ) ;
#14991=UNCERTAINTY_MEASURE_WITH_UNIT (LENGTH_MEASURE( 1.000000000000000082E-05 ), #10803, 'distance_accuracy_value', 'NONE');
#14995=CARTESIAN_POINT ( 'NONE',  ( 2.789999999999999147, -14.18181402625756959, 19.91106274590508107 ) ) ;
#15001=VERTEX_POINT ( 'NONE', #10855 ) ;
#15003=AXIS2_PLACEMENT_3D ( 'NONE', #9664, #5048, #6728 ) ;
#15004=CARTESIAN_POINT ( 'NONE',  ( 0.02436607992776541887, 12.59161484032942901, -21.30679549418617924 ) ) ;
#15014=CARTESIAN_POINT ( 'NONE',  ( 1.039999999999996261, 12.96210679857786197, 24.89775460606836788 ) ) ;
#15018=CARTESIAN_POINT ( 'NONE',  ( 1.749999999999998002, -12.52377138324206030, -25.12109765559667096 ) ) ;
#15019=CARTESIAN_POINT ( 'NONE',  ( 2.031033465052724196, 27.14933624560908498, 4.828387785248115627 ) ) ;
#15023=CARTESIAN_POINT ( 'NONE',  ( 2.262072706628479590, 18.56460150496938155, 19.66369668717039332 ) ) ;
#15024=B_SPLINE_CURVE_WITH_KNOTS ( 'NONE', 3,
 ( #10226, #2504, #5414, #11524, #19216, #16029 ),
 .UNSPECIFIED., .F., .F.,
 ( 4, 2, 4 ),
 ( 2.586195665736120714E-07, 0.001878649493629692274, 0.003757040367692811213 ),
 .UNSPECIFIED. ) ;
#15038=CARTESIAN_POINT ( 'NONE',  ( 2.765633920072235519, 18.55949924794892780, 16.37294372382865504 ) ) ;
#15045=CARTESIAN_POINT ( 'NONE',  ( 2.789999999999999147, -15.04425356660744839, -20.70663861606288236 ) ) ;
#15047=DIRECTION ( 'NONE',  ( 0.000000000000000000, 0.000000000000000000, 1.000000000000000000 ) ) ;
#15052=EDGE_CURVE ( 'NONE', #16588, #479, #18523, .T. ) ;
#15059=VERTEX_POINT ( 'NONE', #18452 ) ;
#15062=CIRCLE ( 'NONE', #2960, 28.06981291497571007 ) ;
#15067=ORIENTED_EDGE ( 'NONE', *, *, #3459, .F. ) ;
#15076=CARTESIAN_POINT ( 'NONE',  ( 0.5279273620711166792, -12.96450951081199499, -23.73240184472509995 ) ) ;
#15081=ADVANCED_FACE ( 'NONE', ( #4745 ), #2042, .F. ) ;
#15088=ORIENTED_EDGE ( 'NONE', *, *, #10988, .F. ) ;
#15096=CARTESIAN_POINT ( 'NONE',  ( 0.02436607992776238310, -12.59161484032927092, 21.30679549418627161 ) ) ;
#15097=EDGE_LOOP ( 'NONE', ( #10903, #9978, #17445, #5301 ) ) ;
#15098=CARTESIAN_POINT ( 'NONE',  ( 1.394999999999999574, -25.12109765559644714, -12.52377138324250616 ) ) ;
#15105=AXIS2_PLACEMENT_3D ( 'NONE', #12442, #3335, #137 ) ;
#15112=TOROIDAL_SURFACE ( 'NONE', #1046, 24.12539914357697768, 8.000000000000000000 ) ;
#15116=DIRECTION ( 'NONE',  ( 0.000000000000000000, 0.000000000000000000, -1.000000000000000000 ) ) ;
#15118=DIRECTION ( 'NONE',  ( -1.000000000000000000, -0.000000000000000000, -0.000000000000000000 ) ) ;
#15123=CARTESIAN_POINT ( 'NONE',  ( 2.718184745196084773, 21.92234060054363809, -12.74223776959176568 ) ) ;
#15124=ORIENTED_EDGE ( 'NONE', *, *, #13684, .F. ) ;
#15125=AXIS2_PLACEMENT_3D ( 'NONE', #14833, #4225, #17735 ) ;
#15129=CARTESIAN_POINT ( 'NONE',  ( -5.209999999999999964, 0.000000000000000000, 0.000000000000000000 ) ) ;
#15130=ORIENTED_EDGE ( 'NONE', *, *, #12842, .T. ) ;
#15133=CARTESIAN_POINT ( 'NONE',  ( -5.209999999999999964, 0.000000000000000000, 0.000000000000000000 ) ) ;
#15139=CARTESIAN_POINT ( 'NONE',  ( 2.789999999999999147, 25.59481291497571220, 0.000000000000000000 ) ) ;
#15140=AXIS2_PLACEMENT_3D ( 'NONE', #1200, #12107, #7685 ) ;
#15141=CARTESIAN_POINT ( 'NONE',  ( 0.000000000000000000, -12.52067188844335988, -20.62201879784928238 ) ) ;
#15152=CARTESIAN_POINT ( 'NONE',  ( 0.000000000000000000, 15.04425356660760293, 20.70663861606276868 ) ) ;
#15157=DIRECTION ( 'NONE',  ( -1.000000000000000000, 0.000000000000000000, -0.000000000000000000 ) ) ;
#15158=ORIENTED_EDGE ( 'NONE', *, *, #16534, .F. ) ;
#15162=CARTESIAN_POINT ( 'NONE',  ( 2.030753602223783094, -4.828194074574165384, -27.14986936243579763 ) ) ;
#15169=ORIENTED_EDGE ( 'NONE', *, *, #4390, .F. ) ;
#15171=EDGE_CURVE ( 'NONE', #283, #6839, #10420, .T. ) ;
#15172=CARTESIAN_POINT ( 'NONE',  ( 2.789999999999999147, 15.04425356660790136, -20.70663861606255196 ) ) ;
#15175=EDGE_CURVE ( 'NONE', #19072, #17360, #16157, .T. ) ;
#15179=CARTESIAN_POINT ( 'NONE',  ( 0.000000000000000000, 0.000000000000000000, 0.000000000000000000 ) ) ;
#15185=ORIENTED_EDGE ( 'NONE', *, *, #6477, .F. ) ;
#15187=CARTESIAN_POINT ( 'NONE',  ( 2.765633920072235963, -5.391175441198450713, -24.15498966839968276 ) ) ;
#15189=CARTESIAN_POINT ( 'NONE',  ( 2.789999999999999147, 7.334849878007844382, -23.31896751603323992 ) ) ;
#15190=CIRCLE ( 'NONE', #7471, 24.12539914357697413 ) ;
#15192=CARTESIAN_POINT ( 'NONE',  ( 0.02436607992775978102, 24.63872515616082737, 2.336989772644355146 ) ) ;
#15201=B_SPLINE_CURVE_WITH_KNOTS ( 'NONE', 3,
 ( #16709, #12200, #1199, #7482, #1592, #11903 ),
 .UNSPECIFIED., .F., .F.,
 ( 4, 2, 4 ),
 ( 2.132675795045763710E-07, 0.001878604073277002169, 0.003756994878974500001 ),
 .UNSPECIFIED. ) ;
#15210=ORIENTED_EDGE ( 'NONE', *, *, #15222, .T. ) ;
#15213=ADVANCED_FACE ( 'NONE', ( #17456 ), #6926, .T. ) ;
#15221=CARTESIAN_POINT ( 'NONE',  ( 2.789999999999999147, 15.74360496233408213, -18.28042085475260592 ) ) ;
#15222=EDGE_CURVE ( 'NONE', #18023, #11483, #3000, .T. ) ;
#15226=AXIS2_PLACEMENT_3D ( 'NONE', #2608, #3925, #19222 ) ;
#15228=DIRECTION ( 'NONE',  ( -1.000000000000000000, -0.000000000000000000, 0.000000000000000000 ) ) ;
#15229=FACE_OUTER_BOUND ( 'NONE', #18253, .T. ) ;
#15235=AXIS2_PLACEMENT_3D ( 'NONE', #10217, #2994, #16713 ) ;
#15240=ORIENTED_EDGE ( 'NONE', *, *, #3708, .F. ) ;
#15250=CARTESIAN_POINT ( 'NONE',  ( 0.5279273381794633568, -3.461047254864449307, 26.82026385750176445 ) ) ;
#15251=EDGE_CURVE ( 'NONE', #15528, #10889, #7266, .T. ) ;
#15252=VERTEX_POINT ( 'NONE', #9865 ) ;
#15254=CARTESIAN_POINT ( 'NONE',  ( 2.789999999999999147, -5.456805104201270851, 23.69843731927166885 ) ) ;
#15257=ORIENTED_EDGE ( 'NONE', *, *, #3095, .F. ) ;
#15258=EDGE_CURVE ( 'NONE', #8477, #11999, #8746, .T. ) ;
#15259=CARTESIAN_POINT ( 'NONE',  ( 2.783068961317272549, 21.08061549536614976, 12.53626894672835945 ) ) ;
#15260=CARTESIAN_POINT ( 'NONE',  ( 2.789999999999999147, -22.25075486061731667, -9.324097380959683434 ) ) ;
#15264=ORIENTED_EDGE ( 'NONE', *, *, #1055, .T. ) ;
#15269=VECTOR ( 'NONE', #19737, 1000.000000000000000 ) ;
#15272=ORIENTED_EDGE ( 'NONE', *, *, #2245, .F. ) ;
#15275=ADVANCED_FACE ( 'NONE', ( #1327 ), #9032, .T. ) ;
#15277=DIRECTION ( 'NONE',  ( 0.000000000000000000, 0.000000000000000000, 1.000000000000000000 ) ) ;
#15278=ORIENTED_EDGE ( 'NONE', *, *, #14385, .T. ) ;
#15281=ORIENTED_EDGE ( 'NONE', *, *, #9903, .T. ) ;
#15288=VERTEX_POINT ( 'NONE', #5917 ) ;
#15289=CARTESIAN_POINT ( 'NONE',  ( 1.039999999999996483, -19.67366047555544384, 20.02152543075338897 ) ) ;
#15292=CARTESIAN_POINT ( 'NONE',  ( 2.789999999999999591, 12.51294990530046292, -20.85230829256839513 ) ) ;
#15295=CARTESIAN_POINT ( 'NONE',  ( 0.02436607992776411782, -24.63872515616084513, 2.336989772644183283 ) ) ;
#15297=ADVANCED_FACE ( 'NONE', ( #11834 ), #13531, .F. ) ;
#15301=CARTESIAN_POINT ( 'NONE',  ( 2.262072625383134916, -26.57710921259758408, -4.996265754456650221 ) ) ;
#15304=CARTESIAN_POINT ( 'NONE',  ( 0.000000000000000000, -1.991882183130148087, -24.04302995059968140 ) ) ;
#15305=B_SPLINE_CURVE_WITH_KNOTS ( 'NONE', 3,
 ( #18803, #7519, #19735, #16748 ),
 .UNSPECIFIED., .F., .F.,
 ( 4, 4 ),
 ( 0.005258105385878709091, 0.005948373736081389272 ),
 .UNSPECIFIED. ) ;
#15312=( NAMED_UNIT ( * ) SI_UNIT ( $, .STERADIAN. ) SOLID_ANGLE_UNIT ( ) );
#15321=EDGE_CURVE ( 'NONE', #18731, #1773, #16636, .T. ) ;
#15322=DIRECTION ( 'NONE',  ( -1.000000000000000000, 0.000000000000000000, 0.000000000000000000 ) ) ;
#15325=ORIENTED_EDGE ( 'NONE', *, *, #14313, .F. ) ;
#15327=DIRECTION ( 'NONE',  ( 0.000000000000000000, 0.000000000000000000, 1.000000000000000000 ) ) ;
#15331=EDGE_CURVE ( 'NONE', #9218, #283, #11934, .T. ) ;
#15334=ORIENTED_EDGE ( 'NONE', *, *, #2734, .T. ) ;
#15335=DIRECTION ( 'NONE',  ( 0.000000000000000000, -0.5877852522924684742, -0.8090169943749507819 ) ) ;
#15336=ADVANCED_FACE ( 'NONE', ( #16741 ), #19525, .T. ) ;
#15340=CARTESIAN_POINT ( 'NONE',  ( 0.02436607992776325046, 16.37294372382858398, 18.55949924794898465 ) ) ;
#15345=B_SPLINE_CURVE_WITH_KNOTS ( 'NONE', 3,
 ( #10669, #9468, #3052, #12569, #7847, #4957 ),
 .UNSPECIFIED., .F., .F.,
 ( 4, 2, 4 ),
 ( 1.979325885420462316E-07, 0.001878588715165608420, 0.003756979497742674902 ),
 .UNSPECIFIED. ) ;
#15347=CARTESIAN_POINT ( 'NONE',  ( 2.765633920072242624, -22.71065055754459650, 9.836394144775621129 ) ) ;
#15348=CARTESIAN_POINT ( 'NONE',  ( 8.000000000000000000, 0.000000000000000000, 0.000000000000000000 ) ) ;
#15350=ORIENTED_EDGE ( 'NONE', *, *, #15052, .T. ) ;
#15352=DIRECTION ( 'NONE',  ( 0.000000000000000000, 0.000000000000000000, 1.000000000000000000 ) ) ;
#15356=B_SPLINE_CURVE_WITH_KNOTS ( 'NONE', 3,
 ( #13733, #12239, #10734, #1626 ),
 .UNSPECIFIED., .F., .F.,
 ( 4, 4 ),
 ( 2.135345996173300665E-07, 0.0006888010880210822381 ),
 .UNSPECIFIED. ) ;
#15357=CARTESIAN_POINT ( 'NONE',  ( 2.765633920072239516, 21.30679549418631780, 12.59161484032919986 ) ) ;
#15366=CARTESIAN_POINT ( 'NONE',  ( 2.262072637928881580, 12.96450951081251191, -23.73240184472483350 ) ) ;
#15370=CARTESIAN_POINT ( 'NONE',  ( 0.006931038682726457442, 12.53626894672828485, 21.08061549536619950 ) ) ;
#15371=AXIS2_PLACEMENT_3D ( 'NONE', #13796, #493, #10797 ) ;
#15377=CIRCLE ( 'NONE', #7693, 2.524999999999995914 ) ;
#15383=VERTEX_POINT ( 'NONE', #18241 ) ;
#15384=CARTESIAN_POINT ( 'NONE',  ( 2.765633920072241292, 18.55949924794916228, -16.37294372382838148 ) ) ;
#15387=ORIENTED_EDGE ( 'NONE', *, *, #9817, .F. ) ;
#15398=ORIENTED_EDGE ( 'NONE', *, *, #4026, .T. ) ;
#15399=CARTESIAN_POINT ( 'NONE',  ( 1.749999999999998002, -25.12109765559663188, 12.52377138324213668 ) ) ;
#15401=ADVANCED_FACE ( 'NONE', ( #4519 ), #12237, .T. ) ;
#15403=CARTESIAN_POINT ( 'NONE',  ( 2.765633920072239516, -24.15498966839958683, -5.391175441198872598 ) ) ;
#15406=CIRCLE ( 'NONE', #11888, 2.524999999999995914 ) ;
#15412=CYLINDRICAL_SURFACE ( 'NONE', #11607, 2.524999999999995914 ) ;
#15415=CARTESIAN_POINT ( 'NONE',  ( 0.000000000000000000, 25.59481291497571220, 0.000000000000000000 ) ) ;
#15417=CARTESIAN_POINT ( 'NONE',  ( 2.789999999999999147, 5.391175441198956086, -24.15498966839956907 ) ) ;
#15432=CARTESIAN_POINT ( 'NONE',  ( -7.625032001148274383E-14, 9.515416771311183908, 22.38018801136479397 ) ) ;
#15443=DIRECTION ( 'NONE',  ( 0.000000000000000000, 0.000000000000000000, 1.000000000000000000 ) ) ;
#15452=STYLED_ITEM ( 'NONE', ( #1301 ), #2068 ) ;
#15459=AXIS2_PLACEMENT_3D ( 'NONE', #8701, #11704, #910 ) ;
#15464=LINE ( 'NONE', #16868, #87 ) ;
#15468=ORIENTED_EDGE ( 'NONE', *, *, #9329, .F. ) ;
#15473=EDGE_CURVE ( 'NONE', #3050, #15740, #11128, .T. ) ;
#15474=CARTESIAN_POINT ( 'NONE',  ( 0.000000000000000000, 24.34211360614300190, 7.909232158574900140 ) ) ;
#15478=DIRECTION ( 'NONE',  ( -1.000000000000000000, -0.000000000000000000, -0.000000000000000000 ) ) ;
#15480=CARTESIAN_POINT ( 'NONE',  ( 2.765633920072239071, -12.59161484032927092, 21.30679549418627161 ) ) ;
#15485=ADVANCED_FACE ( 'NONE', ( #10732 ), #16843, .F. ) ;
#15490=DIRECTION ( 'NONE',  ( -1.000000000000000000, -0.000000000000000000, 0.000000000000000000 ) ) ;
#15496=DIRECTION ( 'NONE',  ( 0.000000000000000000, 0.000000000000000000, 1.000000000000000000 ) ) ;
#15501=CARTESIAN_POINT ( 'NONE',  ( 0.1882238782932339760, -19.18368891937503307, 17.47009390565483855 ) ) ;
#15502=EDGE_CURVE ( 'NONE', #5836, #13251, #15980, .T. ) ;
#15507=TOROIDAL_SURFACE ( 'NONE', #11988, 24.12539914357697768, 8.000000000000000000 ) ;
#15508=CARTESIAN_POINT ( 'NONE',  ( 1.894355403937850069, -24.59653223688283674, 12.96989951879399072 ) ) ;
#15516=CARTESIAN_POINT ( 'NONE',  ( 1.039999999999997593, 0.000000000000000000, 0.000000000000000000 ) ) ;
#15517=DIRECTION ( 'NONE',  ( -1.000000000000000000, -0.000000000000000000, -0.000000000000000000 ) ) ;
#15519=ORIENTED_EDGE ( 'NONE', *, *, #7465, .F. ) ;
#15520=CYLINDRICAL_SURFACE ( 'NONE', #12522, 13.19999999999999929 ) ;
#15522=AXIS2_PLACEMENT_3D ( 'NONE', #2436, #6933, #6732 ) ;
#15528=VERTEX_POINT ( 'NONE', #9331 ) ;
#15531=ORIENTED_EDGE ( 'NONE', *, *, #11763, .F. ) ;
#15532=EDGE_CURVE ( 'NONE', #7717, #2446, #2236, .T. ) ;
#15536=DIRECTION ( 'NONE',  ( -1.000000000000000000, 0.000000000000000000, -0.000000000000000000 ) ) ;
#15539=DIRECTION ( 'NONE',  ( -1.000000000000000000, -0.000000000000000000, -0.000000000000000000 ) ) ;
#15546=CARTESIAN_POINT ( 'NONE',  ( 2.790000000000079527, 18.34439787333507255, 15.96555658743769079 ) ) ;
#15551=CARTESIAN_POINT ( 'NONE',  ( 2.789999999999999147, -5.535312321042557215, -23.48180575137735815 ) ) ;
#15555=VERTEX_POINT ( 'NONE', #15340 ) ;
#15557=ORIENTED_EDGE ( 'NONE', *, *, #6095, .F. ) ;
#15565=B_SPLINE_CURVE_WITH_KNOTS ( 'NONE', 3,
 ( #17992, #18088, #5670, #2567 ),
 .UNSPECIFIED., .F., .F.,
 ( 4, 4 ),
 ( 0.0006045424356927869836, 0.0006887909409525213005 ),
 .UNSPECIFIED. ) ;
#15566=AXIS2_PLACEMENT_3D ( 'NONE', #15415, #1709, #7799 ) ;
#15569=ADVANCED_FACE ( 'NONE', ( #7716 ), #12337, .F. ) ;
#15571=VERTEX_POINT ( 'NONE', #6803 ) ;
#15575=DIRECTION ( 'NONE',  ( -1.000000000000000000, -0.000000000000000000, -0.000000000000000000 ) ) ;
#15577=ORIENTED_EDGE ( 'NONE', *, *, #7099, .T. ) ;
#15584=DIRECTION ( 'NONE',  ( 0.000000000000000000, 0.000000000000000000, 1.000000000000000000 ) ) ;
#15591=VERTEX_POINT ( 'NONE', #9839 ) ;
#15594=EDGE_LOOP ( 'NONE', ( #18365, #6015, #10758, #15997, #15387, #891 ) ) ;
#15596=EDGE_CURVE ( 'NONE', #9581, #5937, #9740, .T. ) ;
#15599=DIRECTION ( 'NONE',  ( 0.000000000000000000, 0.000000000000000000, 1.000000000000000000 ) ) ;
#15602=AXIS2_PLACEMENT_3D ( 'NONE', #3195, #202, #6284 ) ;
#15609=CARTESIAN_POINT ( 'NONE',  ( 0.02436607992776411782, -24.63872515616084513, 2.336989772644183283 ) ) ;
#15622=B_SPLINE_CURVE_WITH_KNOTS ( 'NONE', 3,
 ( #9537, #15636, #3621, #5114, #3328, #4827 ),
 .UNSPECIFIED., .F., .F.,
 ( 4, 2, 4 ),
 ( 1.979325885420663486E-07, 0.001878588715165609938, 0.003756979497742677504 ),
 .UNSPECIFIED. ) ;
#15627=CARTESIAN_POINT ( 'NONE',  ( 2.601776105308175602, -25.78859396478526023, -2.857713464478961463 ) ) ;
#15628=DIRECTION ( 'NONE',  ( 0.000000000000000000, 0.000000000000000000, 1.000000000000000000 ) ) ;
#15632=ORIENTED_EDGE ( 'NONE', *, *, #3825, .T. ) ;
#15633=AXIS2_PLACEMENT_3D ( 'NONE', #17166, #761, #15662 ) ;
#15634=CARTESIAN_POINT ( 'NONE',  ( 1.394999999999998685, -4.147968289691093879, -27.76164181293055933 ) ) ;
#15635=EDGE_LOOP ( 'NONE', ( #568, #6522, #13461, #9381, #16545, #7914 ) ) ;
#15636=CARTESIAN_POINT ( 'NONE',  ( 2.718131847775119514, -5.344160105508880321, 24.78765742476137035 ) ) ;
#15642=CARTESIAN_POINT ( 'NONE',  ( 2.765633920072234631, -21.30679549418640306, 12.59161484032904887 ) ) ;
#15647=DIRECTION ( 'NONE',  ( -1.000000000000000000, 0.000000000000000000, -0.000000000000000000 ) ) ;
#15649=ORIENTED_EDGE ( 'NONE', *, *, #5059, .T. ) ;
#15651=CARTESIAN_POINT ( 'NONE',  ( 1.749999999999998002, 27.68468304288265358, -4.633866840648635410 ) ) ;
#15661=ORIENTED_EDGE ( 'NONE', *, *, #18759, .T. ) ;
#15662=DIRECTION ( 'NONE',  ( 0.000000000000000000, 0.000000000000000000, 1.000000000000000000 ) ) ;
#15664=ORIENTED_EDGE ( 'NONE', *, *, #408, .T. ) ;
#15668=EDGE_CURVE ( 'NONE', #5937, #17326, #3187, .T. ) ;
#15674=EDGE_CURVE ( 'NONE', #5246, #10962, #324, .T. ) ;
#15675=VERTEX_POINT ( 'NONE', #5314 ) ;
#15678=FACE_OUTER_BOUND ( 'NONE', #10111, .T. ) ;
#15680=ORIENTED_EDGE ( 'NONE', *, *, #650, .T. ) ;
#15683=CARTESIAN_POINT ( 'NONE',  ( 2.783068930044319877, -16.17493693894864393, -18.43696893154776006 ) ) ;
#15689=ORIENTED_EDGE ( 'NONE', *, *, #6148, .T. ) ;
#15701=ORIENTED_EDGE ( 'NONE', *, *, #18008, .F. ) ;
#15705=AXIS2_PLACEMENT_3D ( 'NONE', #31, #3866, #7524 ) ;
#15714=ORIENTED_EDGE ( 'NONE', *, *, #15674, .F. ) ;
#15717=ORIENTED_EDGE ( 'NONE', *, *, #13684, .T. ) ;
#15719=VECTOR ( 'NONE', #10696, 1000.000000000000000 ) ;
#15722=ORIENTED_EDGE ( 'NONE', *, *, #453, .T. ) ;
#15723=CARTESIAN_POINT ( 'NONE',  ( 2.718184749312774429, -25.22524549359948409, -2.576941577947671647 ) ) ;
#15734=CARTESIAN_POINT ( 'NONE',  ( 1.394999999999999574, -12.52377138324241734, 25.12109765559649688 ) ) ;
#15740=VERTEX_POINT ( 'NONE', #13608 ) ;
#15742=FACE_OUTER_BOUND ( 'NONE', #19359, .T. ) ;
#15745=EDGE_CURVE ( 'NONE', #3868, #14825, #4173, .T. ) ;
#15747=FACE_OUTER_BOUND ( 'NONE', #11641, .T. ) ;
#15756=ORIENTED_EDGE ( 'NONE', *, *, #7081, .T. ) ;
#15765=ORIENTED_EDGE ( 'NONE', *, *, #11877, .F. ) ;
#15769=CIRCLE ( 'NONE', #7422, 24.12539914357697768 ) ;
#15772=ORIENTED_EDGE ( 'NONE', *, *, #18739, .F. ) ;
#15775=CARTESIAN_POINT ( 'NONE',  ( 0.07181525696555239591, 24.78695292654921545, 5.344212458769448837 ) ) ;
#15778=DIRECTION ( 'NONE',  ( 0.000000000000000000, 0.000000000000000000, 1.000000000000000000 ) ) ;
#15779=DIRECTION ( 'NONE',  ( -1.000000000000000000, -0.000000000000000000, -0.000000000000000000 ) ) ;
#15787=ORIENTED_EDGE ( 'NONE', *, *, #17169, .F. ) ;
#15792=CARTESIAN_POINT ( 'NONE',  ( 2.765633920072236407, 2.336989772644613161, -24.63872515616080250 ) ) ;
#15794=AXIS2_PLACEMENT_3D ( 'NONE', #11516, #5595, #5692 ) ;
#15796=DIRECTION ( 'NONE',  ( -1.000000000000000000, -0.000000000000000000, 0.000000000000000000 ) ) ;
#15799=FACE_OUTER_BOUND ( 'NONE', #17449, .T. ) ;
#15809=CARTESIAN_POINT ( 'NONE',  ( 0.000000000000000000, 23.48180575137729775, 5.535312321042836103 ) ) ;
#15811=CARTESIAN_POINT ( 'NONE',  ( 2.765633920072238627, -21.30679549418621832, -12.59161484032935618 ) ) ;
#15818=ORIENTED_EDGE ( 'NONE', *, *, #2581, .F. ) ;
#15820=ADVANCED_FACE ( 'NONE', ( #6186 ), #4604, .T. ) ;
#15823=VERTEX_POINT ( 'NONE', #101 ) ;
#15824=CARTESIAN_POINT ( 'NONE',  ( 2.789999999999999147, 12.59161484032912171, 21.30679549418635688 ) ) ;
#15827=EDGE_LOOP ( 'NONE', ( #15765, #248, #4741, #11721, #13055, #3627 ) ) ;
#15829=VERTEX_POINT ( 'NONE', #10710 ) ;
#15831=CARTESIAN_POINT ( 'NONE',  ( 2.031033491000350466, -24.80232951178386713, 12.05173163741713083 ) ) ;
#15832=ORIENTED_EDGE ( 'NONE', *, *, #18708, .T. ) ;
#15842=CARTESIAN_POINT ( 'NONE',  ( 2.790000000000000480, 9.514945144208736494, 22.37986894186676423 ) ) ;
#15845=EDGE_CURVE ( 'NONE', #16305, #16734, #12810, .T. ) ;
#15849=AXIS2_PLACEMENT_3D ( 'NONE', #18164, #12750, #4947 ) ;
#15853=AXIS2_PLACEMENT_3D ( 'NONE', #1717, #16928, #13817 ) ;
#15863=EDGE_LOOP ( 'NONE', ( #3143, #9487, #17060, #9175, #10756, #18189 ) ) ;
#15868=ADVANCED_FACE ( 'NONE', ( #10807 ), #4901, .T. ) ;
#15875=CARTESIAN_POINT ( 'NONE',  ( 2.031033467310410234, -12.98167595241039329, 24.32849926382746020 ) ) ;
#15879=CARTESIAN_POINT ( 'NONE',  ( 0.07181525480391401373, -21.92234060054336098, -12.74223776959224708 ) ) ;
#15887=CARTESIAN_POINT ( 'NONE',  ( 1.039999999999997593, 0.000000000000000000, 0.000000000000000000 ) ) ;
#15892=ORIENTED_EDGE ( 'NONE', *, *, #3667, .T. ) ;
#15901=CARTESIAN_POINT ( 'NONE',  ( 0.000000000000000000, 1.991882183130315953, 24.04302995059967074 ) ) ;
#15903=DIRECTION ( 'NONE',  ( -1.000000000000000000, -0.000000000000000000, -0.000000000000000000 ) ) ;
#15905=CARTESIAN_POINT ( 'NONE',  ( 0.000000000000000000, -9.324097380959319281, -22.25075486061748009 ) ) ;
#15906=TOROIDAL_SURFACE ( 'NONE', #14301, 24.12539914357697768, 8.000000000000000000 ) ;
#15911=B_SPLINE_CURVE_WITH_KNOTS ( 'NONE', 3,
 ( #4082, #6668, #17398, #3682 ),
 .UNSPECIFIED., .F., .F.,
 ( 4, 4 ),
 ( 0.005258110598983608240, 0.005948376585272727862 ),
 .UNSPECIFIED. ) ;
#15913=VERTEX_POINT ( 'NONE', #17298 ) ;
#15915=DIRECTION ( 'NONE',  ( -1.000000000000000000, -0.000000000000000000, -0.000000000000000000 ) ) ;
#15917=LINE ( 'NONE', #8413, #14545 ) ;
#15929=VERTEX_POINT ( 'NONE', #12999 ) ;
#15936=CYLINDRICAL_SURFACE ( 'NONE', #16360, 2.524999999999995914 ) ;
#15939=ORIENTED_EDGE ( 'NONE', *, *, #9442, .F. ) ;
#15942=CARTESIAN_POINT ( 'NONE',  ( 1.749999999999998002, 0.000000000000000000, 0.000000000000000000 ) ) ;
#15946=EDGE_CURVE ( 'NONE', #15913, #15001, #17587, .T. ) ;
#15949=CIRCLE ( 'NONE', #5398, 2.524999999999998135 ) ;
#15950=ORIENTED_EDGE ( 'NONE', *, *, #861, .T. ) ;
#15955=CARTESIAN_POINT ( 'NONE',  ( 0.000000000000000000, -18.28042085475266632, -15.74360496233403239 ) ) ;
#15960=ORIENTED_EDGE ( 'NONE', *, *, #12764, .F. ) ;
#15962=CARTESIAN_POINT ( 'NONE',  ( 0.000000000000000000, -5.535312321042547445, -23.48180575137738302 ) ) ;
#15968=CIRCLE ( 'NONE', #8938, 28.06981291497571007 ) ;
#15970=DIRECTION ( 'NONE',  ( -1.000000000000000000, 0.000000000000000000, 0.000000000000000000 ) ) ;
#15971=CARTESIAN_POINT ( 'NONE',  ( 1.749999999999998002, 20.02152543075374069, -19.67366047555509212 ) ) ;
#15978=CARTESIAN_POINT ( 'NONE',  ( 2.790000000000000924, 0.000000000000000000, 4.000000000000000000 ) ) ;
#15980=CIRCLE ( 'NONE', #12793, 2.524999999999996358 ) ;
#15981=CARTESIAN_POINT ( 'NONE',  ( 2.790000000000000036, -15.96500990068111214, -18.34424029220128816 ) ) ;
#15986=ORIENTED_EDGE ( 'NONE', *, *, #9883, .T. ) ;
#15987=CARTESIAN_POINT ( 'NONE',  ( 2.789999999999999147, 0.000000000000000000, 0.000000000000000000 ) ) ;
#15993=CARTESIAN_POINT ( 'NONE',  ( 2.789999999999999147, -24.34211360614305875, 7.909232158574721616 ) ) ;
#15997=ORIENTED_EDGE ( 'NONE', *, *, #6477, .T. ) ;
#16003=EDGE_CURVE ( 'NONE', #18935, #15675, #14867, .T. ) ;
#16013=EDGE_CURVE ( 'NONE', #9137, #6839, #15968, .T. ) ;
#16019=CARTESIAN_POINT ( 'NONE',  ( 0.02436607992776151574, -18.55949924794880346, -16.37294372382878649 ) ) ;
#16027=EDGE_LOOP ( 'NONE', ( #6256, #6231, #17127, #14793, #13229, #11915 ) ) ;
#16029=CARTESIAN_POINT ( 'NONE',  ( 1.749999999999998002, 25.12109765559671004, -12.52377138324198391 ) ) ;
#16034=CARTESIAN_POINT ( 'NONE',  ( 2.718184745196085661, 12.74223776959200727, 21.92234060054350309 ) ) ;
#16039=AXIS2_PLACEMENT_3D ( 'NONE', #12297, #3280, #7973 ) ;
#16040=AXIS2_PLACEMENT_3D ( 'NONE', #13813, #12417, #4806 ) ;
#16047=B_SPLINE_CURVE_WITH_KNOTS ( 'NONE', 3,
 ( #14583, #872, #6952, #2067 ),
 .UNSPECIFIED., .F., .F.,
 ( 4, 4 ),
 ( 0.005258105385878691744, 0.005948373736081389272 ),
 .UNSPECIFIED. ) ;
#16054=ORIENTED_EDGE ( 'NONE', *, *, #19212, .F. ) ;
#16061=CARTESIAN_POINT ( 'NONE',  ( 0.8291131470075020493, -24.44424927289185590, 12.96989951879399072 ) ) ;
#16067=B_SPLINE_CURVE_WITH_KNOTS ( 'NONE', 3,
 ( #13371, #2561, #5567, #19373 ),
 .UNSPECIFIED., .F., .F.,
 ( 4, 4 ),
 ( 0.005258214619651953650, 0.005948481662034169060 ),
 .UNSPECIFIED. ) ;
#16068=CARTESIAN_POINT ( 'NONE',  ( 0.02436607992776064838, 5.391175441198615914, 24.15498966839965078 ) ) ;
#16069=B_SPLINE_CURVE_WITH_KNOTS ( 'NONE', 3,
 ( #10932, #7916, #14229, #3223, #15831, #3426 ),
 .UNSPECIFIED., .F., .F.,
 ( 4, 2, 4 ),
 ( 2.586195665736120714E-07, 0.001878649493629689022, 0.003757040367692804708 ),
 .UNSPECIFIED. ) ;
#16071=VERTEX_POINT ( 'NONE', #1257 ) ;
#16074=CYLINDRICAL_SURFACE ( 'NONE', #16602, 2.524999999999995914 ) ;
#16078=EDGE_LOOP ( 'NONE', ( #7135, #11024, #2805, #12138, #18895, #7542 ) ) ;
#16079=DIRECTION ( 'NONE',  ( 1.000000000000000000, 0.000000000000000000, 0.000000000000000000 ) ) ;
#16085=EDGE_CURVE ( 'NONE', #18433, #608, #311, .T. ) ;
#16086=AXIS2_PLACEMENT_3D ( 'NONE', #17862, #8955, #16466 ) ;
#16088=FACE_OUTER_BOUND ( 'NONE', #2909, .T. ) ;
#16090=VERTEX_POINT ( 'NONE', #4360 ) ;
#16097=CARTESIAN_POINT ( 'NONE',  ( 1.749999999999998002, -12.52377138324206030, -25.12109765559667096 ) ) ;
#16106=ORIENTED_EDGE ( 'NONE', *, *, #10806, .F. ) ;
#16110=EDGE_CURVE ( 'NONE', #18594, #2162, #14258, .T. ) ;
#16114=AXIS2_PLACEMENT_3D ( 'NONE', #8679, #14787, #11490 ) ;
#16125=DIRECTION ( 'NONE',  ( 0.000000000000000000, 0.000000000000000000, -1.000000000000000000 ) ) ;
#16126=LINE ( 'NONE', #11419, #769 ) ;
#16129=B_SPLINE_CURVE_WITH_KNOTS ( 'NONE', 3,
 ( #12242, #10639, #9239, #12043 ),
 .UNSPECIFIED., .F., .F.,
 ( 4, 4 ),
 ( 2.135345996700793610E-07, 0.0006888010880211471818 ),
 .UNSPECIFIED. ) ;
#16130=FACE_OUTER_BOUND ( 'NONE', #8220, .T. ) ;
#16132=DIRECTION ( 'NONE',  ( 1.000000000000000000, -0.000000000000000000, -0.000000000000000000 ) ) ;
#16137=CARTESIAN_POINT ( 'NONE',  ( 0.000000000000000000, -1.991882183130475603, 24.04302995059966719 ) ) ;
#16138=ADVANCED_FACE ( 'NONE', ( #7844 ), #17065, .T. ) ;
#16146=ORIENTED_EDGE ( 'NONE', *, *, #12769, .T. ) ;
#16150=DIRECTION ( 'NONE',  ( 0.000000000000000000, 0.000000000000000000, 1.000000000000000000 ) ) ;
#16152=ORIENTED_EDGE ( 'NONE', *, *, #858, .T. ) ;
#16153=CARTESIAN_POINT ( 'NONE',  ( 2.789999999999999147, 23.48180575137730131, 5.535312321042802353 ) ) ;
#16156=ORIENTED_EDGE ( 'NONE', *, *, #8918, .F. ) ;
#16157=LINE ( 'NONE', #13245, #3977 ) ;
#16162=DIRECTION ( 'NONE',  ( -1.000000000000000000, -0.000000000000000000, -0.000000000000000000 ) ) ;
#16163=ADVANCED_FACE ( 'NONE', ( #11055 ), #3545, .T. ) ;
#16168=DIRECTION ( 'NONE',  ( 0.000000000000000000, 0.000000000000000000, -1.000000000000000000 ) ) ;
#16170=B_SPLINE_CURVE_WITH_KNOTS ( 'NONE', 3,
 ( #4570, #8781, #8879, #13576 ),
 .UNSPECIFIED., .F., .F.,
 ( 4, 4 ),
 ( 3.059063720760159520E-07, 0.0006888942284914070097 ),
 .UNSPECIFIED. ) ;
#16176=ORIENTED_EDGE ( 'NONE', *, *, #14735, .F. ) ;
#16183=EDGE_CURVE ( 'NONE', #15059, #241, #5829, .T. ) ;
#16185=TOROIDAL_SURFACE ( 'NONE', #14901, 24.12539914357697413, 8.000000000000000000 ) ;
#16189=ORIENTED_EDGE ( 'NONE', *, *, #4441, .T. ) ;
#16193=VERTEX_POINT ( 'NONE', #1140 ) ;
#16197=LINE ( 'NONE', #19278, #6827 ) ;
#16199=CARTESIAN_POINT ( 'NONE',  ( -5.209999999999999964, 0.000000000000000000, 0.000000000000000000 ) ) ;
#16200=CARTESIAN_POINT ( 'NONE',  ( 2.789679245949062913, -20.70663861606260525, -12.51925356660783528 ) ) ;
#16209=VERTEX_POINT ( 'NONE', #17747 ) ;
#16216=DIRECTION ( 'NONE',  ( -1.000000000000000000, -0.000000000000000000, -0.000000000000000000 ) ) ;
#16221=CARTESIAN_POINT ( 'NONE',  ( 2.789999999999999147, 0.000000000000000000, 0.000000000000000000 ) ) ;
#16222=DIRECTION ( 'NONE',  ( -1.000000000000000000, -0.000000000000000000, -0.000000000000000000 ) ) ;
#16223=ORIENTED_EDGE ( 'NONE', *, *, #16355, .F. ) ;
#16224=CARTESIAN_POINT ( 'NONE',  ( 2.789999999999999147, 5.535312321042718864, 23.48180575137732262 ) ) ;
#16233=CIRCLE ( 'NONE', #17829, 24.12539914357697768 ) ;
#16234=ORIENTED_EDGE ( 'NONE', *, *, #3261, .F. ) ;
#16241=B_SPLINE_CURVE_WITH_KNOTS ( 'NONE', 3,
 ( #9528, #18816, #17028, #13925 ),
 .UNSPECIFIED., .F., .F.,
 ( 4, 4 ),
 ( 0.003263275852154340524, 0.003756984793530001795 ),
 .UNSPECIFIED. ) ;
#16245=DIRECTION ( 'NONE',  ( -1.000000000000000000, 0.000000000000000000, 0.000000000000000000 ) ) ;
#16255=ORIENTED_EDGE ( 'NONE', *, *, #2835, .F. ) ;
#16256=ADVANCED_FACE ( 'NONE', ( #11642 ), #5627, .F. ) ;
#16257=B_SPLINE_CURVE_WITH_KNOTS ( 'NONE', 3,
 ( #2484, #14899, #14704, #11896 ),
 .UNSPECIFIED., .F., .F.,
 ( 4, 4 ),
 ( 0.005258139959819239928, 0.005948405594583421920 ),
 .UNSPECIFIED. ) ;
#16262=ORIENTED_EDGE ( 'NONE', *, *, #15171, .F. ) ;
#16264=B_SPLINE_CURVE_WITH_KNOTS ( 'NONE', 3,
 ( #17313, #17511, #8410, #7171, #11413, #3800 ),
 .UNSPECIFIED., .F., .F.,
 ( 4, 2, 4 ),
 ( 4.462636731830560059E-07, 0.001879885066974964830, 0.003759323870276746679 ),
 .UNSPECIFIED. ) ;
#16270=B_SPLINE_CURVE_WITH_KNOTS ( 'NONE', 3,
 ( #398, #14008, #14203, #508 ),
 .UNSPECIFIED., .F., .F.,
 ( 4, 4 ),
 ( 1.981826382900813409E-07, 0.0006887856082032186092 ),
 .UNSPECIFIED. ) ;
#16274=CIRCLE ( 'NONE', #10208, 24.12539914357697768 ) ;
#16280=EDGE_LOOP ( 'NONE', ( #9772, #19550, #12834, #2310, #4826, #6652, #212, #9529 ) ) ;
#16283=ADVANCED_FACE ( 'NONE', ( #11546 ), #11491, .T. ) ;
#16295=DIRECTION ( 'NONE',  ( 0.000000000000000000, 0.000000000000000000, 1.000000000000000000 ) ) ;
#16305=VERTEX_POINT ( 'NONE', #4630 ) ;
#16318=CARTESIAN_POINT ( 'NONE',  ( 2.783025342027733995, 5.408388659524090869, 23.92335783895639523 ) ) ;
#16329=B_SPLINE_CURVE_WITH_KNOTS ( 'NONE', 3,
 ( #13407, #9012, #10614, #1412 ),
 .UNSPECIFIED., .F., .F.,
 ( 4, 4 ),
 ( 0.005258139959819238193, 0.005342776758202895035 ),
 .UNSPECIFIED. ) ;
#16333=ORIENTED_EDGE ( 'NONE', *, *, #19720, .F. ) ;
#16337=EDGE_CURVE ( 'NONE', #9696, #10889, #13736, .T. ) ;
#16342=ORIENTED_EDGE ( 'NONE', *, *, #9192, .T. ) ;
#16355=EDGE_CURVE ( 'NONE', #9831, #18489, #16129, .T. ) ;
#16359=CYLINDRICAL_SURFACE ( 'NONE', #12445, 28.06981291497571362 ) ;
#16360=AXIS2_PLACEMENT_3D ( 'NONE', #11231, #9846, #14233 ) ;
#16367=CIRCLE ( 'NONE', #14469, 24.12539914357697413 ) ;
#16368=EDGE_LOOP ( 'NONE', ( #7652, #12367, #19348, #7484, #18654, #13747 ) ) ;
#16370=CARTESIAN_POINT ( 'NONE',  ( 1.394999999999999574, 4.633866840648922292, 27.68468304288260384 ) ) ;
#16372=EDGE_CURVE ( 'NONE', #17740, #12265, #10550, .T. ) ;
#16376=VERTEX_POINT ( 'NONE', #16449 ) ;
#16379=CARTESIAN_POINT ( 'NONE',  ( 0.000000000000000000, -5.535312321042547445, -23.48180575137738302 ) ) ;
#16386=EDGE_CURVE ( 'NONE', #18676, #16477, #11345, .T. ) ;
#16387=CARTESIAN_POINT ( 'NONE',  ( 2.030753602223782206, -27.14986936243577986, 4.828194074574245320 ) ) ;
#16389=CARTESIAN_POINT ( 'NONE',  ( 1.039999999999996927, 4.633866840649313090, -27.68468304288253634 ) ) ;
#16390=FILL_AREA_STYLE_COLOUR ( '', #1667 ) ;
#16398=AXIS2_PLACEMENT_3D ( 'NONE', #14698, #19286, #5576 ) ;
#16403=CARTESIAN_POINT ( 'NONE',  ( 0.5279272304333941790, -24.43806413951667622, -11.57956866523244166 ) ) ;
#16409=B_SPLINE_CURVE_WITH_KNOTS ( 'NONE', 3,
 ( #8696, #2298, #17705, #812 ),
 .UNSPECIFIED., .F., .F.,
 ( 4, 4 ),
 ( 2.034713381942717623E-07, 0.0006887909409525219510 ),
 .UNSPECIFIED. ) ;
#16412=FACE_OUTER_BOUND ( 'NONE', #12363, .T. ) ;
#16417=ORIENTED_EDGE ( 'NONE', *, *, #11909, .F. ) ;
#16418=CARTESIAN_POINT ( 'NONE',  ( 0.7589665326895891351, 12.98167595241022276, 24.32849926382755257 ) ) ;
#16420=ORIENTED_EDGE ( 'NONE', *, *, #4774, .T. ) ;
#16425=PRODUCT_DEFINITION_SHAPE ( 'NONE', 'NONE',  #12983 ) ;
#16430=CARTESIAN_POINT ( 'NONE',  ( 2.765633920072239516, 16.37294372382858398, 18.55949924794898465 ) ) ;
#16433=EDGE_CURVE ( 'NONE', #7960, #16090, #15622, .T. ) ;
#16445=CARTESIAN_POINT ( 'NONE',  ( 0.1882239080259267838, -25.40949241676349146, -5.251266773802644394 ) ) ;
#16446=ORIENTED_EDGE ( 'NONE', *, *, #12271, .T. ) ;
#16449=CARTESIAN_POINT ( 'NONE',  ( 2.789999999999999147, 12.52067188844381107, -20.62201879784899461 ) ) ;
#16455=ORIENTED_EDGE ( 'NONE', *, *, #19594, .T. ) ;
#16457=CARTESIAN_POINT ( 'NONE',  ( 2.257825467309740208, -3.467596033028475855, 26.83036154824992892 ) ) ;
#16461=DIRECTION ( 'NONE',  ( -1.000000000000000000, -0.000000000000000000, -0.000000000000000000 ) ) ;
#16464=FACE_OUTER_BOUND ( 'NONE', #19680, .T. ) ;
#16466=DIRECTION ( 'NONE',  ( 0.000000000000000000, 0.000000000000000000, 1.000000000000000000 ) ) ;
#16468=CARTESIAN_POINT ( 'NONE',  ( 2.783068945535914995, 2.248820353272968919, 24.42321038836783131 ) ) ;
#16475=EDGE_CURVE ( 'NONE', #1013, #5836, #7012, .T. ) ;
#16477=VERTEX_POINT ( 'NONE', #8015 ) ;
#16481=AXIS2_PLACEMENT_3D ( 'NONE', #4367, #8666, #7550 ) ;
#16482=FACE_OUTER_BOUND ( 'NONE', #10563, .T. ) ;
#16484=DIRECTION ( 'NONE',  ( -1.000000000000000000, -0.000000000000000000, -0.000000000000000000 ) ) ;
#16486=CARTESIAN_POINT ( 'NONE',  ( 0.000000000000000000, 1.991882183130641248, -24.04302995059964942 ) ) ;
#16488=FACE_BOUND ( 'NONE', #2819, .T. ) ;
#16496=DIRECTION ( 'NONE',  ( 1.000000000000000000, 0.000000000000000000, 0.000000000000000000 ) ) ;
#16504=AXIS2_PLACEMENT_3D ( 'NONE', #1619, #17030, #15335 ) ;
#16507=CIRCLE ( 'NONE', #17149, 28.06981291497571007 ) ;
#16509=ADVANCED_FACE ( 'NONE', ( #17233 ), #10866, .T. ) ;
#16511=CARTESIAN_POINT ( 'NONE',  ( 2.789999999999999147, 21.30679549418631780, 12.59161484032919986 ) ) ;
#16523=B_SPLINE_CURVE_WITH_KNOTS ( 'NONE', 3,
 ( #10981, #367, #1872, #6069 ),
 .UNSPECIFIED., .F., .F.,
 ( 4, 4 ),
 ( 0.005258139959819248602, 0.005948405594583415848 ),
 .UNSPECIFIED. ) ;
#16527=ORIENTED_EDGE ( 'NONE', *, *, #12390, .T. ) ;
#16532=TOROIDAL_SURFACE ( 'NONE', #14610, 24.12539914357697413, 8.000000000000000000 ) ;
#16534=EDGE_CURVE ( 'NONE', #11113, #15383, #6529, .T. ) ;
#16536=EDGE_CURVE ( 'NONE', #18719, #19366, #5577, .T. ) ;
#16544=CARTESIAN_POINT ( 'NONE',  ( 0.07186813532171117125, -25.22589920183359169, -2.577209017047271011 ) ) ;
#16545=ORIENTED_EDGE ( 'NONE', *, *, #17194, .T. ) ;
#16549=LINE ( 'NONE', #19439, #6017 ) ;
#16555=CARTESIAN_POINT ( 'NONE',  ( 2.604434404052931473, -17.45907811351440841, -19.17825124759797006 ) ) ;
#16559=CARTESIAN_POINT ( 'NONE',  ( 0.02436607992776411782, -16.37294372382844543, -18.55949924794910544 ) ) ;
#16563=DIRECTION ( 'NONE',  ( -1.000000000000000000, -0.000000000000000000, -0.000000000000000000 ) ) ;
#16581=CARTESIAN_POINT ( 'NONE',  ( 0.1855657168891864939, -12.84444904262008436, -22.53097606932998787 ) ) ;
#16586=DIRECTION ( 'NONE',  ( 0.000000000000000000, 0.000000000000000000, 1.000000000000000000 ) ) ;
#16588=VERTEX_POINT ( 'NONE', #17821 ) ;
#16590=SURFACE_STYLE_USAGE ( .BOTH. , #10491 ) ;
#16591=VERTEX_POINT ( 'NONE', #16137 ) ;
#16602=AXIS2_PLACEMENT_3D ( 'NONE', #5644, #15970, #8756 ) ;
#16620=EDGE_CURVE ( 'NONE', #17188, #10783, #2495, .T. ) ;
#16623=CYLINDRICAL_SURFACE ( 'NONE', #11065, 28.06981291497571362 ) ;
#16624=ORIENTED_EDGE ( 'NONE', *, *, #16433, .T. ) ;
#16628=ORIENTED_EDGE ( 'NONE', *, *, #15668, .T. ) ;
#16633=FACE_OUTER_BOUND ( 'NONE', #11038, .T. ) ;
#16636=LINE ( 'NONE', #18046, #14711 ) ;
#16644=EDGE_CURVE ( 'NONE', #14651, #608, #16799, .T. ) ;
#16646=EDGE_LOOP ( 'NONE', ( #3502, #16651, #18444, #2583 ) ) ;
#16651=ORIENTED_EDGE ( 'NONE', *, *, #16013, .F. ) ;
#16655=ORIENTED_EDGE ( 'NONE', *, *, #2311, .F. ) ;
#16656=CARTESIAN_POINT ( 'NONE',  ( 1.039999999999997371, -4.147968289691092991, -27.76164181293055933 ) ) ;
#16658=CARTESIAN_POINT ( 'NONE',  ( 1.749999999999998002, -24.89775460606821866, -12.96210679857815684 ) ) ;
#16662=EDGE_LOOP ( 'NONE', ( #16809, #9418, #7615, #18784 ) ) ;
#16666=DIRECTION ( 'NONE',  ( -1.000000000000000000, -0.000000000000000000, 0.000000000000000000 ) ) ;
#16670=ORIENTED_EDGE ( 'NONE', *, *, #1981, .T. ) ;
#16676=VERTEX_POINT ( 'NONE', #7286 ) ;
#16679=ORIENTED_EDGE ( 'NONE', *, *, #11884, .T. ) ;
#16683=AXIS2_PLACEMENT_3D ( 'NONE', #12700, #14004, #17106 ) ;
#16684=CARTESIAN_POINT ( 'NONE',  ( 8.000000000000000000, 0.000000000000000000, 0.000000000000000000 ) ) ;
#16686=EDGE_CURVE ( 'NONE', #11813, #2358, #16329, .T. ) ;
#16687=ORIENTED_EDGE ( 'NONE', *, *, #18759, .F. ) ;
#16688=CARTESIAN_POINT ( 'NONE',  ( 0.7589665203264103210, -19.12621924769880977, 19.86422722021305631 ) ) ;
#16692=DIRECTION ( 'NONE',  ( 0.000000000000000000, 0.000000000000000000, 1.000000000000000000 ) ) ;
#16693=AXIS2_PLACEMENT_3D ( 'NONE', #17099, #194, #6667 ) ;
#16701=LINE ( 'NONE', #281, #15719 ) ;
#16702=CARTESIAN_POINT ( 'NONE',  ( 2.789999999999999147, -24.04302995059966719, 1.991882183130210482 ) ) ;
#16706=CARTESIAN_POINT ( 'NONE',  ( -7.700916879387133607E-14, 12.51293083811828843, -20.85287692521917080 ) ) ;
#16707=AXIS2_PLACEMENT_3D ( 'NONE', #18569, #10774, #9682 ) ;
#16709=CARTESIAN_POINT ( 'NONE',  ( 0.02436607992775978102, 2.336989772644613161, -24.63872515616080250 ) ) ;
#16710=CYLINDRICAL_SURFACE ( 'NONE', #2029, 2.524999999999995914 ) ;
#16713=DIRECTION ( 'NONE',  ( 0.000000000000000000, 0.000000000000000000, 1.000000000000000000 ) ) ;
#16714=FILL_AREA_STYLE_COLOUR ( '', #16735 ) ;
#16718=VERTEX_POINT ( 'NONE', #18315 ) ;
#16720=CARTESIAN_POINT ( 'NONE',  ( 2.718131914667133220, 10.24630254990516143, 23.19485392143217339 ) ) ;
#16724=AXIS2_PLACEMENT_3D ( 'NONE', #17428, #9833, #6230 ) ;
#16725=EDGE_CURVE ( 'NONE', #12283, #7096, #6051, .T. ) ;
#16729=CARTESIAN_POINT ( 'NONE',  ( 1.749999999999998002, 24.89775460606851354, -12.96210679857759729 ) ) ;
#16730=VERTEX_POINT ( 'NONE', #4609 ) ;
#16733=CARTESIAN_POINT ( 'NONE',  ( 1.749999999999998002, 27.76164181293051669, -4.147968289691384314 ) ) ;
#16734=VERTEX_POINT ( 'NONE', #18219 ) ;
#16735=COLOUR_RGB ( '', 0.66274510, 0.83137255, 0.94901961) ;
#16741=FACE_OUTER_BOUND ( 'NONE', #9071, .T. ) ;
#16743=CARTESIAN_POINT ( 'NONE',  ( 0.02436607992776498519, -21.30679549418621832, -12.59161484032935618 ) ) ;
#16748=CARTESIAN_POINT ( 'NONE',  ( 0.02436607992775544421, -22.71065055754445439, -9.836394144775947979 ) ) ;
#16750=CARTESIAN_POINT ( 'NONE',  ( 2.031033479673586939, 19.86422722021340093, -19.12621924769845805 ) ) ;
#16752=CARTESIAN_POINT ( 'NONE',  ( 1.039999999999997593, 0.000000000000000000, 0.000000000000000000 ) ) ;
#16761=B_SPLINE_CURVE_WITH_KNOTS ( 'NONE', 3,
 ( #9773, #11364, #6731, #18755, #2049, #8460, #13056, #16061 ),
 .UNSPECIFIED., .F., .F.,
 ( 4, 2, 2, 4 ),
 ( 2.032124546156068561E-07, 0.001631739532304432192, 0.002447507692229335726, 0.003263275852154239043 ),
 .UNSPECIFIED. ) ;
#16762=VECTOR ( 'NONE', #1274, 1000.000000000000000 ) ;
#16777=DIRECTION ( 'NONE',  ( -1.000000000000000000, -0.000000000000000000, -0.000000000000000000 ) ) ;
#16780=ORIENTED_EDGE ( 'NONE', *, *, #12443, .T. ) ;
#16789=CARTESIAN_POINT ( 'NONE',  ( 0.02436607992776368414, 18.55949924794916228, -16.37294372382838148 ) ) ;
#16791=ORIENTED_EDGE ( 'NONE', *, *, #9806, .T. ) ;
#16796=CARTESIAN_POINT ( 'NONE',  ( 2.604434261026090436, 5.253342437940084153, -25.39738473784996131 ) ) ;
#16797=CIRCLE ( 'NONE', #14234, 24.12539914357697768 ) ;
#16798=DIRECTION ( 'NONE',  ( -1.000000000000000000, -0.000000000000000000, 0.000000000000000000 ) ) ;
#16799=B_SPLINE_CURVE_WITH_KNOTS ( 'NONE', 3,
 ( #6999, #2503, #11715, #8226, #5319, #11432 ),
 .UNSPECIFIED., .F., .F.,
 ( 4, 2, 4 ),
 ( 2.586195665723156346E-07, 0.001878649493629684468, 0.003757040367692796902 ),
 .UNSPECIFIED. ) ;
#16801=DIRECTION ( 'NONE',  ( -1.000000000000000000, -0.000000000000000000, -0.000000000000000000 ) ) ;
#16802=EDGE_CURVE ( 'NONE', #3927, #18676, #204, .T. ) ;
#16809=ORIENTED_EDGE ( 'NONE', *, *, #11170, .F. ) ;
#16812=FACE_OUTER_BOUND ( 'NONE', #8280, .T. ) ;
#16813=TOROIDAL_SURFACE ( 'NONE', #17450, 24.12539914357697768, 8.000000000000000000 ) ;
#16816=CYLINDRICAL_SURFACE ( 'NONE', #3957, 2.524999999999995914 ) ;
#16819=( NAMED_UNIT ( * ) PLANE_ANGLE_UNIT ( ) SI_UNIT ( $, .RADIAN. ) );
#16821=DIRECTION ( 'NONE',  ( -1.000000000000000000, -0.000000000000000000, -0.000000000000000000 ) ) ;
#16833=CARTESIAN_POINT ( 'NONE',  ( 0.5279273381794625797, 26.82026385750178932, 3.461047254864356049 ) ) ;
#16836=CARTESIAN_POINT ( 'NONE',  ( 2.604434325169353581, 25.77772010606605946, -2.851997810081738027 ) ) ;
#16837=ORIENTED_EDGE ( 'NONE', *, *, #19677, .T. ) ;
#16838=AXIS2_PLACEMENT_3D ( 'NONE', #12087, #17789, #4085 ) ;
#16843=CYLINDRICAL_SURFACE ( 'NONE', #7015, 2.524999999999995914 ) ;
#16847=DIRECTION ( 'NONE',  ( -1.000000000000000000, -0.000000000000000000, 0.000000000000000000 ) ) ;
#16848=CARTESIAN_POINT ( 'NONE',  ( 2.765633920072235963, 22.71065055754452544, 9.836394144775786330 ) ) ;
#16851=CARTESIAN_POINT ( 'NONE',  ( 1.394999999999999574, -20.02152543075331081, -19.67366047555552555 ) ) ;
#16862=CARTESIAN_POINT ( 'NONE',  ( 2.790000000000077751, 24.22524813288762147, 2.133839912090885527 ) ) ;
#16863=VERTEX_POINT ( 'NONE', #5089 ) ;
#16868=CARTESIAN_POINT ( 'NONE',  ( 50.00050000000000239, 4.898587196589412829E-16, -4.000000000000000000 ) ) ;
#16871=EDGE_LOOP ( 'NONE', ( #5586, #15278, #1368, #2590 ) ) ;
#16874=DIRECTION ( 'NONE',  ( 1.000000000000000000, -0.000000000000000000, 0.000000000000000000 ) ) ;
#16876=ORIENTED_EDGE ( 'NONE', *, *, #9538, .T. ) ;
#16881=VECTOR ( 'NONE', #6197, 1000.000000000000000 ) ;
#16887=DIRECTION ( 'NONE',  ( -1.000000000000000000, -0.000000000000000000, -0.000000000000000000 ) ) ;
#16889=CARTESIAN_POINT ( 'NONE',  ( 2.789999999999999147, -7.909232158574647009, -21.81711360614308148 ) ) ;
#16890=ORIENTED_EDGE ( 'NONE', *, *, #19319, .T. ) ;
#16891=EDGE_CURVE ( 'NONE', #10624, #4466, #11203, .T. ) ;
#16896=CARTESIAN_POINT ( 'NONE',  ( 1.960886852992457241, 24.44424927289185945, 12.96989951879416125 ) ) ;
#16901=EDGE_CURVE ( 'NONE', #10556, #3868, #6781, .T. ) ;
#16902=CARTESIAN_POINT ( 'NONE',  ( 0.8291131470075020493, -24.44424927289185590, 12.96989951879399072 ) ) ;
#16909=CARTESIAN_POINT ( 'NONE',  ( 0.006974657972266581039, -23.92335783895634194, -5.408388659524344000 ) ) ;
#16913=DIRECTION ( 'NONE',  ( -1.000000000000000000, -0.000000000000000000, -0.000000000000000000 ) ) ;
#16923=CARTESIAN_POINT ( 'NONE',  ( 0.5279272304333949561, 11.57956866523252870, -24.43806413951663004 ) ) ;
#16928=DIRECTION ( 'NONE',  ( -1.000000000000000000, 0.000000000000000000, -0.000000000000000000 ) ) ;
#16930=ORIENTED_EDGE ( 'NONE', *, *, #2521, .T. ) ;
#16935=ORIENTED_EDGE ( 'NONE', *, *, #13962, .T. ) ;
#16937=ORIENTED_EDGE ( 'NONE', *, *, #7117, .T. ) ;
#16941=CARTESIAN_POINT ( 'NONE',  ( 0.000000000000000000, 20.70663861606272249, 15.04425356660767932 ) ) ;
#16944=VECTOR ( 'NONE', #1822, 1000.000000000000000 ) ;
#16945=DIRECTION ( 'NONE',  ( 0.000000000000000000, 0.000000000000000000, 1.000000000000000000 ) ) ;
#16950=CYLINDRICAL_SURFACE ( 'NONE', #13498, 13.20000000000000284 ) ;
#16956=CARTESIAN_POINT ( 'NONE',  ( 2.765633920072236851, -22.71065055754445439, -9.836394144775947979 ) ) ;
#16962=ORIENTED_EDGE ( 'NONE', *, *, #650, .F. ) ;
#16975=DIRECTION ( 'NONE',  ( 0.000000000000000000, 0.000000000000000000, 1.000000000000000000 ) ) ;
#16977=CIRCLE ( 'NONE', #17617, 28.06981291497571362 ) ;
#16983=APPLICATION_CONTEXT ( 'automotive_design' ) ;
#16985=DIRECTION ( 'NONE',  ( 0.000000000000000000, 0.000000000000000000, 1.000000000000000000 ) ) ;
#16991=FACE_OUTER_BOUND ( 'NONE', #16368, .T. ) ;
#16992=CARTESIAN_POINT ( 'NONE',  ( 2.430066721642811345, 23.15620303736532293, 12.90954937922509238 ) ) ;
#16995=ORIENTED_EDGE ( 'NONE', *, *, #7190, .T. ) ;
#17002=ADVANCED_FACE ( 'NONE', ( #11691 ), #10400, .F. ) ;
#17013=DIRECTION ( 'NONE',  ( 0.000000000000000000, 0.000000000000000000, 1.000000000000000000 ) ) ;
#17021=CARTESIAN_POINT ( 'NONE',  ( 2.783025325906566927, -2.249040938978666748, 24.42374957165204563 ) ) ;
#17028=CARTESIAN_POINT ( 'NONE',  ( 1.823865745262398308, 24.74813374239829145, 12.96725027898200899 ) ) ;
#17030=DIRECTION ( 'NONE',  ( 1.000000000000000000, 0.000000000000000000, 0.000000000000000000 ) ) ;
#17034=CARTESIAN_POINT ( 'NONE',  ( 2.789999999999999147, 15.04425356660790136, -20.70663861606255196 ) ) ;
#17055=LINE ( 'NONE', #8028, #6469 ) ;
#17056=VERTEX_POINT ( 'NONE', #18483 ) ;
#17060=ORIENTED_EDGE ( 'NONE', *, *, #17638, .F. ) ;
#17065=CYLINDRICAL_SURFACE ( 'NONE', #15003, 13.19999999999999929 ) ;
#17066=ORIENTED_EDGE ( 'NONE', *, *, #12990, .T. ) ;
#17069=CARTESIAN_POINT ( 'NONE',  ( 2.789999999999999147, 7.909232158575156824, -21.81711360614291806 ) ) ;
#17074=EDGE_CURVE ( 'NONE', #12346, #14758, #9389, .T. ) ;
#17082=DIRECTION ( 'NONE',  ( -1.000000000000000000, 0.000000000000000000, 0.000000000000000000 ) ) ;
#17086=CARTESIAN_POINT ( 'NONE',  ( -7.816002369513581784E-14, 15.96555658743763217, 18.34439787333512939 ) ) ;
#17089=LINE ( 'NONE', #5971, #11267 ) ;
#17092=ORIENTED_EDGE ( 'NONE', *, *, #7099, .F. ) ;
#17093=DIRECTION ( 'NONE',  ( -1.000000000000000000, -0.000000000000000000, -0.000000000000000000 ) ) ;
#17099=CARTESIAN_POINT ( 'NONE',  ( 2.789999999999999147, -14.18181402625728360, -19.91106274590529068 ) ) ;
#17106=DIRECTION ( 'NONE',  ( 0.000000000000000000, 0.000000000000000000, 1.000000000000000000 ) ) ;
#17110=CARTESIAN_POINT ( 'NONE',  ( 1.749999999999998002, 12.52377138324224148, 25.12109765559658570 ) ) ;
#17112=CARTESIAN_POINT ( 'NONE',  ( 4.424224194511527805E-17, 20.65025570340106853, -12.51972505884970488 ) ) ;
#17113=ADVANCED_FACE ( 'NONE', ( #16991 ), #18862, .T. ) ;
#17121=AXIS2_PLACEMENT_3D ( 'NONE', #12539, #13739, #12344 ) ;
#17124=AXIS2_PLACEMENT_3D ( 'NONE', #8330, #18838, #15277 ) ;
#17127=ORIENTED_EDGE ( 'NONE', *, *, #19594, .F. ) ;
#17128=CARTESIAN_POINT ( 'NONE',  ( -7.928732286808572430E-16, 18.34424029220111052, 15.96500990068130577 ) ) ;
#17130=VERTEX_POINT ( 'NONE', #3076 ) ;
#17131=DIRECTION ( 'NONE',  ( -1.000000000000000000, 0.000000000000000000, 0.000000000000000000 ) ) ;
#17132=EDGE_LOOP ( 'NONE', ( #18058, #5456, #9580, #13393 ) ) ;
#17134=VERTEX_POINT ( 'NONE', #1875 ) ;
#17137=CARTESIAN_POINT ( 'NONE',  ( 0.07181525480391388883, 12.74223776959231991, -21.92234060054331479 ) ) ;
#17140=CARTESIAN_POINT ( 'NONE',  ( 8.000000000000000000, 0.000000000000000000, 0.000000000000000000 ) ) ;
#17149=AXIS2_PLACEMENT_3D ( 'NONE', #1881, #12591, #12688 ) ;
#17155=EDGE_LOOP ( 'NONE', ( #3243, #6729, #2855, #12717 ) ) ;
#17162=B_SPLINE_CURVE_WITH_KNOTS ( 'NONE', 3,
 ( #9917, #12616, #9721, #15809 ),
 .UNSPECIFIED., .F., .F.,
 ( 4, 4 ),
 ( 1.981826382900847290E-07, 0.0006887856082032348722 ),
 .UNSPECIFIED. ) ;
#17165=VERTEX_POINT ( 'NONE', #13689 ) ;
#17166=CARTESIAN_POINT ( 'NONE',  ( -5.209999999999999964, 0.000000000000000000, 0.000000000000000000 ) ) ;
#17167=CIRCLE ( 'NONE', #8533, 28.06981291497571362 ) ;
#17168=DIRECTION ( 'NONE',  ( -1.000000000000000000, -0.000000000000000000, -0.000000000000000000 ) ) ;
#17169=EDGE_CURVE ( 'NONE', #4945, #3153, #2220, .T. ) ;
#17171=ORIENTED_EDGE ( 'NONE', *, *, #7731, .F. ) ;
#17173=ORIENTED_EDGE ( 'NONE', *, *, #1128, .F. ) ;
#17177=CARTESIAN_POINT ( 'NONE',  ( 1.039999999999996927, -4.633866840649124796, 27.68468304288256832 ) ) ;
#17182=ORIENTED_EDGE ( 'NONE', *, *, #7903, .F. ) ;
#17183=CARTESIAN_POINT ( 'NONE',  ( 2.765633920072235075, -12.59161484032896361, -21.30679549418645280 ) ) ;
#17187=AXIS2_PLACEMENT_3D ( 'NONE', #2099, #15517, #8101 ) ;
#17188=VERTEX_POINT ( 'NONE', #16656 ) ;
#17192=CARTESIAN_POINT ( 'NONE',  ( 0.02436607992776064838, 12.59161484032912171, 21.30679549418635688 ) ) ;
#17193=CARTESIAN_POINT ( 'NONE',  ( 0.07181524296601550506, -18.89296398180203695, 16.91181672897726784 ) ) ;
#17194=EDGE_CURVE ( 'NONE', #12265, #11483, #19490, .T. ) ;
#17196=DIRECTION ( 'NONE',  ( 0.000000000000000000, 0.000000000000000000, 1.000000000000000000 ) ) ;
#17208=EDGE_CURVE ( 'NONE', #6715, #2313, #13653, .T. ) ;
#17221=CARTESIAN_POINT ( 'NONE',  ( 2.262072706628479146, -19.66369668717046437, 18.56460150496932116 ) ) ;
#17226=DIRECTION ( 'NONE',  ( 0.000000000000000000, 1.374038396813314559E-15, -1.000000000000000000 ) ) ;
#17227=VERTEX_POINT ( 'NONE', #7637 ) ;
#17228=DIRECTION ( 'NONE',  ( 0.000000000000000000, 0.000000000000000000, 1.000000000000000000 ) ) ;
#17233=FACE_OUTER_BOUND ( 'NONE', #12662, .T. ) ;
#17236=CARTESIAN_POINT ( 'NONE',  ( 0.07186811453410689443, 18.89333555428554590, 16.91241718342006450 ) ) ;
#17249=ORIENTED_EDGE ( 'NONE', *, *, #5797, .F. ) ;
#17254=DIRECTION ( 'NONE',  ( 0.000000000000000000, 0.000000000000000000, 1.000000000000000000 ) ) ;
#17256=ORIENTED_EDGE ( 'NONE', *, *, #5523, .F. ) ;
#17259=DIRECTION ( 'NONE',  ( 0.000000000000000000, -0.3090169943749486170, 0.9510565162951530871 ) ) ;
#17260=B_SPLINE_CURVE_WITH_KNOTS ( 'NONE', 3,
 ( #8692, #3996, #14517, #19290, #12908, #13009 ),
 .UNSPECIFIED., .F., .F.,
 ( 4, 2, 4 ),
 ( 4.462636882221863355E-07, 0.001879885203074805429, 0.003759324142461388692 ),
 .UNSPECIFIED. ) ;
#17262=ORIENTED_EDGE ( 'NONE', *, *, #9855, .T. ) ;
#17273=CARTESIAN_POINT ( 'NONE',  ( 0.02436607992775934733, -2.336989772644440855, 24.63872515616082026 ) ) ;
#17277=ADVANCED_FACE ( 'NONE', ( #13445, #12157 ), #14860, .F. ) ;
#17278=ORIENTED_EDGE ( 'NONE', *, *, #19688, .T. ) ;
#17279=ORIENTED_EDGE ( 'NONE', *, *, #9049, .F. ) ;
#17280=ADVANCED_FACE ( 'NONE', ( #1155 ), #11208, .T. ) ;
#17292=ADVANCED_FACE ( 'NONE', ( #16464 ), #1248, .T. ) ;
#17298=CARTESIAN_POINT ( 'NONE',  ( 2.789999999999999147, 18.28042085475278355, 15.74360496233388140 ) ) ;
#17300=CARTESIAN_POINT ( 'NONE',  ( 0.02436607992776368414, -9.836394144775550075, -22.71065055754462492 ) ) ;
#17304=TOROIDAL_SURFACE ( 'NONE', #17954, 24.12539914357697413, 8.000000000000000000 ) ;
#17313=CARTESIAN_POINT ( 'NONE',  ( 1.039999999999996705, 27.76164181293051669, -4.147968289691385202 ) ) ;
#17318=ADVANCED_FACE ( 'NONE', ( #1450 ), #12817, .T. ) ;
#17326=VERTEX_POINT ( 'NONE', #11511 ) ;
#17333=CARTESIAN_POINT ( 'NONE',  ( 0.7592463965288815952, 12.98165646470117274, -24.32906614999601302 ) ) ;
#17334=CARTESIAN_POINT ( 'NONE',  ( 1.749999999999998002, 19.67366047555558950, -20.02152543075324687 ) ) ;
#17336=DIRECTION ( 'NONE',  ( 0.000000000000000000, -0.9510565162951544194, 0.3090169943749446757 ) ) ;
#17340=FACE_OUTER_BOUND ( 'NONE', #17132, .T. ) ;
#17354=ORIENTED_EDGE ( 'NONE', *, *, #9460, .F. ) ;
#17358=DIRECTION ( 'NONE',  ( -1.000000000000000000, 0.000000000000000000, 0.000000000000000000 ) ) ;
#17360=VERTEX_POINT ( 'NONE', #11605 ) ;
#17364=DIRECTION ( 'NONE',  ( -1.000000000000000000, 0.000000000000000000, -0.000000000000000000 ) ) ;
#17370=EDGE_CURVE ( 'NONE', #11363, #15591, #18001, .T. ) ;
#17372=B_SPLINE_CURVE_WITH_KNOTS ( 'NONE', 3,
 ( #1187, #13099, #11891, #1287 ),
 .UNSPECIFIED., .F., .F.,
 ( 4, 4 ),
 ( 3.059063720746937335E-07, 0.0006888942284914199117 ),
 .UNSPECIFIED. ) ;
#17375=CARTESIAN_POINT ( 'NONE',  ( 1.749999999999998002, -12.96210679857804671, 24.89775460606827551 ) ) ;
#17377=CARTESIAN_POINT ( 'NONE',  ( 0.7592463965288811512, -24.32906614999605921, -12.98165646470108925 ) ) ;
#17391=ORIENTED_EDGE ( 'NONE', *, *, #2228, .T. ) ;
#17392=LINE ( 'NONE', #11389, #6855 ) ;
#17395=CARTESIAN_POINT ( 'NONE',  ( -10.00000000000000000, 0.000000000000000000, 0.000000000000000000 ) ) ;
#17398=CARTESIAN_POINT ( 'NONE',  ( 2.783068930044319433, 18.43696893154781691, -16.17493693894858353 ) ) ;
#17400=DIRECTION ( 'NONE',  ( 0.000000000000000000, 5.496153587253259026E-15, -1.000000000000000000 ) ) ;
#17402=CARTESIAN_POINT ( 'NONE',  ( 1.039999999999997593, 0.000000000000000000, 0.000000000000000000 ) ) ;
#17412=DIRECTION ( 'NONE',  ( -1.000000000000000000, 0.000000000000000000, -0.000000000000000000 ) ) ;
#17414=EDGE_CURVE ( 'NONE', #3340, #19072, #1521, .T. ) ;
#17422=CARTESIAN_POINT ( 'NONE',  ( 0.02436607992776455150, 5.391175441198956086, -24.15498966839956907 ) ) ;
#17425=CARTESIAN_POINT ( 'NONE',  ( 2.790000000000077307, 22.38018801136476554, 9.515416771311276278 ) ) ;
#17428=CARTESIAN_POINT ( 'NONE',  ( 0.000000000000000000, 0.000000000000000000, 0.000000000000000000 ) ) ;
#17434=VERTEX_POINT ( 'NONE', #11416 ) ;
#17443=B_SPLINE_CURVE_WITH_KNOTS ( 'NONE', 3,
 ( #5116, #17333, #630, #3623, #17137, #8227 ),
 .UNSPECIFIED., .F., .F.,
 ( 4, 2, 4 ),
 ( 4.462636695653741059E-07, 0.001879885036799761131, 0.003759323809929956614 ),
 .UNSPECIFIED. ) ;
#17444=LINE ( 'NONE', #3529, #5289 ) ;
#17445=ORIENTED_EDGE ( 'NONE', *, *, #11969, .F. ) ;
#17447=DIRECTION ( 'NONE',  ( 0.000000000000000000, 0.000000000000000000, 1.000000000000000000 ) ) ;
#17449=EDGE_LOOP ( 'NONE', ( #18157, #6699, #14432, #6675 ) ) ;
#17450=AXIS2_PLACEMENT_3D ( 'NONE', #7226, #7327, #10461 ) ;
#17455=VERTEX_POINT ( 'NONE', #3805 ) ;
#17456=FACE_OUTER_BOUND ( 'NONE', #2323, .T. ) ;
#17460=CARTESIAN_POINT ( 'NONE',  ( 2.718184767880468922, -23.19431517146925970, -10.24584646439563507 ) ) ;
#17462=EDGE_LOOP ( 'NONE', ( #17703, #403, #13742, #6651 ) ) ;
#17468=CIRCLE ( 'NONE', #1807, 24.12539914357697768 ) ;
#17470=FACE_OUTER_BOUND ( 'NONE', #1365, .T. ) ;
#17490=AXIS2_PLACEMENT_3D ( 'NONE', #17562, #11554, #16168 ) ;
#17493=CARTESIAN_POINT ( 'NONE',  ( 0.0003207540509378258692, 20.70663861606293921, -12.51925356660738053 ) ) ;
#17494=EDGE_CURVE ( 'NONE', #4466, #15252, #10552, .T. ) ;
#17498=DIRECTION ( 'NONE',  ( 0.000000000000000000, -0.5877852522924743583, 0.8090169943749465631 ) ) ;
#17507=ADVANCED_FACE ( 'NONE', ( #16812 ), #9293, .T. ) ;
#17508=FACE_OUTER_BOUND ( 'NONE', #3021, .T. ) ;
#17509=VERTEX_POINT ( 'NONE', #5888 ) ;
#17511=CARTESIAN_POINT ( 'NONE',  ( 0.7592463941534238758, 27.31305418910209681, -3.797885586973310801 ) ) ;
#17513=CARTESIAN_POINT ( 'NONE',  ( 4.098876516494237640E-16, -15.96500990068138570, 18.34424029220106078 ) ) ;
#17516=CIRCLE ( 'NONE', #7586, 4.000000000000000000 ) ;
#17524=CARTESIAN_POINT ( 'NONE',  ( 1.749999999999998002, -20.02152543075331081, -19.67366047555553266 ) ) ;
#17526=EDGE_LOOP ( 'NONE', ( #9290, #6306, #1304, #16937, #10666, #8299 ) ) ;
#17530=EDGE_LOOP ( 'NONE', ( #6134, #15185, #10677, #18077, #6198, #280 ) ) ;
#17541=EDGE_CURVE ( 'NONE', #16734, #10744, #8335, .T. ) ;
#17548=VERTEX_POINT ( 'NONE', #13899 ) ;
#17553=CARTESIAN_POINT ( 'NONE',  ( 0.7589665203264078785, 19.12621924769895898, -19.86422722021291776 ) ) ;
#17562=CARTESIAN_POINT ( 'NONE',  ( 0.000000000000000000, 7.909232158574813099, 24.34211360614303388 ) ) ;
#17565=EDGE_CURVE ( 'NONE', #1584, #3868, #9596, .T. ) ;
#17567=ORIENTED_EDGE ( 'NONE', *, *, #1008, .F. ) ;
#17575=ORIENTED_EDGE ( 'NONE', *, *, #18026, .F. ) ;
#17576=ORIENTED_EDGE ( 'NONE', *, *, #4647, .F. ) ;
#17579=EDGE_CURVE ( 'NONE', #2052, #941, #1618, .T. ) ;
#17580=DIRECTION ( 'NONE',  ( 0.000000000000000000, 1.000000000000000000, 1.099230717450651647E-14 ) ) ;
#17586=DIRECTION ( 'NONE',  ( -1.000000000000000000, -0.000000000000000000, -0.000000000000000000 ) ) ;
#17587=CIRCLE ( 'NONE', #4809, 2.524999999999994582 ) ;
#17591=CARTESIAN_POINT ( 'NONE',  ( 2.257825459230520693, -26.58873630738055738, 4.993157874727710777 ) ) ;
#17592=B_SPLINE_CURVE_WITH_KNOTS ( 'NONE', 3,
 ( #1057, #13447, #13655, #10266, #4256, #16658 ),
 .UNSPECIFIED., .F., .F.,
 ( 4, 2, 4 ),
 ( 2.032124546189621919E-07, 0.001878594002992306630, 0.003756984793529993989 ),
 .UNSPECIFIED. ) ;
#17594=CARTESIAN_POINT ( 'NONE',  ( 2.789999999999999147, 24.44424927289185945, -0.2301004812058395077 ) ) ;
#17596=EDGE_LOOP ( 'NONE', ( #15398, #8484, #850, #15088 ) ) ;
#17603=AXIS2_PLACEMENT_3D ( 'NONE', #13350, #16563, #4543 ) ;
#17608=EDGE_CURVE ( 'NONE', #19636, #18433, #12303, .T. ) ;
#17614=CARTESIAN_POINT ( 'NONE',  ( 0.02436607992776455150, -22.71065055754459650, 9.836394144775621129 ) ) ;
#17617=AXIS2_PLACEMENT_3D ( 'NONE', #2229, #4943, #11349 ) ;
#17621=CARTESIAN_POINT ( 'NONE',  ( 1.394999999999998685, 25.12109765559653596, 12.52377138324232675 ) ) ;
#17631=ORIENTED_EDGE ( 'NONE', *, *, #15532, .T. ) ;
#17638=EDGE_CURVE ( 'NONE', #13278, #2736, #991, .T. ) ;
#17659=ORIENTED_EDGE ( 'NONE', *, *, #4623, .T. ) ;
#17664=AXIS2_PLACEMENT_3D ( 'NONE', #12377, #12578, #7763 ) ;
#17682=DIRECTION ( 'NONE',  ( 1.000000000000000000, 0.000000000000000000, -0.000000000000000000 ) ) ;
#17683=B_SPLINE_CURVE_WITH_KNOTS ( 'NONE', 3,
 ( #6752, #10172, #3663, #9788 ),
 .UNSPECIFIED., .F., .F.,
 ( 4, 4 ),
 ( 0.003263275852154239043, 0.003756984793529996591 ),
 .UNSPECIFIED. ) ;
#17685=EDGE_LOOP ( 'NONE', ( #17781, #4319, #15158, #1687, #15722, #4406 ) ) ;
#17687=LINE ( 'NONE', #14690, #1663 ) ;
#17703=ORIENTED_EDGE ( 'NONE', *, *, #4345, .F. ) ;
#17705=CARTESIAN_POINT ( 'NONE',  ( 2.790000000000077751, 12.51293083811798645, 20.85287692521934488 ) ) ;
#17706=ORIENTED_EDGE ( 'NONE', *, *, #5459, .F. ) ;
#17707=B_SPLINE_CURVE_WITH_KNOTS ( 'NONE', 3,
 ( #6323, #7634, #12447, #3736, #2134, #9549 ),
 .UNSPECIFIED., .F., .F.,
 ( 4, 2, 4 ),
 ( 4.462636732872785396E-07, 0.001879885066975069564, 0.003759323870276851630 ),
 .UNSPECIFIED. ) ;
#17711=DIRECTION ( 'NONE',  ( 0.000000000000000000, 0.000000000000000000, 1.000000000000000000 ) ) ;
#17714=AXIS2_PLACEMENT_3D ( 'NONE', #5550, #7136, #17765 ) ;
#17722=CARTESIAN_POINT ( 'NONE',  ( 0.7592463941534229876, -3.797885586973023475, -27.31305418910213234 ) ) ;
#17724=B_SPLINE_CURVE_WITH_KNOTS ( 'NONE', 3,
 ( #9387, #15292, #18384, #4973 ),
 .UNSPECIFIED., .F., .F.,
 ( 4, 4 ),
 ( 0.005258139959819237326, 0.005948405594583419317 ),
 .UNSPECIFIED. ) ;
#17729=ORIENTED_EDGE ( 'NONE', *, *, #4351, .F. ) ;
#17733=ORIENTED_EDGE ( 'NONE', *, *, #8123, .T. ) ;
#17734=CARTESIAN_POINT ( 'NONE',  ( 2.789999999999999147, 23.17675759782029843, 7.772527002114834715 ) ) ;
#17735=DIRECTION ( 'NONE',  ( 0.000000000000000000, 0.000000000000000000, 1.000000000000000000 ) ) ;
#17740=VERTEX_POINT ( 'NONE', #5174 ) ;
#17746=AXIS2_PLACEMENT_3D ( 'NONE', #1570, #4279, #1379 ) ;
#17747=CARTESIAN_POINT ( 'NONE',  ( 1.039999999999995817, -27.76164181293048472, -4.147968289691575272 ) ) ;
#17756=CARTESIAN_POINT ( 'NONE',  ( 1.749999999999998002, -4.147968289691484678, 27.76164181293050603 ) ) ;
#17760=B_SPLINE_CURVE_WITH_KNOTS ( 'NONE', 3,
 ( #15480, #12379, #18571, #10873, #15875, #17375 ),
 .UNSPECIFIED., .F., .F.,
 ( 4, 2, 4 ),
 ( 2.032124546189621919E-07, 0.001878594002992309232, 0.003756984793529999193 ),
 .UNSPECIFIED. ) ;
#17761=EDGE_CURVE ( 'NONE', #14183, #16193, #7049, .T. ) ;
#17765=DIRECTION ( 'NONE',  ( 0.000000000000000000, 0.000000000000000000, 1.000000000000000000 ) ) ;
#17773=LINE ( 'NONE', #4067, #14304 ) ;
#17776=ADVANCED_FACE ( 'NONE', ( #4251 ), #592, .T. ) ;
#17781=ORIENTED_EDGE ( 'NONE', *, *, #17414, .F. ) ;
#17787=DIRECTION ( 'NONE',  ( -1.000000000000000000, 0.000000000000000000, 0.000000000000000000 ) ) ;
#17789=DIRECTION ( 'NONE',  ( -1.000000000000000000, -0.000000000000000000, -0.000000000000000000 ) ) ;
#17791=DIRECTION ( 'NONE',  ( -1.000000000000000000, 0.000000000000000000, 0.000000000000000000 ) ) ;
#17792=ORIENTED_EDGE ( 'NONE', *, *, #15745, .F. ) ;
#17793=DIRECTION ( 'NONE',  ( -1.000000000000000000, -0.000000000000000000, -0.000000000000000000 ) ) ;
#17801=AXIS2_PLACEMENT_3D ( 'NONE', #10689, #16798, #1483 ) ;
#17808=CARTESIAN_POINT ( 'NONE',  ( 2.718184743034449014, 5.344212458769360907, 24.78695292654923676 ) ) ;
#17810=DIRECTION ( 'NONE',  ( -1.000000000000000000, -0.000000000000000000, -0.000000000000000000 ) ) ;
#17812=CIRCLE ( 'NONE', #11102, 2.524999999999995914 ) ;
#17819=CARTESIAN_POINT ( 'NONE',  ( 2.765633920072234631, 5.391175441198615914, 24.15498966839965078 ) ) ;
#17821=CARTESIAN_POINT ( 'NONE',  ( 0.0003207540509381473352, -20.70663861606275447, -12.51925356660783528 ) ) ;
#17826=VERTEX_POINT ( 'NONE', #16559 ) ;
#17829=AXIS2_PLACEMENT_3D ( 'NONE', #7359, #17998, #16692 ) ;
#17837=EDGE_CURVE ( 'NONE', #18641, #1940, #6105, .T. ) ;
#17839=CARTESIAN_POINT ( 'NONE',  ( 2.790000000000077307, 23.69897269326684963, -5.456611084821608948 ) ) ;
#17841=AXIS2_PLACEMENT_3D ( 'NONE', #76, #19776, #15584 ) ;
#17848=CARTESIAN_POINT ( 'NONE',  ( 2.789999999999999147, -24.04302995059964587, -1.991882183130548878 ) ) ;
#17851=CARTESIAN_POINT ( 'NONE',  ( 0.07186815222487989707, 5.344160105508701797, 24.78765742476140943 ) ) ;
#17854=AXIS2_PLACEMENT_3D ( 'NONE', #1758, #16777, #13865 ) ;
#17861=B_SPLINE_CURVE_WITH_KNOTS ( 'NONE', 3,
 ( #2604, #13513, #4409, #8715, #15019, #19616 ),
 .UNSPECIFIED., .F., .F.,
 ( 4, 2, 4 ),
 ( 1.979325885420663221E-07, 0.001878588715165609505, 0.003756979497742676637 ),
 .UNSPECIFIED. ) ;
#17862=CARTESIAN_POINT ( 'NONE',  ( -5.209999999999999964, 0.000000000000000000, 0.000000000000000000 ) ) ;
#17864=CYLINDRICAL_SURFACE ( 'NONE', #17714, 28.06981291497571362 ) ;
#17869=CARTESIAN_POINT ( 'NONE',  ( 1.039999999999996705, -19.67366047555515252, -20.02152543075367319 ) ) ;
#17872=EDGE_LOOP ( 'NONE', ( #16262, #7846, #14175, #11898, #5139, #14044 ) ) ;
#17877=CARTESIAN_POINT ( 'NONE',  ( 2.789999999999999147, 24.15498966839963302, 5.391175441198700291 ) ) ;
#17880=CARTESIAN_POINT ( 'NONE',  ( 0.000000000000000000, 0.000000000000000000, 0.000000000000000000 ) ) ;
#17886=VECTOR ( 'NONE', #16847, 1000.000000000000000 ) ;
#17890=LINE ( 'NONE', #13193, #10944 ) ;
#17891=ORIENTED_EDGE ( 'NONE', *, *, #11417, .T. ) ;
#17894=DIRECTION ( 'NONE',  ( -1.000000000000000000, -0.000000000000000000, 0.000000000000000000 ) ) ;
#17895=EDGE_CURVE ( 'NONE', #13659, #18587, #58, .T. ) ;
#17898=EDGE_LOOP ( 'NONE', ( #2018, #11669, #17092, #12530, #1157, #729 ) ) ;
#17908=CARTESIAN_POINT ( 'NONE',  ( 0.02436607992776758727, 24.15498966839963302, 5.391175441198700291 ) ) ;
#17916=CYLINDRICAL_SURFACE ( 'NONE', #5031, 28.06981291497571362 ) ;
#17921=DIRECTION ( 'NONE',  ( -1.000000000000000000, -0.000000000000000000, -0.000000000000000000 ) ) ;
#17926=ORIENTED_EDGE ( 'NONE', *, *, #9817, .T. ) ;
#17930=B_SPLINE_CURVE_WITH_KNOTS ( 'NONE', 3,
 ( #16729, #18128, #9, #10525, #15123, #9122 ),
 .UNSPECIFIED., .F., .F.,
 ( 4, 2, 4 ),
 ( 4.462636695653044375E-07, 0.001879885036799765685, 0.003759323809929966155 ),
 .UNSPECIFIED. ) ;
#17932=EDGE_CURVE ( 'NONE', #18641, #5854, #15377, .T. ) ;
#17951=VECTOR ( 'NONE', #12098, 1000.000000000000000 ) ;
#17954=AXIS2_PLACEMENT_3D ( 'NONE', #12958, #8548, #6833 ) ;
#17955=EDGE_CURVE ( 'NONE', #15001, #5363, #11753, .T. ) ;
#17956=CYLINDRICAL_SURFACE ( 'NONE', #8789, 4.000000000000000000 ) ;
#17957=B_SPLINE_CURVE_WITH_KNOTS ( 'NONE', 3,
 ( #8994, #7367, #14804, #994 ),
 .UNSPECIFIED., .F., .F.,
 ( 4, 4 ),
 ( 2.324263106244728226E-07, 0.0006888201370294799210 ),
 .UNSPECIFIED. ) ;
#17959=B_SPLINE_CURVE_WITH_KNOTS ( 'NONE', 3,
 ( #3751, #18856, #9874, #14158 ),
 .UNSPECIFIED., .F., .F.,
 ( 4, 4 ),
 ( 0.005258214619651938905, 0.005948481662034165590 ),
 .UNSPECIFIED. ) ;
#17973=EDGE_LOOP ( 'NONE', ( #10146, #2032, #10309, #17576, #18403, #16223 ) ) ;
#17976=DIRECTION ( 'NONE',  ( -1.000000000000000000, -0.000000000000000000, -0.000000000000000000 ) ) ;
#17978=ORIENTED_EDGE ( 'NONE', *, *, #2710, .T. ) ;
#17983=EDGE_CURVE ( 'NONE', #4324, #9831, #17707, .T. ) ;
#17987=DIRECTION ( 'NONE',  ( 0.000000000000000000, 0.000000000000000000, 1.000000000000000000 ) ) ;
#17990=CARTESIAN_POINT ( 'NONE',  ( 2.789999999999999147, 0.000000000000000000, 0.000000000000000000 ) ) ;
#17992=CARTESIAN_POINT ( 'NONE',  ( 2.789679245949058917, 20.70663861606308487, -12.51925356660738053 ) ) ;
#17998=DIRECTION ( 'NONE',  ( -1.000000000000000000, -0.000000000000000000, -0.000000000000000000 ) ) ;
#18001=B_SPLINE_CURVE_WITH_KNOTS ( 'NONE', 3,
 ( #19298, #2585, #9928, #14619, #11323, #17422 ),
 .UNSPECIFIED., .F., .F.,
 ( 4, 2, 4 ),
 ( 4.462636678151279571E-07, 0.001879885020955181143, 0.003759323778242547407 ),
 .UNSPECIFIED. ) ;
#18007=DIRECTION ( 'NONE',  ( -1.000000000000000000, -0.000000000000000000, 0.000000000000000000 ) ) ;
#18008=EDGE_CURVE ( 'NONE', #12785, #2162, #16977, .T. ) ;
#18009=CARTESIAN_POINT ( 'NONE',  ( 2.789999999999999147, 24.34211360614310848, -7.909232158574561744 ) ) ;
#18013=DIRECTION ( 'NONE',  ( -1.000000000000000000, -0.000000000000000000, -0.000000000000000000 ) ) ;
#18014=VECTOR ( 'NONE', #6989, 1000.000000000000000 ) ;
#18016=CARTESIAN_POINT ( 'NONE',  ( 1.749999999999998002, 0.000000000000000000, 0.000000000000000000 ) ) ;
#18023=VERTEX_POINT ( 'NONE', #3342 ) ;
#18024=CARTESIAN_POINT ( 'NONE',  ( 1.749999999999998002, 24.89775460606832524, 12.96210679857795256 ) ) ;
#18025=ORIENTED_EDGE ( 'NONE', *, *, #4691, .F. ) ;
#18026=EDGE_CURVE ( 'NONE', #15829, #11710, #8337, .T. ) ;
#18037=EDGE_LOOP ( 'NONE', ( #4308, #11759, #6376, #4737, #11659, #18955, #8471, #17256 ) ) ;
#18046=CARTESIAN_POINT ( 'NONE',  ( 2.789999999999999147, -24.15498966839966855, 5.391175441198523544 ) ) ;
#18048=CARTESIAN_POINT ( 'NONE',  ( 2.718184757033982990, 18.89296398180191616, 16.91181672897740640 ) ) ;
#18058=ORIENTED_EDGE ( 'NONE', *, *, #14554, .T. ) ;
#18062=DIRECTION ( 'NONE',  ( -1.000000000000000000, -0.000000000000000000, -0.000000000000000000 ) ) ;
#18077=ORIENTED_EDGE ( 'NONE', *, *, #9623, .F. ) ;
#18079=LINE ( 'NONE', #17877, #18912 ) ;
#18088=CARTESIAN_POINT ( 'NONE',  ( 2.789895104907798906, 20.67847077765723185, -12.51925356660737876 ) ) ;
#18094=CARTESIAN_POINT ( 'NONE',  ( 1.394999999999999574, 4.633866840649313090, -27.68468304288253989 ) ) ;
#18102=VERTEX_POINT ( 'NONE', #3534 ) ;
#18104=CIRCLE ( 'NONE', #9169, 2.524999999999996803 ) ;
#18105=ADVANCED_FACE ( 'NONE', ( #7930 ), #6717, .F. ) ;
#18109=DIRECTION ( 'NONE',  ( -1.000000000000000000, 0.000000000000000000, -0.000000000000000000 ) ) ;
#18118=VECTOR ( 'NONE', #2868, 1000.000000000000000 ) ;
#18128=CARTESIAN_POINT ( 'NONE',  ( 2.030753603471114221, 24.32906614999634698, -12.98165646470055634 ) ) ;
#18137=CARTESIAN_POINT ( 'NONE',  ( 1.749999999999998002, 19.67366047555558950, -20.02152543075324687 ) ) ;
#18139=ORIENTED_EDGE ( 'NONE', *, *, #3353, .F. ) ;
#18141=ORIENTED_EDGE ( 'NONE', *, *, #12803, .T. ) ;
#18143=ORIENTED_EDGE ( 'NONE', *, *, #14122, .F. ) ;
#18144=CARTESIAN_POINT ( 'NONE',  ( 0.07181523211953112773, 23.19431517146946931, -10.24584646439514657 ) ) ;
#18149=DIRECTION ( 'NONE',  ( 1.000000000000000000, 0.000000000000000000, 0.000000000000000000 ) ) ;
#18157=ORIENTED_EDGE ( 'NONE', *, *, #12794, .T. ) ;
#18159=CARTESIAN_POINT ( 'NONE',  ( 0.5321745087963413168, -24.44564404695853455, 11.58891744060097295 ) ) ;
#18160=CARTESIAN_POINT ( 'NONE',  ( 2.789999999999999147, -16.37294372382844543, -18.55949924794910544 ) ) ;
#18164=CARTESIAN_POINT ( 'NONE',  ( 8.000000000000000000, 0.000000000000000000, 0.000000000000000000 ) ) ;
#18179=CARTESIAN_POINT ( 'NONE',  ( 0.02436607992776108206, -24.15498966839966855, 5.391175441198523544 ) ) ;
#18182=EDGE_LOOP ( 'NONE', ( #10536, #5608, #4513, #8871, #3978, #3383, #4159, #5611 ) ) ;
#18186=CARTESIAN_POINT ( 'NONE',  ( 0.000000000000000000, 15.74360496233409634, -18.28042085475261302 ) ) ;
#18189=ORIENTED_EDGE ( 'NONE', *, *, #12127, .T. ) ;
#18191=CYLINDRICAL_SURFACE ( 'NONE', #14596, 28.06981291497571362 ) ;
#18192=CARTESIAN_POINT ( 'NONE',  ( 0.8956445960621760571, 24.59653223688280121, 12.96989951879416125 ) ) ;
#18195=LINE ( 'NONE', #9091, #2452 ) ;
#18198=CARTESIAN_POINT ( 'NONE',  ( 2.351340098004231383, 23.41653927703715965, 12.93238701107315514 ) ) ;
#18202=DIRECTION ( 'NONE',  ( 0.000000000000000000, 0.3090169943749350723, 0.9510565162951576390 ) ) ;
#18213=CARTESIAN_POINT ( 'NONE',  ( 2.783068945535915439, 24.42321038836782776, -2.248820353273055517 ) ) ;
#18215=CARTESIAN_POINT ( 'NONE',  ( -7.940452095251188120E-14, -18.34439787333518268, 15.96555658743757000 ) ) ;
#18219=CARTESIAN_POINT ( 'NONE',  ( 2.789999999999999147, 18.28042085475301093, -15.74360496233361673 ) ) ;
#18220=EDGE_CURVE ( 'NONE', #17227, #16305, #10605, .T. ) ;
#18226=CARTESIAN_POINT ( 'NONE',  ( 2.783069004973551142, 5.408431875071779693, -23.92277630352788975 ) ) ;
#18229=CARTESIAN_POINT ( 'NONE',  ( -10.00000000000000000, 0.000000000000000000, 0.000000000000000000 ) ) ;
#18234=CARTESIAN_POINT ( 'NONE',  ( 1.039999999999995817, 4.633866840648921404, 27.68468304288260029 ) ) ;
#18241=CARTESIAN_POINT ( 'NONE',  ( 1.749999999999998002, 4.147968289691286614, 27.76164181293053090 ) ) ;
#18245=CARTESIAN_POINT ( 'NONE',  ( 1.039999999999996039, 19.67366047555559305, -20.02152543075323976 ) ) ;
#18252=ADVANCED_FACE ( 'NONE', ( #8536 ), #1221, .T. ) ;
#18253=EDGE_LOOP ( 'NONE', ( #2844, #8019, #19781, #9150, #15701, #6391 ) ) ;
#18255=DIRECTION ( 'NONE',  ( 0.000000000000000000, 0.000000000000000000, 1.000000000000000000 ) ) ;
#18256=ORIENTED_EDGE ( 'NONE', *, *, #16686, .F. ) ;
#18261=ADVANCED_FACE ( 'NONE', ( #11444 ), #11631, .T. ) ;
#18262=CARTESIAN_POINT ( 'NONE',  ( 1.039999999999998259, 12.52377138324223615, 25.12109765559657859 ) ) ;
#18266=CARTESIAN_POINT ( 'NONE',  ( 2.718184743034447681, -5.344212458769196594, -24.78695292654926519 ) ) ;
#18268=VERTEX_POINT ( 'NONE', #19324 ) ;
#18276=CIRCLE ( 'NONE', #10285, 4.000000000000000000 ) ;
#18277=ORIENTED_EDGE ( 'NONE', *, *, #263, .F. ) ;
#18280=STYLED_ITEM ( 'NONE', ( #18770 ), #2500 ) ;
#18287=CARTESIAN_POINT ( 'NONE',  ( 0.8291131470075423504, 24.44424927289185945, 12.96989951879416125 ) ) ;
#18289=CARTESIAN_POINT ( 'NONE',  ( 1.749999999999998002, -12.96210679857767367, -24.89775460606847091 ) ) ;
#18290=TOROIDAL_SURFACE ( 'NONE', #1034, 24.12539914357697768, 8.000000000000000000 ) ;
#18291=DIRECTION ( 'NONE',  ( -1.000000000000000000, -0.000000000000000000, -0.000000000000000000 ) ) ;
#18292=CARTESIAN_POINT ( 'NONE',  ( 0.07181525068722571792, -25.22524549359951962, 2.576941577947320372 ) ) ;
#18296=ORIENTED_EDGE ( 'NONE', *, *, #19212, .T. ) ;
#18298=AXIS2_PLACEMENT_3D ( 'NONE', #10780, #15779, #2063 ) ;
#18306=LINE ( 'NONE', #16511, #6172 ) ;
#18308=AXIS2_PLACEMENT_3D ( 'NONE', #9250, #4642, #13949 ) ;
#18309=DIRECTION ( 'NONE',  ( -1.000000000000000000, 0.000000000000000000, 0.000000000000000000 ) ) ;
#18315=CARTESIAN_POINT ( 'NONE',  ( 1.749999999999998002, 27.76164181293051669, -4.147968289691384314 ) ) ;
#18318=VERTEX_POINT ( 'NONE', #117 ) ;
#18320=VECTOR ( 'NONE', #11123, 1000.000000000000000 ) ;
#18325=ORIENTED_EDGE ( 'NONE', *, *, #3982, .F. ) ;
#18329=CARTESIAN_POINT ( 'NONE',  ( 2.789999999999999147, -15.04425356660744839, -20.70663861606288236 ) ) ;
#18335=VERTEX_POINT ( 'NONE', #10823 ) ;
#18343=DIRECTION ( 'NONE',  ( -1.000000000000000000, -0.000000000000000000, -0.000000000000000000 ) ) ;
#18357=CARTESIAN_POINT ( 'NONE',  ( 2.789999999999999147, -12.59161484032927092, 21.30679549418627161 ) ) ;
#18360=EDGE_CURVE ( 'NONE', #17134, #19326, #18276, .T. ) ;
#18365=ORIENTED_EDGE ( 'NONE', *, *, #4801, .T. ) ;
#18368=CARTESIAN_POINT ( 'NONE',  ( 0.1882238552569852619, 10.68696068830407420, 23.64332819722385182 ) ) ;
#18374=ORIENTED_EDGE ( 'NONE', *, *, #4002, .F. ) ;
#18379=ORIENTED_EDGE ( 'NONE', *, *, #7851, .F. ) ;
#18380=ORIENTED_EDGE ( 'NONE', *, *, #11763, .T. ) ;
#18381=DIRECTION ( 'NONE',  ( 0.000000000000000000, 0.9510565162951498674, 0.3090169943749583870 ) ) ;
#18384=CARTESIAN_POINT ( 'NONE',  ( 2.783068961317272993, 12.53626894672858683, -21.08061549536601476 ) ) ;
#18386=FACE_OUTER_BOUND ( 'NONE', #361, .T. ) ;
#18387=EDGE_CURVE ( 'NONE', #10556, #11614, #2883, .T. ) ;
#18389=CIRCLE ( 'NONE', #9781, 28.06981291497571362 ) ;
#18390=CARTESIAN_POINT ( 'NONE',  ( 2.071132347512118166, 24.19190980169967631, 12.96989951879416658 ) ) ;
#18402=CARTESIAN_POINT ( 'NONE',  ( 2.790000000000000036, -23.69843731927165109, -5.456805104201351675 ) ) ;
#18403=ORIENTED_EDGE ( 'NONE', *, *, #5425, .T. ) ;
#18405=FACE_OUTER_BOUND ( 'NONE', #4955, .T. ) ;
#18406=DIRECTION ( 'NONE',  ( 1.000000000000000000, 0.000000000000000000, 0.000000000000000000 ) ) ;
#18407=VERTEX_POINT ( 'NONE', #11020 ) ;
#18408=CARTESIAN_POINT ( 'NONE',  ( 1.039999999999997593, 0.000000000000000000, 0.000000000000000000 ) ) ;
#18413=DIRECTION ( 'NONE',  ( 0.000000000000000000, 0.000000000000000000, 1.000000000000000000 ) ) ;
#18414=B_SPLINE_CURVE_WITH_KNOTS ( 'NONE', 3,
 ( #1688, #1880, #6457, #15301, #13992, #9291 ),
 .UNSPECIFIED., .F., .F.,
 ( 4, 2, 4 ),
 ( 1.979325885387340151E-07, 0.001878588715165610589, 0.003756979497742682708 ),
 .UNSPECIFIED. ) ;
#18420=VERTEX_POINT ( 'NONE', #2108 ) ;
#18433=VERTEX_POINT ( 'NONE', #9624 ) ;
#18437=CARTESIAN_POINT ( 'NONE',  ( 2.789999999999999147, 2.680914349914567470E-13, -25.59481291497571220 ) ) ;
#18438=CARTESIAN_POINT ( 'NONE',  ( 1.039999999999998925, -4.147968289691484678, 27.76164181293050248 ) ) ;
#18439=ORIENTED_EDGE ( 'NONE', *, *, #17494, .T. ) ;
#18440=CARTESIAN_POINT ( 'NONE',  ( 0.06555561860988173839, 21.84113606038307509, 12.72236714503170596 ) ) ;
#18444=ORIENTED_EDGE ( 'NONE', *, *, #11467, .F. ) ;
#18447=CARTESIAN_POINT ( 'NONE',  ( 2.789999999999999147, 0.000000000000000000, 0.000000000000000000 ) ) ;
#18452=CARTESIAN_POINT ( 'NONE',  ( 1.749999999999998002, -25.12109765559643648, -12.52377138324252570 ) ) ;
#18453=AXIS2_PLACEMENT_3D ( 'NONE', #14431, #11615, #11712 ) ;
#18456=CIRCLE ( 'NONE', #10469, 2.524999999999995914 ) ;
#18461=B_SPLINE_CURVE_WITH_KNOTS ( 'NONE', 3,
 ( #9144, #10544, #135, #15250, #19534, #18438 ),
 .UNSPECIFIED., .F., .F.,
 ( 4, 2, 4 ),
 ( 2.132675795041204291E-07, 0.001878604073277003036, 0.003756994878974502169 ),
 .UNSPECIFIED. ) ;
#18463=ORIENTED_EDGE ( 'NONE', *, *, #16725, .T. ) ;
#18468=EDGE_LOOP ( 'NONE', ( #13268, #1711, #15661, #12642 ) ) ;
#18471=CARTESIAN_POINT ( 'NONE',  ( -7.595268335593441642E-14, -22.38018801136484015, 9.515416771311118183 ) ) ;
#18473=CARTESIAN_POINT ( 'NONE',  ( 2.789999999999999147, 0.000000000000000000, 0.000000000000000000 ) ) ;
#18474=ORIENTED_EDGE ( 'NONE', *, *, #17608, .F. ) ;
#18477=CYLINDRICAL_SURFACE ( 'NONE', #13809, 13.19999999999999929 ) ;
#18478=ORIENTED_EDGE ( 'NONE', *, *, #11474, .T. ) ;
#18483=CARTESIAN_POINT ( 'NONE',  ( 0.02436607992776151574, -16.37294372382871188, 18.55949924794887096 ) ) ;
#18489=VERTEX_POINT ( 'NONE', #3612 ) ;
#18494=AXIS2_PLACEMENT_3D ( 'NONE', #1437, #1535, #7623 ) ;
#18495=FACE_OUTER_BOUND ( 'NONE', #3234, .T. ) ;
#18500=CARTESIAN_POINT ( 'NONE',  ( 0.5321745227542249435, 18.57583492944418779, 19.66801664102709779 ) ) ;
#18519=EDGE_CURVE ( 'NONE', #16090, #19316, #1646, .T. ) ;
#18523=B_SPLINE_CURVE_WITH_KNOTS ( 'NONE', 3,
 ( #3541, #12362, #3643, #3348 ),
 .UNSPECIFIED., .F., .F.,
 ( 4, 4 ),
 ( 0.0006045424356928436873, 0.0006887909409525051459 ),
 .UNSPECIFIED. ) ;
#18535=ADVANCED_FACE ( 'NONE', ( #7906 ), #4845, .T. ) ;
#18536=CARTESIAN_POINT ( 'NONE',  ( 2.789999999999999147, 7.909232158574813099, 24.34211360614303388 ) ) ;
#18539=CARTESIAN_POINT ( 'NONE',  ( 0.000000000000000000, 7.909232158575156824, -24.34211360614291664 ) ) ;
#18545=VERTEX_POINT ( 'NONE', #2011 ) ;
#18546=DIRECTION ( 'NONE',  ( -1.000000000000000000, -0.000000000000000000, -0.000000000000000000 ) ) ;
#18550=ADVANCED_FACE ( 'NONE', ( #2492 ), #9974, .T. ) ;
#18557=ORIENTED_EDGE ( 'NONE', *, *, #11534, .T. ) ;
#18562=EDGE_CURVE ( 'NONE', #19081, #4439, #6424, .T. ) ;
#18566=AXIS2_PLACEMENT_3D ( 'NONE', #11241, #6617, #17447 ) ;
#18569=CARTESIAN_POINT ( 'NONE',  ( 2.789999999999999147, 15.04425356660790136, -20.70663861606255196 ) ) ;
#18571=CARTESIAN_POINT ( 'NONE',  ( 2.604434283110813375, -12.84444904262041121, 22.53097606932980312 ) ) ;
#18572=ORIENTED_EDGE ( 'NONE', *, *, #14706, .T. ) ;
#18577=CARTESIAN_POINT ( 'NONE',  ( 2.257825462012207129, -12.96514671151749631, -23.74442027961374890 ) ) ;
#18582=AXIS2_PLACEMENT_3D ( 'NONE', #313, #6392, #9731 ) ;
#18585=CARTESIAN_POINT ( 'NONE',  ( 0.000000000000000000, 0.000000000000000000, 0.000000000000000000 ) ) ;
#18586=CARTESIAN_POINT ( 'NONE',  ( 0.000000000000000000, -9.324097380959594616, 22.25075486061734509 ) ) ;
#18587=VERTEX_POINT ( 'NONE', #17614 ) ;
#18591=CARTESIAN_POINT ( 'NONE',  ( 2.789999999999999147, -19.91106274590503844, -14.18181402625762821 ) ) ;
#18594=VERTEX_POINT ( 'NONE', #5688 ) ;
#18599=CIRCLE ( 'NONE', #3904, 2.524999999999996358 ) ;
#18604=AXIS2_PLACEMENT_3D ( 'NONE', #14986, #14891, #19480 ) ;
#18606=EDGE_LOOP ( 'NONE', ( #1698, #9612, #15257, #1476, #12504, #10574 ) ) ;
#18607=ADVANCED_FACE ( 'NONE', ( #5498 ), #11886, .T. ) ;
#18612=CARTESIAN_POINT ( 'NONE',  ( 1.039999999999999369, -12.52377138324206918, -25.12109765559666741 ) ) ;
#18613=ORIENTED_EDGE ( 'NONE', *, *, #11519, .F. ) ;
#18615=EDGE_CURVE ( 'NONE', #19204, #10556, #12929, .T. ) ;
#18622=CARTESIAN_POINT ( 'NONE',  ( 0.006931069955679173590, 18.43696893154758598, 16.17493693894884998 ) ) ;
#18627=VERTEX_POINT ( 'NONE', #1105 ) ;
#18630=CARTESIAN_POINT ( 'NONE',  ( 2.718131864678288601, 2.577209017047007666, 25.22589920183362722 ) ) ;
#18635=ORIENTED_EDGE ( 'NONE', *, *, #892, .F. ) ;
#18638=B_SPLINE_CURVE_WITH_KNOTS ( 'NONE', 3,
 ( #8961, #15162, #7540, #13661, #18266, #4551 ),
 .UNSPECIFIED., .F., .F.,
 ( 4, 2, 4 ),
 ( 4.462636678112536814E-07, 0.001879885020955181143, 0.003759323778242551310 ),
 .UNSPECIFIED. ) ;
#18639=LINE ( 'NONE', #9546, #12655 ) ;
#18641=VERTEX_POINT ( 'NONE', #14420 ) ;
#18645=CARTESIAN_POINT ( 'NONE',  ( 2.718184767880471142, 10.24584646439571500, -23.19431517146922417 ) ) ;
#18647=VECTOR ( 'NONE', #14908, 1000.000000000000000 ) ;
#18654=ORIENTED_EDGE ( 'NONE', *, *, #13316, .F. ) ;
#18660=B_SPLINE_CURVE_WITH_KNOTS ( 'NONE', 3,
 ( #15642, #3528, #10843, #9644 ),
 .UNSPECIFIED., .F., .F.,
 ( 4, 4 ),
 ( 2.034713381942717888E-07, 0.0006887909409525252036 ),
 .UNSPECIFIED. ) ;
#18664=CIRCLE ( 'NONE', #7150, 2.524999999999996358 ) ;
#18669=DIRECTION ( 'NONE',  ( -1.000000000000000000, -0.000000000000000000, -0.000000000000000000 ) ) ;
#18671=CARTESIAN_POINT ( 'NONE',  ( 0.07186811453410638095, -16.91241718342012490, 18.89333555428548905 ) ) ;
#18676=VERTEX_POINT ( 'NONE', #10026 ) ;
#18677=ORIENTED_EDGE ( 'NONE', *, *, #11519, .T. ) ;
#18683=CARTESIAN_POINT ( 'NONE',  ( 0.006931111373678406143, -9.685942809247212182, 22.53293026234500473 ) ) ;
#18693=FACE_OUTER_BOUND ( 'NONE', #4782, .T. ) ;
#18695=DIRECTION ( 'NONE',  ( 0.000000000000000000, 0.5877852522924629231, 0.8090169943749548898 ) ) ;
#18701=ORIENTED_EDGE ( 'NONE', *, *, #15251, .T. ) ;
#18707=CARTESIAN_POINT ( 'NONE',  ( 0.7592463834391192101, -12.05220173035421993, -24.80264696524895385 ) ) ;
#18708=EDGE_CURVE ( 'NONE', #9066, #1328, #2623, .T. ) ;
#18711=B_SPLINE_CURVE_WITH_KNOTS ( 'NONE', 3,
 ( #7858, #671, #2161, #9683, #15775, #14170 ),
 .UNSPECIFIED., .F., .F.,
 ( 4, 2, 4 ),
 ( 4.462636677693390501E-07, 0.001879885020955133004, 0.003759323778242496666 ),
 .UNSPECIFIED. ) ;
#18717=CARTESIAN_POINT ( 'NONE',  ( 0.000000000000000000, 9.324097380959415204, 22.25075486061743391 ) ) ;
#18718=CARTESIAN_POINT ( 'NONE',  ( 1.039999999999995373, -12.96210679857767900, -24.89775460606846380 ) ) ;
#18719=VERTEX_POINT ( 'NONE', #12005 ) ;
#18729=DIRECTION ( 'NONE',  ( -1.000000000000000000, -0.000000000000000000, 0.000000000000000000 ) ) ;
#18731=VERTEX_POINT ( 'NONE', #13700 ) ;
#18736=CIRCLE ( 'NONE', #14273, 2.524999999999995914 ) ;
#18739=EDGE_CURVE ( 'NONE', #3268, #14183, #428, .T. ) ;
#18755=CARTESIAN_POINT ( 'NONE',  ( 0.3599332783571699279, -23.15620303736534069, 12.90954937922492007 ) ) ;
#18757=LINE ( 'NONE', #17069, #11749 ) ;
#18759=EDGE_CURVE ( 'NONE', #1519, #17434, #15201, .T. ) ;
#18761=CARTESIAN_POINT ( 'NONE',  ( 2.718184767880468478, 23.19431517146933430, 10.24584646439546987 ) ) ;
#18765=CIRCLE ( 'NONE', #17490, 2.524999999999995914 ) ;
#18770=PRESENTATION_STYLE_ASSIGNMENT (( #16590 ) ) ;
#18773=VERTEX_POINT ( 'NONE', #6181 ) ;
#18780=CIRCLE ( 'NONE', #11757, 2.524999999999996803 ) ;
#18784=ORIENTED_EDGE ( 'NONE', *, *, #17761, .T. ) ;
#18785=DIRECTION ( 'NONE',  ( 0.000000000000000000, 0.000000000000000000, 1.000000000000000000 ) ) ;
#18793=DIRECTION ( 'NONE',  ( 1.000000000000000000, -0.000000000000000000, -0.000000000000000000 ) ) ;
#18795=CARTESIAN_POINT ( 'NONE',  ( 0.02436607992776325046, 16.37294372382858398, 18.55949924794898465 ) ) ;
#18797=EDGE_LOOP ( 'NONE', ( #12682, #1841, #5592, #19154, #8170, #9568, #13953 ) ) ;
#18803=CARTESIAN_POINT ( 'NONE',  ( 0.000000000000000000, -22.25075486061732732, -9.324097380959701198 ) ) ;
#18808=ORIENTED_EDGE ( 'NONE', *, *, #4328, .F. ) ;
#18810=CARTESIAN_POINT ( 'NONE',  ( 0.1882238552569854284, -10.68696068830390900, -23.64332819722392287 ) ) ;
#18816=CARTESIAN_POINT ( 'NONE',  ( 1.894165461959355756, 24.59696699259432151, 12.96989951879416303 ) ) ;
#18827=LINE ( 'NONE', #15634, #19403 ) ;
#18833=DIRECTION ( 'NONE',  ( 1.000000000000000000, 0.000000000000000000, 0.000000000000000000 ) ) ;
#18837=CARTESIAN_POINT ( 'NONE',  ( 0.006931054464086492187, 24.42321038836783131, 2.248820353273056405 ) ) ;
#18838=DIRECTION ( 'NONE',  ( -1.000000000000000000, 0.000000000000000000, 0.000000000000000000 ) ) ;
#18840=CYLINDRICAL_SURFACE ( 'NONE', #3277, 13.19999999999999574 ) ;
#18843=ORIENTED_EDGE ( 'NONE', *, *, #167, .T. ) ;
#18850=ORIENTED_EDGE ( 'NONE', *, *, #6032, .T. ) ;
#18856=CARTESIAN_POINT ( 'NONE',  ( -8.051804217113518143E-16, 5.456805104201102985, 23.69843731927169728 ) ) ;
#18862=TOROIDAL_SURFACE ( 'NONE', #10875, 24.12539914357697768, 8.000000000000000000 ) ;
#18863=VECTOR ( 'NONE', #8837, 1000.000000000000000 ) ;
#18864=CARTESIAN_POINT ( 'NONE',  ( 1.039999999999996927, 20.02152543075374069, -19.67366047555508501 ) ) ;
#18870=ADVANCED_FACE ( 'NONE', ( #14191 ), #6567, .T. ) ;
#18892=DIRECTION ( 'NONE',  ( 0.000000000000000000, 0.000000000000000000, 1.000000000000000000 ) ) ;
#18895=ORIENTED_EDGE ( 'NONE', *, *, #13204, .F. ) ;
#18903=EDGE_LOOP ( 'NONE', ( #4887, #4938, #12136, #15067, #1299, #9919 ) ) ;
#18904=DIRECTION ( 'NONE',  ( -1.000000000000000000, -0.000000000000000000, 0.000000000000000000 ) ) ;
#18912=VECTOR ( 'NONE', #7148, 1000.000000000000000 ) ;
#18914=DIRECTION ( 'NONE',  ( 0.000000000000000000, 0.000000000000000000, 1.000000000000000000 ) ) ;
#18916=B_SPLINE_CURVE_WITH_KNOTS ( 'NONE', 3,
 ( #15096, #4481, #4585, #7672 ),
 .UNSPECIFIED., .F., .F.,
 ( 4, 4 ),
 ( 2.034713381942770827E-07, 0.0006887909409525120848 ),
 .UNSPECIFIED. ) ;
#18925=ORIENTED_EDGE ( 'NONE', *, *, #7632, .F. ) ;
#18926=CARTESIAN_POINT ( 'NONE',  ( 1.749999999999998002, 4.147968289691286614, 27.76164181293053090 ) ) ;
#18931=DIRECTION ( 'NONE',  ( -1.000000000000000000, -0.000000000000000000, -0.000000000000000000 ) ) ;
#18935=VERTEX_POINT ( 'NONE', #2080 ) ;
#18944=DIRECTION ( 'NONE',  ( 1.000000000000000000, 0.000000000000000000, 0.000000000000000000 ) ) ;
#18947=ADVANCED_FACE ( 'NONE', ( #18495 ), #18290, .T. ) ;
#18955=ORIENTED_EDGE ( 'NONE', *, *, #4214, .T. ) ;
#18958=CARTESIAN_POINT ( 'NONE',  ( 8.000000000000000000, 0.000000000000000000, 0.000000000000000000 ) ) ;
#18961=CARTESIAN_POINT ( 'NONE',  ( 2.257825491203654611, 24.44564404695844573, 11.58891744060115947 ) ) ;
#18969=EDGE_CURVE ( 'NONE', #6839, #10551, #17687, .T. ) ;
#18979=DIRECTION ( 'NONE',  ( -1.000000000000000000, -0.000000000000000000, 0.000000000000000000 ) ) ;
#18980=CARTESIAN_POINT ( 'NONE',  ( 0.02436607992776238310, -12.59161484032927092, 21.30679549418627161 ) ) ;
#18987=EDGE_CURVE ( 'NONE', #12173, #3750, #12120, .T. ) ;
#18991=CARTESIAN_POINT ( 'NONE',  ( 0.07186811453410632544, -18.89333555428542155, -16.91241718342019951 ) ) ;
#19003=CARTESIAN_POINT ( 'NONE',  ( 2.789999999999999147, -18.55949924794904504, 16.37294372382852004 ) ) ;
#19017=DIRECTION ( 'NONE',  ( 0.000000000000000000, 0.000000000000000000, 1.000000000000000000 ) ) ;
#19022=ORIENTED_EDGE ( 'NONE', *, *, #10725, .F. ) ;
#19030=DIRECTION ( 'NONE',  ( -1.000000000000000000, -0.000000000000000000, -0.000000000000000000 ) ) ;
#19036=DIRECTION ( 'NONE',  ( -1.000000000000000000, 0.000000000000000000, 0.000000000000000000 ) ) ;
#19037=VERTEX_POINT ( 'NONE', #5569 ) ;
#19041=CARTESIAN_POINT ( 'NONE',  ( 0.7592463896980138349, 19.86438386685688684, -19.12676442129323107 ) ) ;
#19049=ORIENTED_EDGE ( 'NONE', *, *, #5386, .F. ) ;
#19058=ORIENTED_EDGE ( 'NONE', *, *, #1740, .F. ) ;
#19061=ORIENTED_EDGE ( 'NONE', *, *, #18008, .T. ) ;
#19068=CIRCLE ( 'NONE', #15566, 2.524999999999996358 ) ;
#19072=VERTEX_POINT ( 'NONE', #2281 ) ;
#19080=VECTOR ( 'NONE', #8166, 1000.000000000000000 ) ;
#19081=VERTEX_POINT ( 'NONE', #9804 ) ;
#19089=CARTESIAN_POINT ( 'NONE',  ( 2.789999999999999147, 20.70663861606272249, 15.04425356660767932 ) ) ;
#19091=B_SPLINE_CURVE_WITH_KNOTS ( 'NONE', 3,
 ( #10863, #9070, #10765, #1560, #19665, #4462 ),
 .UNSPECIFIED., .F., .F.,
 ( 4, 2, 4 ),
 ( 2.132675795048140697E-07, 0.001878604073277005205, 0.003756994878974505639 ),
 .UNSPECIFIED. ) ;
#19098=CARTESIAN_POINT ( 'NONE',  ( -10.00000000000000000, 0.000000000000000000, 0.000000000000000000 ) ) ;
#19103=EDGE_CURVE ( 'NONE', #10889, #6099, #8998, .T. ) ;
#19105=B_SPLINE_CURVE_WITH_KNOTS ( 'NONE', 3,
 ( #16956, #3236, #144, #15260 ),
 .UNSPECIFIED., .F., .F.,
 ( 4, 4 ),
 ( 3.059063720760159520E-07, 0.0006888942284914164422 ),
 .UNSPECIFIED. ) ;
#19111=CARTESIAN_POINT ( 'NONE',  ( 0.000000000000000000, 15.04425356660790136, -20.70663861606255196 ) ) ;
#19112=DIRECTION ( 'NONE',  ( -1.000000000000000000, -0.000000000000000000, -0.000000000000000000 ) ) ;
#19113=ORIENTED_EDGE ( 'NONE', *, *, #18360, .T. ) ;
#19119=B_SPLINE_CURVE_WITH_KNOTS ( 'NONE', 3,
 ( #665, #12573, #18961, #2256, #18761, #6639 ),
 .UNSPECIFIED., .F., .F.,
 ( 4, 2, 4 ),
 ( 4.462636882235905044E-07, 0.001879885203074807597, 0.003759324142461391294 ),
 .UNSPECIFIED. ) ;
#19122=ADVANCED_FACE ( 'NONE', ( #2967 ), #19376, .T. ) ;
#19124=CARTESIAN_POINT ( 'NONE',  ( 0.07186815222488071586, -5.344160105508533931, -24.78765742476144140 ) ) ;
#19130=CARTESIAN_POINT ( 'NONE',  ( 0.000000000000000000, 24.04302995059966719, 1.991882183130389228 ) ) ;
#19134=ADVANCED_FACE ( 'NONE', ( #19474 ), #1049, .T. ) ;
#19147=CARTESIAN_POINT ( 'NONE',  ( 0.02436607992776021470, 21.30679549418649543, -12.59161484032888723 ) ) ;
#19154=ORIENTED_EDGE ( 'NONE', *, *, #12035, .F. ) ;
#19157=ORIENTED_EDGE ( 'NONE', *, *, #11944, .T. ) ;
#19171=CARTESIAN_POINT ( 'NONE',  ( 1.749999999999998002, -19.67366047555515252, -20.02152543075368030 ) ) ;
#19178=CARTESIAN_POINT ( 'NONE',  ( 2.718131914667133220, -10.24630254990500511, -23.19485392143224445 ) ) ;
#19184=ADVANCED_FACE ( 'NONE', ( #16488, #13373 ), #4177, .F. ) ;
#19191=DIRECTION ( 'NONE',  ( 0.000000000000000000, 0.000000000000000000, 1.000000000000000000 ) ) ;
#19204=VERTEX_POINT ( 'NONE', #11878 ) ;
#19212=EDGE_CURVE ( 'NONE', #8201, #9486, #16170, .T. ) ;
#19214=VERTEX_POINT ( 'NONE', #1472 ) ;
#19216=CARTESIAN_POINT ( 'NONE',  ( 2.031033491000349134, 24.80232951178394885, -12.05173163741697451 ) ) ;
#19222=DIRECTION ( 'NONE',  ( 0.000000000000000000, 0.000000000000000000, 1.000000000000000000 ) ) ;
#19237=ORIENTED_EDGE ( 'NONE', *, *, #15745, .T. ) ;
#19238=AXIS2_PLACEMENT_3D ( 'NONE', #10382, #2757, #14877 ) ;
#19240=CARTESIAN_POINT ( 'NONE',  ( 2.765633920072236851, -22.71065055754445439, -9.836394144775947979 ) ) ;
#19241=AXIS2_PLACEMENT_3D ( 'NONE', #7363, #10401, #19191 ) ;
#19260=CYLINDRICAL_SURFACE ( 'NONE', #12869, 13.20000000000000284 ) ;
#19262=ORIENTED_EDGE ( 'NONE', *, *, #4815, .T. ) ;
#19265=CARTESIAN_POINT ( 'NONE',  ( 0.006931111373678920488, 22.53293026234503316, 9.685942809247130469 ) ) ;
#19267=ORIENTED_EDGE ( 'NONE', *, *, #15331, .F. ) ;
#19268=CARTESIAN_POINT ( 'NONE',  ( 0.1882239034349757756, -12.84621645676860702, 22.54313264455009147 ) ) ;
#19269=ORIENTED_EDGE ( 'NONE', *, *, #13372, .T. ) ;
#19278=CARTESIAN_POINT ( 'NONE',  ( 1.394999999999999574, -25.12109765559663188, 12.52377138324214378 ) ) ;
#19281=ADVANCED_FACE ( 'NONE', ( #3263 ), #734, .T. ) ;
#19283=AXIS2_PLACEMENT_3D ( 'NONE', #384, #2081, #8082 ) ;
#19284=ORIENTED_EDGE ( 'NONE', *, *, #4165, .T. ) ;
#19286=DIRECTION ( 'NONE',  ( -1.000000000000000000, -0.000000000000000000, -0.000000000000000000 ) ) ;
#19288=FACE_OUTER_BOUND ( 'NONE', #2126, .T. ) ;
#19290=CARTESIAN_POINT ( 'NONE',  ( 2.601776144743012775, -10.68696068830424473, 23.64332819722378076 ) ) ;
#19293=DIRECTION ( 'NONE',  ( -1.000000000000000000, -0.000000000000000000, -0.000000000000000000 ) ) ;
#19298=CARTESIAN_POINT ( 'NONE',  ( 1.039999999999996927, 4.633866840649313090, -27.68468304288253634 ) ) ;
#19300=CARTESIAN_POINT ( 'NONE',  ( 1.749999999999998002, 0.000000000000000000, 0.000000000000000000 ) ) ;
#19304=CARTESIAN_POINT ( 'NONE',  ( 2.765633920072235519, -18.55949924794880346, -16.37294372382878649 ) ) ;
#19312=CARTESIAN_POINT ( 'NONE',  ( 0.7589665349472707323, -4.828387785247840291, -27.14933624560912762 ) ) ;
#19316=VERTEX_POINT ( 'NONE', #17177 ) ;
#19319=EDGE_CURVE ( 'NONE', #18587, #6920, #8026, .T. ) ;
#19324=CARTESIAN_POINT ( 'NONE',  ( 0.000000000000000000, 5.535312321042724193, 23.48180575137730841 ) ) ;
#19326=VERTEX_POINT ( 'NONE', #6159 ) ;
#19329=CARTESIAN_POINT ( 'NONE',  ( 0.02436607992776498519, -21.30679549418621832, -12.59161484032935618 ) ) ;
#19336=CARTESIAN_POINT ( 'NONE',  ( 1.039999999999997593, 0.000000000000000000, 0.000000000000000000 ) ) ;
#19339=ORIENTED_EDGE ( 'NONE', *, *, #18739, .T. ) ;
#19348=ORIENTED_EDGE ( 'NONE', *, *, #3360, .F. ) ;
#19350=DIRECTION ( 'NONE',  ( 0.000000000000000000, 0.000000000000000000, 1.000000000000000000 ) ) ;
#19352=ADVANCED_FACE ( 'NONE', ( #9575 ), #10331, .T. ) ;
#19359=EDGE_LOOP ( 'NONE', ( #7549, #11233, #12261, #14053 ) ) ;
#19360=CARTESIAN_POINT ( 'NONE',  ( 0.02436607992776368414, -9.836394144775550075, -22.71065055754462492 ) ) ;
#19363=CARTESIAN_POINT ( 'NONE',  ( 0.02436607992775761261, 22.71065055754452544, 9.836394144775786330 ) ) ;
#19364=EDGE_CURVE ( 'NONE', #14825, #5362, #9691, .T. ) ;
#19366=VERTEX_POINT ( 'NONE', #472 ) ;
#19371=AXIS2_PLACEMENT_3D ( 'NONE', #12185, #18291, #13784 ) ;
#19372=ORIENTED_EDGE ( 'NONE', *, *, #8647, .T. ) ;
#19373=CARTESIAN_POINT ( 'NONE',  ( 2.765633920072236851, 24.15498966839963302, 5.391175441198700291 ) ) ;
#19374=VECTOR ( 'NONE', #7280, 1000.000000000000000 ) ;
#19376=CYLINDRICAL_SURFACE ( 'NONE', #1680, 28.06981291497571362 ) ;
#19377=EDGE_CURVE ( 'NONE', #725, #16376, #11281, .T. ) ;
#19379=CARTESIAN_POINT ( 'NONE',  ( 2.765633920072233742, -24.15498966839966855, 5.391175441198523544 ) ) ;
#19381=DIRECTION ( 'NONE',  ( -1.000000000000000000, -0.000000000000000000, -0.000000000000000000 ) ) ;
#19385=CARTESIAN_POINT ( 'NONE',  ( 50.00050000000000239, 0.000000000000000000, 4.000000000000000000 ) ) ;
#19391=AXIS2_PLACEMENT_3D ( 'NONE', #1923, #3524, #12733 ) ;
#19392=ORIENTED_EDGE ( 'NONE', *, *, #12270, .T. ) ;
#19403=VECTOR ( 'NONE', #15536, 1000.000000000000000 ) ;
#19409=ORIENTED_EDGE ( 'NONE', *, *, #2426, .T. ) ;
#19411=ORIENTED_EDGE ( 'NONE', *, *, #12460, .F. ) ;
#19415=DIRECTION ( 'NONE',  ( -1.000000000000000000, -0.000000000000000000, -0.000000000000000000 ) ) ;
#19431=CARTESIAN_POINT ( 'NONE',  ( 2.789999999999999147, -24.44424927289185590, 0.2301004812056573479 ) ) ;
#19439=CARTESIAN_POINT ( 'NONE',  ( 2.789999999999999147, 2.336989772644269436, 24.63872515616083447 ) ) ;
#19442=VERTEX_POINT ( 'NONE', #10167 ) ;
#19451=CARTESIAN_POINT ( 'NONE',  ( 1.749999999999998002, -12.96210679857804671, 24.89775460606827551 ) ) ;
#19455=CARTESIAN_POINT ( 'NONE',  ( 2.789999999999999147, -12.59161484032896361, -21.30679549418645280 ) ) ;
#19463=VECTOR ( 'NONE', #3352, 1000.000000000000000 ) ;
#19465=FACE_OUTER_BOUND ( 'NONE', #10860, .T. ) ;
#19467=CARTESIAN_POINT ( 'NONE',  ( 1.394999999999998685, -27.76164181293049182, -4.147968289691579713 ) ) ;
#19469=CYLINDRICAL_SURFACE ( 'NONE', #1960, 2.524999999999995914 ) ;
#19474=FACE_OUTER_BOUND ( 'NONE', #528, .T. ) ;
#19478=FACE_OUTER_BOUND ( 'NONE', #18797, .T. ) ;
#19480=DIRECTION ( 'NONE',  ( 0.000000000000000000, 0.000000000000000000, 1.000000000000000000 ) ) ;
#19481=VERTEX_POINT ( 'NONE', #15971 ) ;
#19482=DIRECTION ( 'NONE',  ( -1.000000000000000000, 0.000000000000000000, -0.000000000000000000 ) ) ;
#19485=CYLINDRICAL_SURFACE ( 'NONE', #2940, 13.20000000000000284 ) ;
#19487=VERTEX_POINT ( 'NONE', #14670 ) ;
#19488=FACE_OUTER_BOUND ( 'NONE', #13509, .T. ) ;
#19490=CIRCLE ( 'NONE', #12474, 24.12539914357697413 ) ;
#19497=VERTEX_POINT ( 'NONE', #12972 ) ;
#19498=CARTESIAN_POINT ( 'NONE',  ( 2.789999999999999147, 24.04302995059966364, -1.991882183130384121 ) ) ;
#19503=CARTESIAN_POINT ( 'NONE',  ( -10.00000000000000000, 0.000000000000000000, 0.000000000000000000 ) ) ;
#19504=ORIENTED_EDGE ( 'NONE', *, *, #2648, .F. ) ;
#19505=AXIS2_PLACEMENT_3D ( 'NONE', #9155, #14956, #8856 ) ;
#19508=CARTESIAN_POINT ( 'NONE',  ( 0.000000000000000000, -1.991882183130148087, -24.04302995059968140 ) ) ;
#19510=B_SPLINE_CURVE_WITH_KNOTS ( 'NONE', 3,
 ( #8189, #6282, #18500, #10901, #14197, #18795 ),
 .UNSPECIFIED., .F., .F.,
 ( 4, 2, 4 ),
 ( 4.462636793131339774E-07, 0.001879885123570645012, 0.003759323983461976965 ),
 .UNSPECIFIED. ) ;
#19512=ORIENTED_EDGE ( 'NONE', *, *, #10725, .T. ) ;
#19515=ORIENTED_EDGE ( 'NONE', *, *, #13204, .T. ) ;
#19520=EDGE_LOOP ( 'NONE', ( #9867, #6056, #5072, #17173, #5746, #9385 ) ) ;
#19525=CYLINDRICAL_SURFACE ( 'NONE', #11192, 13.19999999999999929 ) ;
#19527=CARTESIAN_POINT ( 'NONE',  ( 2.257825477245772650, 19.66801664102704095, 18.57583492944426951 ) ) ;
#19534=CARTESIAN_POINT ( 'NONE',  ( 0.7589665283901001480, -3.797536611356509439, 27.31260702007174146 ) ) ;
#19536=AXIS2_PLACEMENT_3D ( 'NONE', #2026, #19030, #5322 ) ;
#19541=ORIENTED_EDGE ( 'NONE', *, *, #7251, .T. ) ;
#19550=ORIENTED_EDGE ( 'NONE', *, *, #15946, .T. ) ;
#19565=ORIENTED_EDGE ( 'NONE', *, *, #840, .T. ) ;
#19568=DIRECTION ( 'NONE',  ( 0.000000000000000000, 0.000000000000000000, 1.000000000000000000 ) ) ;
#19574=DIRECTION ( 'NONE',  ( 0.000000000000000000, 0.000000000000000000, -1.000000000000000000 ) ) ;
#19576=DIRECTION ( 'NONE',  ( -1.000000000000000000, -0.000000000000000000, -0.000000000000000000 ) ) ;
#19581=CARTESIAN_POINT ( 'NONE',  ( 0.000000000000000000, -15.74360496233370021, -18.28042085475294698 ) ) ;
#19586=AXIS2_PLACEMENT_3D ( 'NONE', #3441, #8726, #13325 ) ;
#19594=EDGE_CURVE ( 'NONE', #16863, #10962, #15769, .T. ) ;
#19599=CARTESIAN_POINT ( 'NONE',  ( 2.789999999999999147, 2.680914349914567470E-13, -23.06981291497571362 ) ) ;
#19603=DIRECTION ( 'NONE',  ( 0.000000000000000000, 0.000000000000000000, 1.000000000000000000 ) ) ;
#19605=ORIENTED_EDGE ( 'NONE', *, *, #2228, .F. ) ;
#19609=CARTESIAN_POINT ( 'NONE',  ( 0.02436607992776325046, -18.55949924794904504, 16.37294372382852004 ) ) ;
#19613=CIRCLE ( 'NONE', #9735, 28.06981291497571362 ) ;
#19615=CARTESIAN_POINT ( 'NONE',  ( -7.646929282184496191E-14, 5.456611084822186264, -23.69897269326672884 ) ) ;
#19616=CARTESIAN_POINT ( 'NONE',  ( 1.749999999999998002, 27.68468304288259318, 4.633866840649019103 ) ) ;
#19619=ADVANCED_FACE ( 'NONE', ( #13353 ), #10021, .T. ) ;
#19623=CARTESIAN_POINT ( 'NONE',  ( 0.7589665283900991488, 27.31260702007175567, 3.797536611356412628 ) ) ;
#19624=ORIENTED_EDGE ( 'NONE', *, *, #17074, .T. ) ;
#19627=CARTESIAN_POINT ( 'NONE',  ( 2.718131864678290821, 25.22589920183360945, -2.577209017047097372 ) ) ;
#19628=EDGE_LOOP ( 'NONE', ( #13244, #3553, #8169, #4099, #16890, #13112, #552, #14938 ) ) ;
#19631=FACE_OUTER_BOUND ( 'NONE', #7673, .T. ) ;
#19636=VERTEX_POINT ( 'NONE', #19451 ) ;
#19639=CARTESIAN_POINT ( 'NONE',  ( 0.5321745087963410947, 24.44564404695860205, -11.58891744060082019 ) ) ;
#19640=CARTESIAN_POINT ( 'NONE',  ( 0.000000000000000000, 7.909232158575156824, -21.81711360614291806 ) ) ;
#19647=CARTESIAN_POINT ( 'NONE',  ( 2.765633920072238183, -5.391175441198789109, 24.15498966839961170 ) ) ;
#19664=CARTESIAN_POINT ( 'NONE',  ( 2.789999999999999147, 0.000000000000000000, 0.000000000000000000 ) ) ;
#19665=CARTESIAN_POINT ( 'NONE',  ( 2.031033471609899888, -3.797536611356125746, -27.31260702007179830 ) ) ;
#19667=ORIENTED_EDGE ( 'NONE', *, *, #17565, .F. ) ;
#19671=VECTOR ( 'NONE', #19036, 1000.000000000000000 ) ;
#19677=EDGE_CURVE ( 'NONE', #15929, #1471, #17592, .T. ) ;
#19679=CIRCLE ( 'NONE', #11063, 2.524999999999995470 ) ;
#19680=EDGE_LOOP ( 'NONE', ( #5918, #16670, #19541, #6046 ) ) ;
#19684=ORIENTED_EDGE ( 'NONE', *, *, #19103, .T. ) ;
#19685=CARTESIAN_POINT ( 'NONE',  ( 2.789999999999999147, 16.37294372382858398, 18.55949924794898465 ) ) ;
#19688=EDGE_CURVE ( 'NONE', #18545, #16477, #1251, .T. ) ;
#19714=DIRECTION ( 'NONE',  ( -1.000000000000000000, -0.000000000000000000, -0.000000000000000000 ) ) ;
#19718=DIRECTION ( 'NONE',  ( -1.000000000000000000, -0.000000000000000000, -0.000000000000000000 ) ) ;
#19720=EDGE_CURVE ( 'NONE', #8429, #4625, #2644, .T. ) ;
#19721=CIRCLE ( 'NONE', #18453, 28.06981291497571007 ) ;
#19735=CARTESIAN_POINT ( 'NONE',  ( 0.006931111373679591826, -22.53293026234497276, -9.685942809247297447 ) ) ;
#19737=DIRECTION ( 'NONE',  ( -1.000000000000000000, 0.000000000000000000, -0.000000000000000000 ) ) ;
#19743=CARTESIAN_POINT ( 'NONE',  ( 0.07181523211953064201, -23.19431517146941246, 10.24584646439529756 ) ) ;
#19761=CIRCLE ( 'NONE', #14666, 28.06981291497571362 ) ;
#19776=DIRECTION ( 'NONE',  ( -1.000000000000000000, 0.000000000000000000, 0.000000000000000000 ) ) ;
#19778=CARTESIAN_POINT ( 'NONE',  ( 1.039999999999996483, -27.76164181293054511, 4.147968289691193355 ) ) ;
#19781=ORIENTED_EDGE ( 'NONE', *, *, #14369, .F. ) ;
ENDSEC;
END-ISO-10303-21;
